ISO-10303-21;
HEADER;
FILE_DESCRIPTION (('STEP AP214'),
    '1' );
FILE_NAME ('Switch Metal Shield Frame.step',
    '2026-10-09T19:32:29',
    ( '' ),
    ( '' ),
    'SwSTEP 2.0',
    'SolidWorks 2026',
    '' );
FILE_SCHEMA (( 'AUTOMOTIVE_DESIGN' ));
ENDSEC;

DATA;
#2=ORIENTED_EDGE ( 'NONE', *, *, #12081, .F. ) ;
#6=VECTOR ( 'NONE', #12765, 1000.000000000000000 ) ;
#9=CYLINDRICAL_SURFACE ( 'NONE', #17623, 0.01000000000000002623 ) ;
#17=EDGE_LOOP ( 'NONE', ( #524, #5810, #763, #9068 ) ) ;
#22=EDGE_LOOP ( 'NONE', ( #588, #1750, #4383 ) ) ;
#27=DIRECTION ( 'NONE',  ( 0.000000000000000000, 0.000000000000000000, -1.000000000000000000 ) ) ;
#36=PLANE ( 'NONE',  #7974 ) ;
#37=VERTEX_POINT ( 'NONE', #9466 ) ;
#41=DIRECTION ( 'NONE',  ( -0.7049180327868849183, 0.7092887755011130224, 8.531426931033447850E-16 ) ) ;
#44=AXIS2_PLACEMENT_3D ( 'NONE', #5027, #10483, #9189 ) ;
#47=ORIENTED_EDGE ( 'NONE', *, *, #18282, .T. ) ;
#55=ORIENTED_EDGE ( 'NONE', *, *, #7049, .T. ) ;
#56=PLANE ( 'NONE',  #5985 ) ;
#69=FACE_OUTER_BOUND ( 'NONE', #15642, .T. ) ;
#80=ORIENTED_EDGE ( 'NONE', *, *, #2571, .F. ) ;
#81=ORIENTED_EDGE ( 'NONE', *, *, #13193, .F. ) ;
#82=CARTESIAN_POINT ( 'NONE',  ( 2.500000000000000000, 10.00000000000000000, 1.600000000000000089 ) ) ;
#87=FILL_AREA_STYLE ('',( #1375 ) ) ;
#101=ORIENTED_EDGE ( 'NONE', *, *, #7303, .T. ) ;
#106=ORIENTED_EDGE ( 'NONE', *, *, #2225, .T. ) ;
#110=CARTESIAN_POINT ( 'NONE',  ( 2.500000000000000000, 11.15000000000000036, -1.135674796306499891E-15 ) ) ;
#112=CARTESIAN_POINT ( 'NONE',  ( 1.889999999999999902, 7.299999999999999822, 0.5999999999999999778 ) ) ;
#113=CARTESIAN_POINT ( 'NONE',  ( 2.500000000000000000, 2.000000000000000000, 1.600000000000000089 ) ) ;
#119=PLANE ( 'NONE',  #9386 ) ;
#121=ORIENTED_EDGE ( 'NONE', *, *, #17653, .F. ) ;
#124=ORIENTED_EDGE ( 'NONE', *, *, #9369, .T. ) ;
#132=EDGE_LOOP ( 'NONE', ( #12967, #8164, #8169, #17199, #14235, #13899, #10080, #12493, #3954, #15631, #1582, #17423, #1346, #16815, #17146, #660 ) ) ;
#134=DIRECTION ( 'NONE',  ( 0.000000000000000000, 1.000000000000000000, -2.081668171172166936E-15 ) ) ;
#139=LINE ( 'NONE', #14116, #7062 ) ;
#142=ORIENTED_EDGE ( 'NONE', *, *, #9998, .T. ) ;
#154=CYLINDRICAL_SURFACE ( 'NONE', #14694, 0.6500000000000003553 ) ;
#155=EDGE_CURVE ( 'NONE', #7849, #17929, #15593, .T. ) ;
#157=CARTESIAN_POINT ( 'NONE',  ( 1.899999999999999911, 4.700000000000000178, 1.600000000000000089 ) ) ;
#161=DIRECTION ( 'NONE',  ( 5.551115123125780730E-16, 1.000000000000000000, 0.000000000000000000 ) ) ;
#173=ADVANCED_FACE ( 'NONE', ( #18226 ), #12517, .F. ) ;
#174=CARTESIAN_POINT ( 'NONE',  ( 1.889999999999999902, 8.500000000000000000, 0.5999999999999999778 ) ) ;
#176=DIRECTION ( 'NONE',  ( 1.000000000000000000, 0.000000000000000000, 0.000000000000000000 ) ) ;
#179=CARTESIAN_POINT ( 'NONE',  ( -1.000000000000000000, 6.400000000000000355, 7.700000000000000178 ) ) ;
#182=CARTESIAN_POINT ( 'NONE',  ( -1.899999999999999911, 7.299999999999999822, 0.6099999999999999867 ) ) ;
#185=ADVANCED_FACE ( 'NONE', ( #9836 ), #11122, .T. ) ;
#186=ORIENTED_EDGE ( 'NONE', *, *, #6092, .T. ) ;
#188=CARTESIAN_POINT ( 'NONE',  ( -2.500000000000000000, 7.299999999999999822, 1.600000000000000089 ) ) ;
#189=CARTESIAN_POINT ( 'NONE',  ( 1.899999999999999911, 9.199999999999999289, 1.600000000000000089 ) ) ;
#198=AXIS2_PLACEMENT_3D ( 'NONE', #9946, #12907, #5782 ) ;
#199=EDGE_CURVE ( 'NONE', #14776, #14634, #1931, .T. ) ;
#205=EDGE_CURVE ( 'NONE', #37, #8434, #9920, .T. ) ;
#211=EDGE_CURVE ( 'NONE', #3339, #16796, #8542, .T. ) ;
#216=EDGE_CURVE ( 'NONE', #16860, #6769, #9644, .T. ) ;
#224=CIRCLE ( 'NONE', #10856, 0.09999999999999939493 ) ;
#226=CIRCLE ( 'NONE', #1107, 0.3999999999999999667 ) ;
#229=VERTEX_POINT ( 'NONE', #1406 ) ;
#237=VECTOR ( 'NONE', #7753, 1000.000000000000000 ) ;
#240=VERTEX_POINT ( 'NONE', #16423 ) ;
#241=AXIS2_PLACEMENT_3D ( 'NONE', #8801, #14538, #6201 ) ;
#242=DIRECTION ( 'NONE',  ( -1.000000000000000000, 1.480297366166879989E-15, 7.401486830834380223E-16 ) ) ;
#248=FACE_OUTER_BOUND ( 'NONE', #10929, .T. ) ;
#252=EDGE_CURVE ( 'NONE', #7890, #13271, #8186, .T. ) ;
#264=CARTESIAN_POINT ( 'NONE',  ( -1.899999999999999911, 7.299999999999999822, 1.600000000000000089 ) ) ;
#285=EDGE_LOOP ( 'NONE', ( #13386, #1128, #2, #3206 ) ) ;
#286=LINE ( 'NONE', #5811, #9790 ) ;
#287=ORIENTED_EDGE ( 'NONE', *, *, #878, .F. ) ;
#289=DIRECTION ( 'NONE',  ( -1.110223024625160090E-15, -1.000000000000000000, 0.000000000000000000 ) ) ;
#290=EDGE_LOOP ( 'NONE', ( #11237, #4760, #6614, #15056 ) ) ;
#291=CIRCLE ( 'NONE', #11810, 0.4000000000000001887 ) ;
#297=DIRECTION ( 'NONE',  ( 2.242874797222539596E-16, 1.794299837778029705E-15, 1.000000000000000000 ) ) ;
#298=DIRECTION ( 'NONE',  ( -1.000000000000000000, 1.850371707708589879E-16, 7.401486830834380223E-16 ) ) ;
#317=AXIS2_PLACEMENT_3D ( 'NONE', #2282, #7935, #16259 ) ;
#319=ORIENTED_EDGE ( 'NONE', *, *, #18192, .F. ) ;
#320=EDGE_CURVE ( 'NONE', #15780, #4246, #13459, .T. ) ;
#321=FACE_OUTER_BOUND ( 'NONE', #2353, .T. ) ;
#327=FACE_OUTER_BOUND ( 'NONE', #394, .T. ) ;
#329=CARTESIAN_POINT ( 'NONE',  ( 1.289999999999999813, 7.900000000000002132, 3.000000000000002220 ) ) ;
#330=EDGE_LOOP ( 'NONE', ( #3061, #9828, #5549, #10787 ) ) ;
#335=CARTESIAN_POINT ( 'NONE',  ( 1.889999999999999902, 3.500000000000000000, -7.771561172376099727E-16 ) ) ;
#338=ORIENTED_EDGE ( 'NONE', *, *, #2122, .F. ) ;
#344=DIRECTION ( 'NONE',  ( 1.708035422500239940E-16, 1.000000000000000000, 5.978123978750840407E-16 ) ) ;
#349=CARTESIAN_POINT ( 'NONE',  ( -1.800000000000000044, 11.40000000000000036, 7.649999999999999467 ) ) ;
#350=CARTESIAN_POINT ( 'NONE',  ( 1.850000000000000089, 0.7500000000000000000, 7.649999999999999467 ) ) ;
#352=EDGE_LOOP ( 'NONE', ( #6999, #6754, #2770, #1267 ) ) ;
#355=PLANE ( 'NONE',  #1395 ) ;
#363=CARTESIAN_POINT ( 'NONE',  ( -0.02999999999999379899, 12.00000000000000000, -2.869354249208270301E-17 ) ) ;
#365=CARTESIAN_POINT ( 'NONE',  ( 1.899999999999999911, 7.299999999999999822, 0.6099999999999999867 ) ) ;
#370=ORIENTED_EDGE ( 'NONE', *, *, #6530, .F. ) ;
#371=DIRECTION ( 'NONE',  ( -1.000000000000000000, 0.000000000000000000, 0.000000000000000000 ) ) ;
#379=EDGE_CURVE ( 'NONE', #14325, #1999, #10215, .T. ) ;
#384=CARTESIAN_POINT ( 'NONE',  ( -1.600000000000000089, -3.475292999508519705E-16, 4.000000000000000000 ) ) ;
#388=FACE_OUTER_BOUND ( 'NONE', #11566, .T. ) ;
#389=VERTEX_POINT ( 'NONE', #1060 ) ;
#394=EDGE_LOOP ( 'NONE', ( #11957, #9883, #11083, #12392 ) ) ;
#396=VERTEX_POINT ( 'NONE', #6700 ) ;
#401=EDGE_LOOP ( 'NONE', ( #12811, #11538, #1032, #13983, #10617, #10576, #15723, #6538 ) ) ;
#402=DIRECTION ( 'NONE',  ( 0.000000000000000000, -1.000000000000000000, -1.332267629550190018E-15 ) ) ;
#405=FACE_OUTER_BOUND ( 'NONE', #8642, .T. ) ;
#406=DIRECTION ( 'NONE',  ( 1.142385477618690076E-14, -1.110223024625153952E-16, 1.000000000000000000 ) ) ;
#410=VERTEX_POINT ( 'NONE', #11050 ) ;
#411=DIRECTION ( 'NONE',  ( 2.220446049250309876E-16, 1.000000000000000000, -1.850371707708599740E-16 ) ) ;
#423=PLANE ( 'NONE',  #3044 ) ;
#427=DIRECTION ( 'NONE',  ( -1.000000000000000000, 0.000000000000000000, 6.123233995736759873E-17 ) ) ;
#432=DIRECTION ( 'NONE',  ( -1.000000000000000000, 1.850371707708589879E-16, 7.401486830834380223E-16 ) ) ;
#435=VERTEX_POINT ( 'NONE', #9942 ) ;
#437=ORIENTED_EDGE ( 'NONE', *, *, #18165, .T. ) ;
#441=ORIENTED_EDGE ( 'NONE', *, *, #14504, .T. ) ;
#444=CARTESIAN_POINT ( 'NONE',  ( -0.5372984490435469551, 4.599999999999999645, 7.700000000000000178 ) ) ;
#451=DIRECTION ( 'NONE',  ( -0.2721173643531200059, -0.9622640697945191723, 0.000000000000000000 ) ) ;
#453=ADVANCED_FACE ( 'NONE', ( #10743 ), #5286, .T. ) ;
#455=ORIENTED_EDGE ( 'NONE', *, *, #14444, .F. ) ;
#470=DIRECTION ( 'NONE',  ( -6.123233995736769734E-17, -0.000000000000000000, -1.000000000000000000 ) ) ;
#475=VERTEX_POINT ( 'NONE', #15390 ) ;
#481=CLOSED_SHELL ( 'NONE', ( #1105, #2707, #9593, #6776, #453, #11667, #7385, #17067, #8138, #15405, #12267, #12757, #9929, #9494, #12651, #4830, #16140, #8466, #10660, #15825, #4528, #1215, #9827, #12773, #4933, #13085, #185, #8268, #11635, #10825, #9835, #17731, #4480, #14796, #4935, #10301, #12187, #10144, #17825, #8156, #17296, #10851, #7547, #10060, #2024, #10760, #7033, #12336, #16058, #1303, #16617, #2049, #15657, #8174, #18268, #10717, #6978, #4586, #7790, #17935, #10266, #3976, #14973, #16625, #13703, #9469, #12597, #1004, #8913, #17259, #1134, #13104, #11381, #542, #2399, #8141, #3638, #14784, #10475, #11632, #17413, #6182, #5439, #4021, #637, #11519, #640, #13095, #2808, #6975, #5978, #17597, #9926, #7014, #12152, #17426, #2903, #9854, #17163, #928, #2476, #15539, #9487, #1231, #11443, #10206, #8402, #9245, #8488, #12540, #15092, #17970, #9951, #905, #10315, #7709, #12982, #2010, #8698, #15268, #13903, #15387, #5590, #1452, #4154, #7892, #3027, #13438, #2170, #8041, #6286, #15148, #12120, #173, #4067, #18029, #7347, #6752, #6683, #5308, #14678, #12014, #16384, #16822, #2892, #6701 ) ) ;
#483=LINE ( 'NONE', #664, #7613 ) ;
#485=ORIENTED_EDGE ( 'NONE', *, *, #13436, .T. ) ;
#486=CARTESIAN_POINT ( 'NONE',  ( -1.899999999999999911, 11.15000000000000036, 7.990820364436479856E-16 ) ) ;
#487=CARTESIAN_POINT ( 'NONE',  ( 1.889999999999999902, 4.100000000000000533, -6.512531667206379696E-16 ) ) ;
#492=CIRCLE ( 'NONE', #4337, 0.5999999999999998668 ) ;
#502=CARTESIAN_POINT ( 'NONE',  ( 1.899999999999999911, 9.199999999999999289, 0.6099999999999999867 ) ) ;
#509=ORIENTED_EDGE ( 'NONE', *, *, #12081, .T. ) ;
#512=CARTESIAN_POINT ( 'NONE',  ( 1.800000000000000044, 11.40000000000000036, 1.600000000000000089 ) ) ;
#514=VECTOR ( 'NONE', #10308, 1000.000000000000000 ) ;
#515=DIRECTION ( 'NONE',  ( 1.059337802663170094E-14, 1.000000000000000000, 1.929541063032960169E-30 ) ) ;
#519=DIRECTION ( 'NONE',  ( 1.000000000000000000, -1.103950578158349959E-14, 0.000000000000000000 ) ) ;
#523=VECTOR ( 'NONE', #3659, 1000.000000000000000 ) ;
#524=ORIENTED_EDGE ( 'NONE', *, *, #10146, .F. ) ;
#525=CARTESIAN_POINT ( 'NONE',  ( 2.500000000000000000, 10.00000000000000000, -5.075305255429290705E-16 ) ) ;
#526=DIRECTION ( 'NONE',  ( -2.220446049250309876E-16, -1.000000000000000000, 4.930380657631319405E-32 ) ) ;
#527=ORIENTED_EDGE ( 'NONE', *, *, #3623, .T. ) ;
#534=CARTESIAN_POINT ( 'NONE',  ( 2.500000000000000000, 9.199999999999999289, 1.600000000000000089 ) ) ;
#536=EDGE_CURVE ( 'NONE', #3882, #3854, #4603, .T. ) ;
#538=AXIS2_PLACEMENT_3D ( 'NONE', #1149, #15052, #18243 ) ;
#540=EDGE_CURVE ( 'NONE', #10260, #6008, #5380, .T. ) ;
#542=ADVANCED_FACE ( 'NONE', ( #18116 ), #8251, .F. ) ;
#543=VECTOR ( 'NONE', #1826, 1000.000000000000000 ) ;
#547=VECTOR ( 'NONE', #6134, 1000.000000000000000 ) ;
#556=EDGE_CURVE ( 'NONE', #14368, #9144, #15286, .T. ) ;
#557=SPHERICAL_SURFACE ( 'NONE', #241, 0.8000000000000000444 ) ;
#559=VECTOR ( 'NONE', #7948, 1000.000000000000000 ) ;
#571=ORIENTED_EDGE ( 'NONE', *, *, #11074, .T. ) ;
#573=ORIENTED_EDGE ( 'NONE', *, *, #11966, .T. ) ;
#574=CARTESIAN_POINT ( 'NONE',  ( 2.616666666666669805, -6.661338147750939243E-16, 7.649999999999999467 ) ) ;
#576=FACE_OUTER_BOUND ( 'NONE', #11007, .T. ) ;
#585=VECTOR ( 'NONE', #11479, 1000.000000000000000 ) ;
#588=ORIENTED_EDGE ( 'NONE', *, *, #1576, .T. ) ;
#589=ORIENTED_EDGE ( 'NONE', *, *, #4710, .F. ) ;
#591=ORIENTED_EDGE ( 'NONE', *, *, #1780, .F. ) ;
#593=CARTESIAN_POINT ( 'NONE',  ( -1.800000000000000044, 12.00000000000000000, 1.600000000000000089 ) ) ;
#594=DIRECTION ( 'NONE',  ( -6.476300976980080477E-16, 9.251858538542978977E-17, -1.000000000000000000 ) ) ;
#595=AXIS2_PLACEMENT_3D ( 'NONE', #12279, #13477, #898 ) ;
#600=CARTESIAN_POINT ( 'NONE',  ( 2.500000000000000000, 11.25000000000000000, 7.649999999999999467 ) ) ;
#605=ORIENTED_EDGE ( 'NONE', *, *, #12076, .T. ) ;
#615=ORIENTED_EDGE ( 'NONE', *, *, #5753, .F. ) ;
#621=PLANE ( 'NONE',  #16828 ) ;
#623=DIRECTION ( 'NONE',  ( 1.000000000000000000, -2.220446049250309876E-16, 0.000000000000000000 ) ) ;
#628=CARTESIAN_POINT ( 'NONE',  ( -1.850000000000000089, 0.7500000000000000000, 7.700000000000000178 ) ) ;
#630=CARTESIAN_POINT ( 'NONE',  ( -2.500000000000000000, 10.00000000000000000, 1.600000000000000089 ) ) ;
#632=ORIENTED_EDGE ( 'NONE', *, *, #4794, .T. ) ;
#633=FACE_OUTER_BOUND ( 'NONE', #18025, .T. ) ;
#634=EDGE_LOOP ( 'NONE', ( #3635, #12875, #12092, #13287 ) ) ;
#635=CARTESIAN_POINT ( 'NONE',  ( -1.899999999999999911, 2.000000000000000000, 1.600000000000000089 ) ) ;
#637=ADVANCED_FACE ( 'NONE', ( #1577 ), #1380, .F. ) ;
#640=ADVANCED_FACE ( 'NONE', ( #9905 ), #12783, .F. ) ;
#642=CARTESIAN_POINT ( 'NONE',  ( -1.899999999999999911, 2.000000000000000000, 1.600000000000000089 ) ) ;
#657=ORIENTED_EDGE ( 'NONE', *, *, #1694, .T. ) ;
#659=EDGE_CURVE ( 'NONE', #4099, #9483, #12309, .T. ) ;
#660=ORIENTED_EDGE ( 'NONE', *, *, #4794, .F. ) ;
#664=CARTESIAN_POINT ( 'NONE',  ( 1.875000000000000000, 12.00000000000000000, 7.700000000000000178 ) ) ;
#666=ORIENTED_EDGE ( 'NONE', *, *, #14756, .T. ) ;
#667=AXIS2_PLACEMENT_3D ( 'NONE', #10886, #9774, #16898 ) ;
#673=EDGE_LOOP ( 'NONE', ( #2543, #4016, #8725, #4883 ) ) ;
#675=LINE ( 'NONE', #16416, #12071 ) ;
#677=AXIS2_PLACEMENT_3D ( 'NONE', #7128, #8673, #12764 ) ;
#684=FACE_OUTER_BOUND ( 'NONE', #16904, .T. ) ;
#691=EDGE_LOOP ( 'NONE', ( #9977, #3355, #6508, #17403, #8904, #10550 ) ) ;
#697=CARTESIAN_POINT ( 'NONE',  ( -2.500000000000000000, 2.000000000000000000, 1.600000000000000089 ) ) ;
#702=ORIENTED_EDGE ( 'NONE', *, *, #16197, .T. ) ;
#703=LINE ( 'NONE', #12194, #7706 ) ;
#709=CARTESIAN_POINT ( 'NONE',  ( -1.800000000000000044, 11.40000000000000036, 7.649999999999999467 ) ) ;
#712=DIRECTION ( 'NONE',  ( 0.000000000000000000, 0.000000000000000000, 1.000000000000000000 ) ) ;
#719=DIRECTION ( 'NONE',  ( 1.000000000000000000, -1.224646799147350002E-16, 0.000000000000000000 ) ) ;
#722=DIRECTION ( 'NONE',  ( 2.114710523095539848E-16, 1.000000000000000000, -8.458842092382139670E-17 ) ) ;
#727=CARTESIAN_POINT ( 'NONE',  ( -0.8740908734716290596, 4.154758922476410099, 7.700000000000000178 ) ) ;
#728=LINE ( 'NONE', #6194, #11194 ) ;
#751=CARTESIAN_POINT ( 'NONE',  ( -1.199999999999880052, 11.40000000000000036, -2.399999999999999911 ) ) ;
#756=ORIENTED_EDGE ( 'NONE', *, *, #4010, .F. ) ;
#757=AXIS2_PLACEMENT_3D ( 'NONE', #3636, #9288, #13742 ) ;
#763=ORIENTED_EDGE ( 'NONE', *, *, #1986, .F. ) ;
#766=AXIS2_PLACEMENT_3D ( 'NONE', #8146, #9443, #5172 ) ;
#767=ORIENTED_EDGE ( 'NONE', *, *, #5410, .F. ) ;
#769=FACE_OUTER_BOUND ( 'NONE', #9696, .T. ) ;
#776=CARTESIAN_POINT ( 'NONE',  ( 1.889999999999999902, 8.500000000000000000, 0.5999999999999999778 ) ) ;
#779=DIRECTION ( 'NONE',  ( 7.401486830834380223E-16, -4.695600626315549922E-31, 1.000000000000000000 ) ) ;
#782=EDGE_CURVE ( 'NONE', #17164, #14972, #13576, .T. ) ;
#783=CARTESIAN_POINT ( 'NONE',  ( 1.889999999999999902, 3.500000000000000000, -6.651892103230508783E-16 ) ) ;
#787=FACE_OUTER_BOUND ( 'NONE', #15263, .T. ) ;
#802=VECTOR ( 'NONE', #10018, 1000.000000000000000 ) ;
#803=AXIS2_PLACEMENT_3D ( 'NONE', #17116, #7059, #2881 ) ;
#807=FACE_OUTER_BOUND ( 'NONE', #12417, .T. ) ;
#808=LINE ( 'NONE', #6450, #6415 ) ;
#812=VECTOR ( 'NONE', #1415, 1000.000000000000000 ) ;
#818=DIRECTION ( 'NONE',  ( 1.000000000000000000, 3.315303352997239924E-31, 0.000000000000000000 ) ) ;
#829=VECTOR ( 'NONE', #11921, 1000.000000000000000 ) ;
#831=VECTOR ( 'NONE', #2430, 1000.000000000000000 ) ;
#834=PLANE ( 'NONE',  #8219 ) ;
#839=VECTOR ( 'NONE', #14410, 1000.000000000000000 ) ;
#841=AXIS2_PLACEMENT_3D ( 'NONE', #7581, #9048, #2022 ) ;
#843=CARTESIAN_POINT ( 'NONE',  ( 0.8740908734716299477, 4.154758922476410099, 7.700000000000000178 ) ) ;
#848=CARTESIAN_POINT ( 'NONE',  ( -1.899999999999999911, 10.00000000000000000, 6.661338147750939243E-16 ) ) ;
#852=DIRECTION ( 'NONE',  ( 0.000000000000000000, 0.000000000000000000, 1.000000000000000000 ) ) ;
#855=DIRECTION ( 'NONE',  ( -1.000000000000000000, 7.401486830834380223E-16, 0.000000000000000000 ) ) ;
#859=ORIENTED_EDGE ( 'NONE', *, *, #8286, .F. ) ;
#867=AXIS2_PLACEMENT_3D ( 'NONE', #11342, #16977, #4289 ) ;
#871=DIRECTION ( 'NONE',  ( 9.588835100573269740E-31, -1.000000000000000000, -3.548581835996780230E-45 ) ) ;
#876=ORIENTED_EDGE ( 'NONE', *, *, #12310, .F. ) ;
#878=EDGE_CURVE ( 'NONE', #4810, #396, #13218, .T. ) ;
#879=AXIS2_PLACEMENT_3D ( 'NONE', #3054, #10353, #4601 ) ;
#883=CARTESIAN_POINT ( 'NONE',  ( 2.616666666666660035, -5.805074450128190455E-17, 4.000000000000000000 ) ) ;
#884=LINE ( 'NONE', #9578, #15287 ) ;
#889=ORIENTED_EDGE ( 'NONE', *, *, #3094, .F. ) ;
#892=LINE ( 'NONE', #17525, #2014 ) ;
#894=ORIENTED_EDGE ( 'NONE', *, *, #5217, .T. ) ;
#898=DIRECTION ( 'NONE',  ( -0.9622640697945192834, -0.2721173643531198949, 0.000000000000000000 ) ) ;
#905=ADVANCED_FACE ( 'NONE', ( #3231, #6187, #7405, #8875 ), #11842, .T. ) ;
#909=PLANE ( 'NONE',  #1757 ) ;
#910=CYLINDRICAL_SURFACE ( 'NONE', #6751, 0.3999999999999999667 ) ;
#912=VECTOR ( 'NONE', #3016, 1000.000000000000000 ) ;
#914=DIRECTION ( 'NONE',  ( -1.000000000000000000, 1.153478467143200106E-14, -8.997169018144999103E-17 ) ) ;
#923=ORIENTED_EDGE ( 'NONE', *, *, #17952, .T. ) ;
#924=ORIENTED_EDGE ( 'NONE', *, *, #12319, .F. ) ;
#928=ADVANCED_FACE ( 'NONE', ( #15069 ), #16017, .F. ) ;
#929=ORIENTED_EDGE ( 'NONE', *, *, #3392, .F. ) ;
#933=CARTESIAN_POINT ( 'NONE',  ( 0.02999999999999939868, 12.00000000000000000, 1.600000000000000089 ) ) ;
#940=ORIENTED_EDGE ( 'NONE', *, *, #5197, .F. ) ;
#944=ORIENTED_EDGE ( 'NONE', *, *, #11615, .T. ) ;
#948=ORIENTED_EDGE ( 'NONE', *, *, #11855, .F. ) ;
#951=CARTESIAN_POINT ( 'NONE',  ( 2.500000000000000000, 4.700000000000000178, 1.600000000000000089 ) ) ;
#952=DIRECTION ( 'NONE',  ( 1.060879779086260081E-14, -8.223874256482640091E-16, 1.000000000000000000 ) ) ;
#966=ORIENTED_EDGE ( 'NONE', *, *, #8760, .T. ) ;
#971=CARTESIAN_POINT ( 'NONE',  ( 1.899999999999999911, 11.15000000000000036, 1.600000000000000089 ) ) ;
#974=CARTESIAN_POINT ( 'NONE',  ( -1.000000000000000000, 5.400000000000000355, 7.700000000000000178 ) ) ;
#977=ORIENTED_EDGE ( 'NONE', *, *, #1593, .F. ) ;
#983=EDGE_CURVE ( 'NONE', #389, #13368, #12182, .T. ) ;
#984=ORIENTED_EDGE ( 'NONE', *, *, #10962, .F. ) ;
#995=FACE_OUTER_BOUND ( 'NONE', #6865, .T. ) ;
#997=CARTESIAN_POINT ( 'NONE',  ( -1.800000000000000044, 12.00000000000000000, 1.600000000000000089 ) ) ;
#1004=ADVANCED_FACE ( 'NONE', ( #8197 ), #12459, .T. ) ;
#1005=EDGE_CURVE ( 'NONE', #4096, #12326, #14856, .T. ) ;
#1006=FACE_OUTER_BOUND ( 'NONE', #2160, .T. ) ;
#1011=CARTESIAN_POINT ( 'NONE',  ( 2.500000000000000000, 8.500000000000000000, 0.6099999999999999867 ) ) ;
#1014=CARTESIAN_POINT ( 'NONE',  ( -1.889999999999999902, 8.500000000000000000, 2.702225438111990169E-15 ) ) ;
#1022=AXIS2_PLACEMENT_3D ( 'NONE', #2980, #8623, #3057 ) ;
#1023=FACE_OUTER_BOUND ( 'NONE', #9086, .T. ) ;
#1029=PLANE ( 'NONE',  #13544 ) ;
#1032=ORIENTED_EDGE ( 'NONE', *, *, #16095, .F. ) ;
#1040=CARTESIAN_POINT ( 'NONE',  ( -1.875000000000000000, 11.25000000000000000, 7.700000000000000178 ) ) ;
#1042=EDGE_CURVE ( 'NONE', #16733, #8528, #14114, .T. ) ;
#1049=EDGE_CURVE ( 'NONE', #18164, #8433, #17791, .T. ) ;
#1053=EDGE_LOOP ( 'NONE', ( #17004, #2069, #18120, #9573 ) ) ;
#1055=FACE_OUTER_BOUND ( 'NONE', #2756, .T. ) ;
#1060=CARTESIAN_POINT ( 'NONE',  ( 1.899999999999999911, 7.299999999999999822, 0.6099999999999999867 ) ) ;
#1064=CARTESIAN_POINT ( 'NONE',  ( -1.889999999999999902, 3.500000000000000000, 0.6099999999999999867 ) ) ;
#1069=FACE_OUTER_BOUND ( 'NONE', #13071, .T. ) ;
#1075=CARTESIAN_POINT ( 'NONE',  ( -1.850000000000000089, 0.7500000000000000000, 7.649999999999999467 ) ) ;
#1088=EDGE_CURVE ( 'NONE', #5474, #13417, #13693, .T. ) ;
#1091=VERTEX_POINT ( 'NONE', #15437 ) ;
#1099=EDGE_LOOP ( 'NONE', ( #16487, #3089, #589, #10486 ) ) ;
#1101=VECTOR ( 'NONE', #12796, 1000.000000000000000 ) ;
#1102=CARTESIAN_POINT ( 'NONE',  ( -0.5372984490435469551, 4.250000000000000000, 7.700000000000000178 ) ) ;
#1104=VECTOR ( 'NONE', #14771, 1000.000000000000000 ) ;
#1105=ADVANCED_FACE ( 'NONE', ( #1069 ), #9498, .F. ) ;
#1107=AXIS2_PLACEMENT_3D ( 'NONE', #16098, #3393, #13312 ) ;
#1112=EDGE_CURVE ( 'NONE', #2205, #3830, #18076, .T. ) ;
#1116=VECTOR ( 'NONE', #14485, 1000.000000000000000 ) ;
#1122=AXIS2_PLACEMENT_3D ( 'NONE', #9742, #8440, #15576 ) ;
#1128=ORIENTED_EDGE ( 'NONE', *, *, #11746, .F. ) ;
#1129=ORIENTED_EDGE ( 'NONE', *, *, #6937, .F. ) ;
#1130=AXIS2_PLACEMENT_3D ( 'NONE', #4959, #6256, #13588 ) ;
#1131=ORIENTED_EDGE ( 'NONE', *, *, #379, .F. ) ;
#1132=LINE ( 'NONE', #1040, #10906 ) ;
#1134=ADVANCED_FACE ( 'NONE', ( #1339 ), #56, .F. ) ;
#1149=CARTESIAN_POINT ( 'NONE',  ( -1.899999999999999911, 2.000000000000000000, 2.388061258337340122E-16 ) ) ;
#1155=ORIENTED_EDGE ( 'NONE', *, *, #1986, .T. ) ;
#1160=DIRECTION ( 'NONE',  ( -1.000000000000000000, 0.000000000000000000, 0.000000000000000000 ) ) ;
#1167=PLANE ( 'NONE',  #5570 ) ;
#1175=LINE ( 'NONE', #2754, #17388 ) ;
#1178=VERTEX_POINT ( 'NONE', #9583 ) ;
#1185=ORIENTED_EDGE ( 'NONE', *, *, #13562, .T. ) ;
#1190=CARTESIAN_POINT ( 'NONE',  ( 1.899999999999999911, 2.000000000000000000, 1.600000000000000089 ) ) ;
#1191=CARTESIAN_POINT ( 'NONE',  ( 2.500000000000000000, 0.4000000000000000222, 4.000000000000000000 ) ) ;
#1193=EDGE_LOOP ( 'NONE', ( #13437, #4135, #9475 ) ) ;
#1194=LINE ( 'NONE', #10731, #16399 ) ;
#1202=( NAMED_UNIT ( * ) SI_UNIT ( $, .STERADIAN. ) SOLID_ANGLE_UNIT ( ) );
#1207=DIRECTION ( 'NONE',  ( -1.216682766712499758E-16, 6.416248801027068947E-32, -1.000000000000000000 ) ) ;
#1209=CARTESIAN_POINT ( 'NONE',  ( 1.899999999999999911, 2.799999999999999822, 1.600000000000000089 ) ) ;
#1210=AXIS2_PLACEMENT_3D ( 'NONE', #1745, #15811, #1911 ) ;
#1214=EDGE_LOOP ( 'NONE', ( #9557, #9004, #14417, #13828 ) ) ;
#1215=ADVANCED_FACE ( 'NONE', ( #12637 ), #18262, .T. ) ;
#1216=EDGE_LOOP ( 'NONE', ( #18170, #9335, #81, #3535 ) ) ;
#1217=VECTOR ( 'NONE', #5462, 1000.000000000000000 ) ;
#1220=LINE ( 'NONE', #6866, #7945 ) ;
#1231=ADVANCED_FACE ( 'NONE', ( #13005 ), #4294, .T. ) ;
#1235=VERTEX_POINT ( 'NONE', #14301 ) ;
#1241=CARTESIAN_POINT ( 'NONE',  ( -1.899999999999999911, 7.299999999999999822, 1.600000000000000089 ) ) ;
#1245=ORIENTED_EDGE ( 'NONE', *, *, #7119, .T. ) ;
#1254=DIRECTION ( 'NONE',  ( 1.224646799147350002E-16, 1.000000000000000000, 1.059261469412979938E-31 ) ) ;
#1262=EDGE_LOOP ( 'NONE', ( #7154, #5175, #6966, #5110 ) ) ;
#1265=DIRECTION ( 'NONE',  ( 0.000000000000000000, 0.000000000000000000, -1.000000000000000000 ) ) ;
#1267=ORIENTED_EDGE ( 'NONE', *, *, #15981, .T. ) ;
#1271=EDGE_CURVE ( 'NONE', #17781, #8865, #17065, .T. ) ;
#1275=EDGE_LOOP ( 'NONE', ( #4293, #12382, #1615, #14286 ) ) ;
#1276=EDGE_CURVE ( 'NONE', #3896, #1735, #15705, .T. ) ;
#1284=ORIENTED_EDGE ( 'NONE', *, *, #16946, .F. ) ;
#1286=FACE_OUTER_BOUND ( 'NONE', #14909, .T. ) ;
#1288=ORIENTED_EDGE ( 'NONE', *, *, #2367, .T. ) ;
#1292=DIRECTION ( 'NONE',  ( -1.000000000000000000, 0.000000000000000000, 0.000000000000000000 ) ) ;
#1303=ADVANCED_FACE ( 'NONE', ( #327 ), #11605, .F. ) ;
#1307=DIRECTION ( 'NONE',  ( 0.000000000000000000, -1.000000000000000000, 1.850371707708589879E-16 ) ) ;
#1323=FACE_OUTER_BOUND ( 'NONE', #12895, .T. ) ;
#1332=EDGE_CURVE ( 'NONE', #2090, #7773, #3777, .T. ) ;
#1334=CARTESIAN_POINT ( 'NONE',  ( -1.889999999999999902, 7.299999999999999822, 0.5999999999999999778 ) ) ;
#1337=DIRECTION ( 'NONE',  ( 7.401486830834380223E-16, 1.000000000000000000, -1.110223024625159992E-16 ) ) ;
#1339=FACE_OUTER_BOUND ( 'NONE', #6141, .T. ) ;
#1340=CARTESIAN_POINT ( 'NONE',  ( 4.898587196589409994E-17, 0.1000000000000000056, 7.700000000000000178 ) ) ;
#1343=ORIENTED_EDGE ( 'NONE', *, *, #15845, .T. ) ;
#1346=ORIENTED_EDGE ( 'NONE', *, *, #6220, .T. ) ;
#1351=EDGE_LOOP ( 'NONE', ( #12487, #10039, #8460, #3936 ) ) ;
#1354=EDGE_CURVE ( 'NONE', #11698, #14775, #3873, .T. ) ;
#1372=VECTOR ( 'NONE', #16701, 1000.000000000000000 ) ;
#1375=FILL_AREA_STYLE_COLOUR ( '', #2318 ) ;
#1380=SPHERICAL_SURFACE ( 'NONE', #5204, 0.2000000000000000111 ) ;
#1383=CARTESIAN_POINT ( 'NONE',  ( -1.899999999999999911, 11.15000000000000036, 7.990820364436479856E-16 ) ) ;
#1384=CIRCLE ( 'NONE', #8783, 1.016666666666670160 ) ;
#1385=DIRECTION ( 'NONE',  ( 0.000000000000000000, -1.000000000000000000, 9.251858538542969116E-17 ) ) ;
#1391=ORIENTED_EDGE ( 'NONE', *, *, #8241, .T. ) ;
#1393=CIRCLE ( 'NONE', #11792, 0.5999999999999998668 ) ;
#1395=AXIS2_PLACEMENT_3D ( 'NONE', #3308, #1912, #6175 ) ;
#1404=CARTESIAN_POINT ( 'NONE',  ( 1.875000000000000000, 12.00000000000000000, 7.700000000000000178 ) ) ;
#1406=CARTESIAN_POINT ( 'NONE',  ( -1.599999999999869971, 12.00000000000000000, -2.399999999999999911 ) ) ;
#1414=ORIENTED_EDGE ( 'NONE', *, *, #13897, .T. ) ;
#1415=DIRECTION ( 'NONE',  ( 6.344131569286600069E-16, 1.000000000000000000, 1.586032892321649771E-16 ) ) ;
#1417=ORIENTED_EDGE ( 'NONE', *, *, #7444, .F. ) ;
#1418=AXIS2_PLACEMENT_3D ( 'NONE', #1340, #6991, #14219 ) ;
#1429=ORIENTED_EDGE ( 'NONE', *, *, #14388, .F. ) ;
#1432=VERTEX_POINT ( 'NONE', #1190 ) ;
#1438=CARTESIAN_POINT ( 'NONE',  ( 1.899999999999999911, 12.00000000000000000, 7.649999999999999467 ) ) ;
#1443=VECTOR ( 'NONE', #1668, 1000.000000000000000 ) ;
#1446=CARTESIAN_POINT ( 'NONE',  ( 2.200000000000000178, 1.071498764318550058E-16, 4.000000000000000000 ) ) ;
#1450=AXIS2_PLACEMENT_3D ( 'NONE', #13857, #4027, #12749 ) ;
#1452=ADVANCED_FACE ( 'NONE', ( #12397 ), #12483, .F. ) ;
#1453=DIRECTION ( 'NONE',  ( -2.960594732333750117E-16, -1.000000000000000000, 0.000000000000000000 ) ) ;
#1454=FACE_OUTER_BOUND ( 'NONE', #9654, .T. ) ;
#1458=VECTOR ( 'NONE', #7416, 1000.000000000000000 ) ;
#1464=EDGE_CURVE ( 'NONE', #15033, #3727, #7023, .T. ) ;
#1481=SURFACE_STYLE_USAGE ( .BOTH. , #6933 ) ;
#1497=DIRECTION ( 'NONE',  ( 0.000000000000000000, -1.000000000000000000, 0.000000000000000000 ) ) ;
#1501=VERTEX_POINT ( 'NONE', #2851 ) ;
#1510=VECTOR ( 'NONE', #17453, 1000.000000000000000 ) ;
#1514=EDGE_CURVE ( 'NONE', #6584, #8504, #14869, .T. ) ;
#1523=ORIENTED_EDGE ( 'NONE', *, *, #9000, .F. ) ;
#1531=ORIENTED_EDGE ( 'NONE', *, *, #1112, .T. ) ;
#1533=DIRECTION ( 'NONE',  ( -6.049014748177265474E-16, -2.081668171172166936E-15, -1.000000000000000000 ) ) ;
#1538=DIRECTION ( 'NONE',  ( -0.000000000000000000, 1.000000000000000000, 0.000000000000000000 ) ) ;
#1540=ORIENTED_EDGE ( 'NONE', *, *, #18205, .F. ) ;
#1545=PLANE ( 'NONE',  #16760 ) ;
#1554=ORIENTED_EDGE ( 'NONE', *, *, #15046, .T. ) ;
#1555=EDGE_CURVE ( 'NONE', #6821, #7200, #3033, .T. ) ;
#1556=CARTESIAN_POINT ( 'NONE',  ( 1.399999999999999911, 5.799999999999999822, 8.300000000000000711 ) ) ;
#1560=DIRECTION ( 'NONE',  ( 1.000000000000000000, 0.000000000000000000, 0.000000000000000000 ) ) ;
#1564=CARTESIAN_POINT ( 'NONE',  ( -1.889999999999999902, 3.500000000000000000, 0.5999999999999999778 ) ) ;
#1574=DIRECTION ( 'NONE',  ( -4.898587196589410857E-16, -1.000000000000000000, 2.696301922142130194E-31 ) ) ;
#1576=EDGE_CURVE ( 'NONE', #10192, #8619, #11922, .T. ) ;
#1577=FACE_OUTER_BOUND ( 'NONE', #10755, .T. ) ;
#1580=LINE ( 'NONE', #12786, #17918 ) ;
#1582=ORIENTED_EDGE ( 'NONE', *, *, #9764, .F. ) ;
#1585=DIRECTION ( 'NONE',  ( -5.921189464667500234E-16, 9.860761315262649757E-32, -1.000000000000000000 ) ) ;
#1586=VECTOR ( 'NONE', #9798, 1000.000000000000000 ) ;
#1593=EDGE_CURVE ( 'NONE', #11546, #16860, #17258, .T. ) ;
#1604=DIRECTION ( 'NONE',  ( 1.000000000000000000, 0.000000000000000000, -3.097720492815726673E-16 ) ) ;
#1608=AXIS2_PLACEMENT_3D ( 'NONE', #4439, #8701, #12962 ) ;
#1615=ORIENTED_EDGE ( 'NONE', *, *, #4010, .T. ) ;
#1620=DIRECTION ( 'NONE',  ( 0.000000000000000000, 1.000000000000000000, 1.332267629550190018E-15 ) ) ;
#1621=AXIS2_PLACEMENT_3D ( 'NONE', #12401, #10925, #15275 ) ;
#1623=ORIENTED_EDGE ( 'NONE', *, *, #5769, .T. ) ;
#1625=CARTESIAN_POINT ( 'NONE',  ( 1.983927814618709873E-15, 10.80000000000000071, 7.700000000000000178 ) ) ;
#1635=VECTOR ( 'NONE', #13186, 1000.000000000000000 ) ;
#1639=VERTEX_POINT ( 'NONE', #10502 ) ;
#1643=DIRECTION ( 'NONE',  ( -3.700743415417199972E-16, 1.000000000000000000, 3.581736239852560511E-31 ) ) ;
#1646=ORIENTED_EDGE ( 'NONE', *, *, #7536, .F. ) ;
#1650=VERTEX_POINT ( 'NONE', #264 ) ;
#1660=VECTOR ( 'NONE', #6566, 1000.000000000000000 ) ;
#1661=CARTESIAN_POINT ( 'NONE',  ( 1.850000000000000089, 11.25000000000000000, 7.700000000000000178 ) ) ;
#1662=CARTESIAN_POINT ( 'NONE',  ( -1.899999999999999911, 7.299999999999999822, 1.600000000000000089 ) ) ;
#1668=DIRECTION ( 'NONE',  ( -2.242874797222529735E-16, 0.000000000000000000, -1.000000000000000000 ) ) ;
#1673=EDGE_CURVE ( 'NONE', #14845, #9755, #3464, .T. ) ;
#1679=VECTOR ( 'NONE', #7092, 1000.000000000000000 ) ;
#1680=CARTESIAN_POINT ( 'NONE',  ( 2.616666666666669805, 1.110223024625159992E-16, 7.649999999999999467 ) ) ;
#1686=AXIS2_PLACEMENT_3D ( 'NONE', #2093, #6340, #17621 ) ;
#1689=ORIENTED_EDGE ( 'NONE', *, *, #1555, .F. ) ;
#1694=EDGE_CURVE ( 'NONE', #7811, #5515, #8860, .T. ) ;
#1696=VERTEX_POINT ( 'NONE', #11628 ) ;
#1700=EDGE_LOOP ( 'NONE', ( #16082, #7539, #16921, #5146, #2357, #9848 ) ) ;
#1701=CARTESIAN_POINT ( 'NONE',  ( -1.899999999999999911, -3.954861110236189622E-16, 3.278889744907200310 ) ) ;
#1702=AXIS2_PLACEMENT_3D ( 'NONE', #8992, #14640, #1954 ) ;
#1713=CARTESIAN_POINT ( 'NONE',  ( 2.500000000000000000, 4.700000000000000178, 0.6099999999999999867 ) ) ;
#1716=ORIENTED_EDGE ( 'NONE', *, *, #8682, .F. ) ;
#1717=AXIS2_PLACEMENT_3D ( 'NONE', #12010, #13305, #14785 ) ;
#1718=CARTESIAN_POINT ( 'NONE',  ( 2.500000000000000000, 4.700000000000000178, 1.600000000000000089 ) ) ;
#1720=EDGE_CURVE ( 'NONE', #13413, #7434, #16161, .T. ) ;
#1729=EDGE_CURVE ( 'NONE', #12906, #17929, #11720, .T. ) ;
#1730=FACE_OUTER_BOUND ( 'NONE', #9445, .T. ) ;
#1732=AXIS2_PLACEMENT_3D ( 'NONE', #4990, #13511, #6471 ) ;
#1734=DIRECTION ( 'NONE',  ( 1.073215590470990073E-14, 1.000000000000000000, 0.000000000000000000 ) ) ;
#1735=VERTEX_POINT ( 'NONE', #14508 ) ;
#1740=PLANE ( 'NONE',  #16577 ) ;
#1745=CARTESIAN_POINT ( 'NONE',  ( -1.899999999999999911, -2.607830583485239887E-17, -2.799999999999999822 ) ) ;
#1748=DIRECTION ( 'NONE',  ( 3.330669073875480271E-15, 1.000000000000000000, 3.700743415417199972E-16 ) ) ;
#1750=ORIENTED_EDGE ( 'NONE', *, *, #5753, .T. ) ;
#1757=AXIS2_PLACEMENT_3D ( 'NONE', #13488, #6446, #5062 ) ;
#1762=ORIENTED_EDGE ( 'NONE', *, *, #7277, .F. ) ;
#1764=LINE ( 'NONE', #7410, #15311 ) ;
#1769=LINE ( 'NONE', #15841, #1458 ) ;
#1772=DIRECTION ( 'NONE',  ( -6.083413833562510128E-16, 1.520853458390629997E-16, -1.000000000000000000 ) ) ;
#1773=DIRECTION ( 'NONE',  ( -1.000000000000000000, 0.000000000000000000, 0.000000000000000000 ) ) ;
#1780=EDGE_CURVE ( 'NONE', #11214, #475, #7552, .T. ) ;
#1782=EDGE_CURVE ( 'NONE', #14972, #12624, #14670, .T. ) ;
#1783=VECTOR ( 'NONE', #451, 1000.000000000000114 ) ;
#1790=ORIENTED_EDGE ( 'NONE', *, *, #16946, .T. ) ;
#1791=CARTESIAN_POINT ( 'NONE',  ( 2.500000000000000000, 0.8000000000000000444, -1.769429514865259726E-15 ) ) ;
#1799=VECTOR ( 'NONE', #6073, 1000.000000000000000 ) ;
#1801=VERTEX_POINT ( 'NONE', #697 ) ;
#1806=EDGE_CURVE ( 'NONE', #17781, #14972, #8098, .T. ) ;
#1813=VECTOR ( 'NONE', #4502, 1000.000000000000000 ) ;
#1818=ORIENTED_EDGE ( 'NONE', *, *, #1042, .T. ) ;
#1820=DIRECTION ( 'NONE',  ( 2.936127007273139866E-16, 0.000000000000000000, -1.000000000000000000 ) ) ;
#1826=DIRECTION ( 'NONE',  ( -2.775557561562890365E-16, -1.000000000000000000, -2.775557561562890365E-16 ) ) ;
#1834=DIRECTION ( 'NONE',  ( 1.000000000000000000, 0.000000000000000000, 0.000000000000000000 ) ) ;
#1843=EDGE_CURVE ( 'NONE', #12160, #16040, #15323, .T. ) ;
#1851=ORIENTED_EDGE ( 'NONE', *, *, #17367, .T. ) ;
#1853=CARTESIAN_POINT ( 'NONE',  ( -1.889999999999999902, 8.500000000000000000, 0.5999999999999999778 ) ) ;
#1854=ORIENTED_EDGE ( 'NONE', *, *, #13294, .F. ) ;
#1884=VERTEX_POINT ( 'NONE', #8079 ) ;
#1885=LINE ( 'NONE', #10053, #912 ) ;
#1890=EDGE_CURVE ( 'NONE', #3235, #13297, #10769, .T. ) ;
#1893=AXIS2_PLACEMENT_3D ( 'NONE', #5470, #12328, #11110 ) ;
#1897=DIRECTION ( 'NONE',  ( 0.000000000000000000, 0.000000000000000000, 1.000000000000000000 ) ) ;
#1900=PLANE ( 'NONE',  #6780 ) ;
#1902=DIRECTION ( 'NONE',  ( 0.000000000000000000, 1.000000000000000000, 0.000000000000000000 ) ) ;
#1904=ORIENTED_EDGE ( 'NONE', *, *, #7833, .F. ) ;
#1907=DIRECTION ( 'NONE',  ( 0.000000000000000000, 0.000000000000000000, 1.000000000000000000 ) ) ;
#1909=ORIENTED_EDGE ( 'NONE', *, *, #16850, .F. ) ;
#1911=DIRECTION ( 'NONE',  ( -1.000000000000000000, 2.220446049250309876E-16, 0.000000000000000000 ) ) ;
#1912=DIRECTION ( 'NONE',  ( 1.000000000000000000, -2.220446049250309876E-16, -6.049014748177260544E-16 ) ) ;
#1913=EDGE_CURVE ( 'NONE', #14807, #14318, #16857, .T. ) ;
#1917=DIRECTION ( 'NONE',  ( -0.2800000000000002487, 6.217248937900899405E-17, -0.9599999999999998535 ) ) ;
#1926=ORIENTED_EDGE ( 'NONE', *, *, #13562, .F. ) ;
#1928=ORIENTED_EDGE ( 'NONE', *, *, #5971, .F. ) ;
#1930=FACE_OUTER_BOUND ( 'NONE', #1053, .T. ) ;
#1931=CIRCLE ( 'NONE', #9015, 1.100000000000000311 ) ;
#1942=DIRECTION ( 'NONE',  ( 0.000000000000000000, -1.000000000000000000, 0.000000000000000000 ) ) ;
#1947=VERTEX_POINT ( 'NONE', #12700 ) ;
#1949=ORIENTED_EDGE ( 'NONE', *, *, #9373, .T. ) ;
#1952=CIRCLE ( 'NONE', #8477, 0.6099999999999999867 ) ;
#1953=DIRECTION ( 'NONE',  ( -1.000000000000000000, 1.850371707708599740E-16, 0.000000000000000000 ) ) ;
#1954=DIRECTION ( 'NONE',  ( 0.7049180327868849183, -1.565232460946939801E-16, -0.7092887755011130224 ) ) ;
#1955=ORIENTED_EDGE ( 'NONE', *, *, #10600, .T. ) ;
#1958=VECTOR ( 'NONE', #11386, 1000.000000000000000 ) ;
#1961=AXIS2_PLACEMENT_3D ( 'NONE', #14860, #2175, #9665 ) ;
#1968=LINE ( 'NONE', #7630, #2418 ) ;
#1971=ORIENTED_EDGE ( 'NONE', *, *, #8472, .T. ) ;
#1986=EDGE_CURVE ( 'NONE', #3622, #12817, #17842, .T. ) ;
#1989=CARTESIAN_POINT ( 'NONE',  ( 2.500000000000000000, 0.7500000000000000000, 7.649999999999999467 ) ) ;
#1994=VECTOR ( 'NONE', #15620, 1000.000000000000000 ) ;
#1995=VERTEX_POINT ( 'NONE', #4344 ) ;
#1999=VERTEX_POINT ( 'NONE', #14265 ) ;
#2000=VECTOR ( 'NONE', #10514, 1000.000000000000000 ) ;
#2010=ADVANCED_FACE ( 'NONE', ( #10010 ), #15672, .T. ) ;
#2014=VECTOR ( 'NONE', #16436, 1000.000000000000000 ) ;
#2016=AXIS2_PLACEMENT_3D ( 'NONE', #11658, #8703, #8625 ) ;
#2017=CARTESIAN_POINT ( 'NONE',  ( -1.850000000000000089, 11.25000000000000000, 7.700000000000000178 ) ) ;
#2019=DIRECTION ( 'NONE',  ( 1.000000000000000000, 0.000000000000000000, -6.123233995736759873E-17 ) ) ;
#2020=ORIENTED_EDGE ( 'NONE', *, *, #2963, .T. ) ;
#2022=DIRECTION ( 'NONE',  ( 1.000000000000000000, 4.157615153618229646E-15, 0.000000000000000000 ) ) ;
#2023=ORIENTED_EDGE ( 'NONE', *, *, #983, .F. ) ;
#2024=ADVANCED_FACE ( 'NONE', ( #10099 ), #17114, .F. ) ;
#2037=DIRECTION ( 'NONE',  ( 2.220446049250309876E-16, 1.000000000000000000, 3.286920438420880041E-31 ) ) ;
#2038=ORIENTED_EDGE ( 'NONE', *, *, #4986, .T. ) ;
#2039=CARTESIAN_POINT ( 'NONE',  ( -1.599999999999880185, 11.40000000000000036, 1.600000000000000089 ) ) ;
#2042=VERTEX_POINT ( 'NONE', #6010 ) ;
#2045=CARTESIAN_POINT ( 'NONE',  ( -1.875000000000000000, 2.220446049250309876E-16, 7.700000000000000178 ) ) ;
#2046=ORIENTED_EDGE ( 'NONE', *, *, #4384, .T. ) ;
#2049=ADVANCED_FACE ( 'NONE', ( #633 ), #14529, .F. ) ;
#2050=DIRECTION ( 'NONE',  ( -1.643460219210440021E-31, -1.000000000000000000, -2.220446049250309876E-16 ) ) ;
#2053=DIRECTION ( 'NONE',  ( 3.515706244646330359E-15, -1.000000000000000000, -1.110223024625510049E-16 ) ) ;
#2060=ORIENTED_EDGE ( 'NONE', *, *, #5000, .F. ) ;
#2062=ORIENTED_EDGE ( 'NONE', *, *, #17684, .T. ) ;
#2066=VECTOR ( 'NONE', #6144, 1000.000000000000000 ) ;
#2069=ORIENTED_EDGE ( 'NONE', *, *, #18205, .T. ) ;
#2071=FACE_OUTER_BOUND ( 'NONE', #22, .T. ) ;
#2072=DIRECTION ( 'NONE',  ( -3.700743415417180054E-15, -1.000000000000000000, -2.220446049250169853E-16 ) ) ;
#2076=CARTESIAN_POINT ( 'NONE',  ( -0.03000000000000000236, 11.40000000000000036, -2.869354249208270301E-17 ) ) ;
#2078=EDGE_LOOP ( 'NONE', ( #605, #9911, #10015, #10387 ) ) ;
#2085=CARTESIAN_POINT ( 'NONE',  ( -2.500000000000000000, 0.4000000000000000222, 4.000000000000000000 ) ) ;
#2090=VERTEX_POINT ( 'NONE', #4605 ) ;
#2091=DIRECTION ( 'NONE',  ( -1.000000000000000000, 0.000000000000000000, 7.401486830834380223E-16 ) ) ;
#2093=CARTESIAN_POINT ( 'NONE',  ( 2.500000000000000000, 0.4000000000000000222, -2.399999999999999911 ) ) ;
#2100=FACE_OUTER_BOUND ( 'NONE', #401, .T. ) ;
#2104=LINE ( 'NONE', #12118, #6711 ) ;
#2105=CARTESIAN_POINT ( 'NONE',  ( 2.500000000000000000, 9.199999999999999289, 0.6099999999999999867 ) ) ;
#2109=DIRECTION ( 'NONE',  ( 2.537652627714639929E-16, 1.000000000000000000, 0.000000000000000000 ) ) ;
#2110=CARTESIAN_POINT ( 'NONE',  ( 1.889999999999999902, 4.100000000000000533, -6.512531667206379696E-16 ) ) ;
#2122=EDGE_CURVE ( 'NONE', #8619, #10260, #15928, .T. ) ;
#2137=CARTESIAN_POINT ( 'NONE',  ( 1.889999999999999902, 4.700000000000000178, 0.5999999999999999778 ) ) ;
#2138=ORIENTED_EDGE ( 'NONE', *, *, #3915, .F. ) ;
#2140=CARTESIAN_POINT ( 'NONE',  ( -2.200000000000000178, 4.053507564265650114E-17, 4.000000000000000000 ) ) ;
#2144=ORIENTED_EDGE ( 'NONE', *, *, #15938, .F. ) ;
#2148=DIRECTION ( 'NONE',  ( 0.000000000000000000, 1.000000000000000000, 9.251858538542969116E-17 ) ) ;
#2153=VERTEX_POINT ( 'NONE', #9529 ) ;
#2160=EDGE_LOOP ( 'NONE', ( #17142, #2876, #13343, #1531 ) ) ;
#2163=ORIENTED_EDGE ( 'NONE', *, *, #17084, .T. ) ;
#2170=ADVANCED_FACE ( 'NONE', ( #15104 ), #15188, .F. ) ;
#2175=DIRECTION ( 'NONE',  ( 1.216682766712499758E-16, 4.229421046191059358E-17, 1.000000000000000000 ) ) ;
#2177=DIRECTION ( 'NONE',  ( 0.000000000000000000, 0.000000000000000000, 1.000000000000000000 ) ) ;
#2178=FACE_OUTER_BOUND ( 'NONE', #7883, .T. ) ;
#2187=CARTESIAN_POINT ( 'NONE',  ( -1.800000000000000044, 11.29999999999999893, 1.600000000000000089 ) ) ;
#2189=EDGE_LOOP ( 'NONE', ( #14221, #6931, #13516, #6227 ) ) ;
#2190=ORIENTED_EDGE ( 'NONE', *, *, #1514, .T. ) ;
#2199=CARTESIAN_POINT ( 'NONE',  ( 1.600000000000000089, 2.886579864025409569E-16, 7.649999999999999467 ) ) ;
#2200=CARTESIAN_POINT ( 'NONE',  ( 1.983927814618709873E-15, 10.80000000000000071, 7.700000000000000178 ) ) ;
#2205=VERTEX_POINT ( 'NONE', #3681 ) ;
#2212=VERTEX_POINT ( 'NONE', #1014 ) ;
#2220=CARTESIAN_POINT ( 'NONE',  ( 0.2000000000000000111, -2.449293598294700066E-17, 8.300000000000000711 ) ) ;
#2225=EDGE_CURVE ( 'NONE', #7642, #8282, #17855, .T. ) ;
#2234=ORIENTED_EDGE ( 'NONE', *, *, #11796, .F. ) ;
#2237=EDGE_CURVE ( 'NONE', #14325, #16249, #1194, .T. ) ;
#2251=AXIS2_PLACEMENT_3D ( 'NONE', #5672, #18130, #15408 ) ;
#2252=VERTEX_POINT ( 'NONE', #16491 ) ;
#2255=VECTOR ( 'NONE', #13462, 1000.000000000000000 ) ;
#2259=ORIENTED_EDGE ( 'NONE', *, *, #1593, .T. ) ;
#2263=CYLINDRICAL_SURFACE ( 'NONE', #5213, 0.8000000000000000444 ) ;
#2267=FACE_OUTER_BOUND ( 'NONE', #1262, .T. ) ;
#2268=AXIS2_PLACEMENT_3D ( 'NONE', #15091, #9318, #7755 ) ;
#2275=EDGE_CURVE ( 'NONE', #3339, #6533, #16588, .T. ) ;
#2279=CARTESIAN_POINT ( 'NONE',  ( -0.2000000000000000111, 0.1000000000000000056, 8.300000000000000711 ) ) ;
#2282=CARTESIAN_POINT ( 'NONE',  ( 2.616666666666660035, -5.805074450128190455E-17, 4.000000000000000000 ) ) ;
#2286=CARTESIAN_POINT ( 'NONE',  ( -1.889999999999999902, 3.500000000000000000, 0.5999999999999999778 ) ) ;
#2290=AXIS2_PLACEMENT_3D ( 'NONE', #486, #17106, #9813 ) ;
#2294=CARTESIAN_POINT ( 'NONE',  ( 1.850000000000000089, 0.7500000000000000000, 7.700000000000000178 ) ) ;
#2295=DIRECTION ( 'NONE',  ( 1.000000000000000000, 0.000000000000000000, 0.000000000000000000 ) ) ;
#2296=LINE ( 'NONE', #4869, #4656 ) ;
#2299=CIRCLE ( 'NONE', #3766, 0.5999999999999998668 ) ;
#2306=VECTOR ( 'NONE', #2373, 1000.000000000000000 ) ;
#2318=COLOUR_RGB ( '', 0.09019608, 0.27058824, 0.51372549) ;
#2323=CARTESIAN_POINT ( 'NONE',  ( 1.889999999999999902, 7.299999999999999822, 0.6099999999999999867 ) ) ;
#2326=CARTESIAN_POINT ( 'NONE',  ( -1.850000000000000089, 11.25000000000000000, 7.649999999999999467 ) ) ;
#2339=EDGE_LOOP ( 'NONE', ( #13552, #7058, #6337, #8230 ) ) ;
#2343=AXIS2_PLACEMENT_3D ( 'NONE', #9293, #7922, #5134 ) ;
#2353=EDGE_LOOP ( 'NONE', ( #7227, #106, #15475, #17569 ) ) ;
#2357=ORIENTED_EDGE ( 'NONE', *, *, #17305, .T. ) ;
#2362=ORIENTED_EDGE ( 'NONE', *, *, #1843, .T. ) ;
#2367=EDGE_CURVE ( 'NONE', #6950, #8261, #14827, .T. ) ;
#2370=DIRECTION ( 'NONE',  ( 0.000000000000000000, -1.000000000000000000, 0.000000000000000000 ) ) ;
#2373=DIRECTION ( 'NONE',  ( 0.000000000000000000, 1.000000000000000000, -1.586032892321649771E-16 ) ) ;
#2374=CARTESIAN_POINT ( 'NONE',  ( 1.800000000000000044, 11.40000000000000036, 7.649999999999999467 ) ) ;
#2390=VERTEX_POINT ( 'NONE', #14921 ) ;
#2399=ADVANCED_FACE ( 'NONE', ( #12327 ), #17853, .F. ) ;
#2415=VERTEX_POINT ( 'NONE', #7878 ) ;
#2418=VECTOR ( 'NONE', #594, 1000.000000000000000 ) ;
#2419=FACE_OUTER_BOUND ( 'NONE', #5055, .T. ) ;
#2430=DIRECTION ( 'NONE',  ( -2.775557561562890365E-16, -1.000000000000000000, -2.775557561562890365E-16 ) ) ;
#2444=VECTOR ( 'NONE', #2629, 1000.000000000000000 ) ;
#2446=ORIENTED_EDGE ( 'NONE', *, *, #17628, .T. ) ;
#2450=CARTESIAN_POINT ( 'NONE',  ( -0.2000000000000000111, 2.449293598294710235E-17, 8.300000000000000711 ) ) ;
#2455=VERTEX_POINT ( 'NONE', #10943 ) ;
#2457=VECTOR ( 'NONE', #17273, 1000.000000000000000 ) ;
#2465=CARTESIAN_POINT ( 'NONE',  ( 2.241103642439659443E-15, 9.099999999999999645, 7.700000000000000178 ) ) ;
#2471=DIRECTION ( 'NONE',  ( 1.853875224168160112E-15, 1.000000000000000000, 2.960594732333760372E-15 ) ) ;
#2474=EDGE_CURVE ( 'NONE', #7262, #6008, #18211, .T. ) ;
#2476=ADVANCED_FACE ( 'NONE', ( #5662 ), #16757, .F. ) ;
#2477=CARTESIAN_POINT ( 'NONE',  ( -1.899999999999999911, 4.700000000000000178, 0.6099999999999999867 ) ) ;
#2493=LINE ( 'NONE', #1011, #11245 ) ;
#2495=ORIENTED_EDGE ( 'NONE', *, *, #5541, .T. ) ;
#2507=CARTESIAN_POINT ( 'NONE',  ( 1.889999999999999902, 7.900000000000000355, 2.872493252184739990E-16 ) ) ;
#2518=ORIENTED_EDGE ( 'NONE', *, *, #16251, .F. ) ;
#2528=ORIENTED_EDGE ( 'NONE', *, *, #1332, .T. ) ;
#2530=ORIENTED_EDGE ( 'NONE', *, *, #2237, .F. ) ;
#2543=ORIENTED_EDGE ( 'NONE', *, *, #6066, .F. ) ;
#2545=DIRECTION ( 'NONE',  ( -1.000000000000000000, 0.000000000000000000, 0.000000000000000000 ) ) ;
#2554=ORIENTED_EDGE ( 'NONE', *, *, #12443, .T. ) ;
#2565=EDGE_CURVE ( 'NONE', #12747, #14464, #14696, .T. ) ;
#2566=DIRECTION ( 'NONE',  ( 1.000000000000000000, 9.280995951607650285E-16, 0.000000000000000000 ) ) ;
#2570=VECTOR ( 'NONE', #3019, 1000.000000000000000 ) ;
#2571=EDGE_CURVE ( 'NONE', #1999, #14325, #12931, .T. ) ;
#2594=EDGE_CURVE ( 'NONE', #4272, #3830, #226, .T. ) ;
#2600=CARTESIAN_POINT ( 'NONE',  ( -1.600000000000000089, -9.269168731236219867E-17, 4.000000000000000000 ) ) ;
#2604=DIRECTION ( 'NONE',  ( 1.000000000000000000, -2.220446049250309876E-16, -6.123233995736759873E-17 ) ) ;
#2617=CARTESIAN_POINT ( 'NONE',  ( 2.500000000000000000, 0.4000000000000000222, 4.000000000000000000 ) ) ;
#2619=VECTOR ( 'NONE', #2883, 1000.000000000000000 ) ;
#2621=VECTOR ( 'NONE', #11865, 1000.000000000000000 ) ;
#2622=EDGE_CURVE ( 'NONE', #4099, #13297, #5073, .T. ) ;
#2626=LINE ( 'NONE', #12612, #812 ) ;
#2627=VERTEX_POINT ( 'NONE', #14800 ) ;
#2629=DIRECTION ( 'NONE',  ( 3.416070845000479880E-16, 1.000000000000000000, 8.540177112501199701E-17 ) ) ;
#2637=ORIENTED_EDGE ( 'NONE', *, *, #5115, .T. ) ;
#2642=EDGE_CURVE ( 'NONE', #1947, #9534, #10247, .T. ) ;
#2644=DIRECTION ( 'NONE',  ( 0.000000000000000000, 3.581736239852560511E-31, -1.000000000000000000 ) ) ;
#2649=CARTESIAN_POINT ( 'NONE',  ( 0.000000000000000000, 4.930380657631319405E-32, 8.300000000000000711 ) ) ;
#2650=DIRECTION ( 'NONE',  ( -1.000000000000000000, 4.956352788505162676E-15, 0.000000000000000000 ) ) ;
#2658=VECTOR ( 'NONE', #7781, 1000.000000000000000 ) ;
#2659=ORIENTED_EDGE ( 'NONE', *, *, #1729, .F. ) ;
#2662=CARTESIAN_POINT ( 'NONE',  ( -1.875000000000000000, 0.7500000000000000000, 7.700000000000000178 ) ) ;
#2668=CARTESIAN_POINT ( 'NONE',  ( 1.399999999999999911, 6.400000000000000355, 8.300000000000000711 ) ) ;
#2673=CARTESIAN_POINT ( 'NONE',  ( 2.241103642439659443E-15, 9.099999999999999645, 8.300000000000000711 ) ) ;
#2675=ORIENTED_EDGE ( 'NONE', *, *, #4647, .F. ) ;
#2680=DIRECTION ( 'NONE',  ( 1.445602896647339508E-15, -1.000000000000000000, -1.264902534566422168E-15 ) ) ;
#2683=VECTOR ( 'NONE', #242, 1000.000000000000000 ) ;
#2686=CARTESIAN_POINT ( 'NONE',  ( 4.898587196589409994E-17, 0.1000000000000000056, 8.300000000000000711 ) ) ;
#2691=AXIS2_PLACEMENT_3D ( 'NONE', #7535, #17431, #4750 ) ;
#2698=ORIENTED_EDGE ( 'NONE', *, *, #252, .F. ) ;
#2700=EDGE_CURVE ( 'NONE', #9144, #7297, #5833, .T. ) ;
#2702=EDGE_CURVE ( 'NONE', #17179, #8282, #7612, .T. ) ;
#2707=ADVANCED_FACE ( 'NONE', ( #6498 ), #15128, .T. ) ;
#2710=LINE ( 'NONE', #8269, #3457 ) ;
#2711=LINE ( 'NONE', #7159, #12638 ) ;
#2733=ORIENTED_EDGE ( 'NONE', *, *, #10055, .T. ) ;
#2736=EDGE_LOOP ( 'NONE', ( #9267, #10945, #16466 ) ) ;
#2738=LINE ( 'NONE', #8566, #7038 ) ;
#2739=DIRECTION ( 'NONE',  ( 1.000000000000000000, -8.673617379884035472E-15, 0.000000000000000000 ) ) ;
#2744=DIRECTION ( 'NONE',  ( 0.000000000000000000, 0.000000000000000000, 1.000000000000000000 ) ) ;
#2746=EDGE_CURVE ( 'NONE', #12789, #3214, #17775, .T. ) ;
#2748=CARTESIAN_POINT ( 'NONE',  ( 0.3367924244280819934, 2.254758922476410188, 8.300000000000000711 ) ) ;
#2750=EDGE_LOOP ( 'NONE', ( #16890, #17506, #9063, #3086 ) ) ;
#2752=AXIS2_PLACEMENT_3D ( 'NONE', #6090, #16341, #3318 ) ;
#2754=CARTESIAN_POINT ( 'NONE',  ( -1.399999999999999911, 6.400000000000000355, 7.700000000000000178 ) ) ;
#2756=EDGE_LOOP ( 'NONE', ( #16576, #2138, #5022, #5992 ) ) ;
#2761=DIRECTION ( 'NONE',  ( -1.110223024625159992E-16, 0.000000000000000000, 1.000000000000000000 ) ) ;
#2762=VERTEX_POINT ( 'NONE', #15309 ) ;
#2763=CARTESIAN_POINT ( 'NONE',  ( 1.290000000000029790, 4.099999999999997868, 3.000000000000006661 ) ) ;
#2767=LINE ( 'NONE', #7130, #16859 ) ;
#2769=ORIENTED_EDGE ( 'NONE', *, *, #3915, .T. ) ;
#2770=ORIENTED_EDGE ( 'NONE', *, *, #3686, .F. ) ;
#2773=ORIENTED_EDGE ( 'NONE', *, *, #659, .T. ) ;
#2781=VECTOR ( 'NONE', #7671, 1000.000000000000000 ) ;
#2787=VERTEX_POINT ( 'NONE', #16317 ) ;
#2791=CARTESIAN_POINT ( 'NONE',  ( -2.500000000000000000, 2.799999999999999822, 1.600000000000000089 ) ) ;
#2798=CARTESIAN_POINT ( 'NONE',  ( 2.500000000000000000, 2.000000000000000000, -1.695950706916410117E-15 ) ) ;
#2803=EDGE_CURVE ( 'NONE', #8504, #2212, #1393, .T. ) ;
#2808=ADVANCED_FACE ( 'NONE', ( #10672 ), #3621, .F. ) ;
#2809=CARTESIAN_POINT ( 'NONE',  ( 1.899999999999999911, 0.7211102550927980248, 4.000000000000000000 ) ) ;
#2813=ORIENTED_EDGE ( 'NONE', *, *, #3828, .F. ) ;
#2827=EDGE_CURVE ( 'NONE', #1696, #1947, #14158, .T. ) ;
#2829=DIRECTION ( 'NONE',  ( -1.000000000000000000, 2.891205793294678228E-15, 3.614007241618347587E-15 ) ) ;
#2831=DIRECTION ( 'NONE',  ( -3.042833474898580443E-15, 3.289549702593060178E-16, 1.000000000000000000 ) ) ;
#2840=CARTESIAN_POINT ( 'NONE',  ( 1.983927814618709085E-15, 11.43245553203367493, 7.700000000000000178 ) ) ;
#2845=EDGE_CURVE ( 'NONE', #4577, #12789, #10567, .T. ) ;
#2851=CARTESIAN_POINT ( 'NONE',  ( -1.000000000000000000, 6.799999999999999822, 7.700000000000000178 ) ) ;
#2852=LINE ( 'NONE', #16731, #7401 ) ;
#2855=ORIENTED_EDGE ( 'NONE', *, *, #15995, .F. ) ;
#2856=DIRECTION ( 'NONE',  ( 2.960594732333750117E-15, 0.000000000000000000, -1.000000000000000000 ) ) ;
#2857=CARTESIAN_POINT ( 'NONE',  ( 1.000000000000000000, 6.799999999999999822, 8.300000000000000711 ) ) ;
#2871=VECTOR ( 'NONE', #14711, 1000.000000000000000 ) ;
#2874=FACE_OUTER_BOUND ( 'NONE', #13634, .T. ) ;
#2875=AXIS2_PLACEMENT_3D ( 'NONE', #9779, #15529, #16633 ) ;
#2876=ORIENTED_EDGE ( 'NONE', *, *, #16604, .F. ) ;
#2877=LINE ( 'NONE', #5468, #7668 ) ;
#2880=ORIENTED_EDGE ( 'NONE', *, *, #17162, .F. ) ;
#2881=DIRECTION ( 'NONE',  ( 1.000000000000000000, 0.000000000000000000, 0.000000000000000000 ) ) ;
#2882=AXIS2_PLACEMENT_3D ( 'NONE', #10471, #7525, #9646 ) ;
#2883=DIRECTION ( 'NONE',  ( -1.000000000000000000, 0.000000000000000000, 0.000000000000000000 ) ) ;
#2884=VECTOR ( 'NONE', #17075, 1000.000000000000000 ) ;
#2885=ORIENTED_EDGE ( 'NONE', *, *, #8331, .F. ) ;
#2888=AXIS2_PLACEMENT_3D ( 'NONE', #1438, #11148, #5503 ) ;
#2890=CIRCLE ( 'NONE', #7590, 0.6324555320336745501 ) ;
#2892=ADVANCED_FACE ( 'NONE', ( #14563 ), #11798, .T. ) ;
#2893=CARTESIAN_POINT ( 'NONE',  ( -2.500000000000000000, 4.700000000000000178, 0.6099999999999999867 ) ) ;
#2894=DIRECTION ( 'NONE',  ( 0.000000000000000000, 1.332267629550190018E-15, -1.000000000000000000 ) ) ;
#2903=ADVANCED_FACE ( 'NONE', ( #12162 ), #10765, .F. ) ;
#2906=AXIS2_PLACEMENT_3D ( 'NONE', #12827, #2744, #12460 ) ;
#2909=ORIENTED_EDGE ( 'NONE', *, *, #6580, .T. ) ;
#2910=ORIENTED_EDGE ( 'NONE', *, *, #3519, .T. ) ;
#2913=MECHANICAL_DESIGN_GEOMETRIC_PRESENTATION_REPRESENTATION('',(#4377),#14138);
#2915=CIRCLE ( 'NONE', #11775, 0.4000000000000001887 ) ;
#2921=VECTOR ( 'NONE', #7699, 1000.000000000000000 ) ;
#2923=CARTESIAN_POINT ( 'NONE',  ( 2.616666666666660035, -5.805074450128190455E-17, 4.000000000000000000 ) ) ;
#2929=CARTESIAN_POINT ( 'NONE',  ( -1.899999999999999911, 10.00000000000000000, 1.600000000000000089 ) ) ;
#2934=VECTOR ( 'NONE', #2961, 1000.000000000000000 ) ;
#2938=DIRECTION ( 'NONE',  ( 0.000000000000000000, 0.000000000000000000, 1.000000000000000000 ) ) ;
#2944=EDGE_CURVE ( 'NONE', #1801, #14551, #5112, .T. ) ;
#2947=LINE ( 'NONE', #15641, #10254 ) ;
#2954=DIRECTION ( 'NONE',  ( -3.652293603810800245E-15, -1.332267629550183904E-15, 1.000000000000000000 ) ) ;
#2955=LINE ( 'NONE', #8229, #14494 ) ;
#2961=DIRECTION ( 'NONE',  ( -1.000000000000000000, -7.401486830834380223E-16, 6.123233995736769734E-17 ) ) ;
#2963=EDGE_CURVE ( 'NONE', #4577, #9295, #6684, .T. ) ;
#2980=CARTESIAN_POINT ( 'NONE',  ( 2.500000000000000000, 11.29999999999999893, 7.649999999999999467 ) ) ;
#2981=ORIENTED_EDGE ( 'NONE', *, *, #6014, .F. ) ;
#2984=ORIENTED_EDGE ( 'NONE', *, *, #8247, .F. ) ;
#2988=FACE_OUTER_BOUND ( 'NONE', #6624, .T. ) ;
#3004=AXIS2_PLACEMENT_3D ( 'NONE', #9172, #6218, #855 ) ;
#3008=EDGE_CURVE ( 'NONE', #6669, #15169, #3624, .T. ) ;
#3014=CARTESIAN_POINT ( 'NONE',  ( 11.62823001646930088, 2.140775818696779709E-14, 0.5999999999998879563 ) ) ;
#3016=DIRECTION ( 'NONE',  ( -1.000000000000000000, 1.850371707708589879E-16, 0.000000000000000000 ) ) ;
#3019=DIRECTION ( 'NONE',  ( 1.000000000000000000, 0.000000000000000000, 0.000000000000000000 ) ) ;
#3020=EDGE_LOOP ( 'NONE', ( #940, #12994, #1646, #1971 ) ) ;
#3022=CARTESIAN_POINT ( 'NONE',  ( -1.000000000000000000, 6.400000000000000355, 7.700000000000000178 ) ) ;
#3027=ADVANCED_FACE ( 'NONE', ( #9274 ), #8089, .T. ) ;
#3033=LINE ( 'NONE', #4047, #1586 ) ;
#3035=DIRECTION ( 'NONE',  ( 1.643460219210440021E-31, 1.000000000000000000, 2.220446049250309876E-16 ) ) ;
#3041=LINE ( 'NONE', #3118, #17614 ) ;
#3044=AXIS2_PLACEMENT_3D ( 'NONE', #13463, #16150, #7817 ) ;
#3054=CARTESIAN_POINT ( 'NONE',  ( -1.889999999999999902, 8.500000000000000000, 0.6099999999999999867 ) ) ;
#3057=DIRECTION ( 'NONE',  ( 1.000000000000000000, 0.000000000000000000, -1.480297366166879989E-15 ) ) ;
#3058=ORIENTED_EDGE ( 'NONE', *, *, #9452, .F. ) ;
#3060=FACE_OUTER_BOUND ( 'NONE', #13252, .T. ) ;
#3061=ORIENTED_EDGE ( 'NONE', *, *, #2827, .T. ) ;
#3064=LINE ( 'NONE', #13148, #17633 ) ;
#3075=CARTESIAN_POINT ( 'NONE',  ( 0.3367924244280819934, 2.254758922476410188, 7.700000000000000178 ) ) ;
#3076=VERTEX_POINT ( 'NONE', #6501 ) ;
#3086=ORIENTED_EDGE ( 'NONE', *, *, #16604, .T. ) ;
#3087=CARTESIAN_POINT ( 'NONE',  ( 2.500000000000000000, 11.15000000000000036, -1.135674796306499891E-15 ) ) ;
#3089=ORIENTED_EDGE ( 'NONE', *, *, #8247, .T. ) ;
#3094=EDGE_CURVE ( 'NONE', #12326, #1091, #15895, .T. ) ;
#3096=CARTESIAN_POINT ( 'NONE',  ( 1.850000000000000089, 0.7500000000000000000, 8.300000000000000711 ) ) ;
#3103=CARTESIAN_POINT ( 'NONE',  ( -1.000000000000000000, 6.400000000000000355, 8.300000000000000711 ) ) ;
#3105=DIRECTION ( 'NONE',  ( 1.000000000000000000, 0.000000000000000000, 0.000000000000000000 ) ) ;
#3107=CARTESIAN_POINT ( 'NONE',  ( 0.2000000000000000111, 0.1000000000000000056, 8.300000000000000711 ) ) ;
#3117=CARTESIAN_POINT ( 'NONE',  ( 1.889999999999999902, 7.900000000000000355, 2.872493252184739990E-16 ) ) ;
#3118=CARTESIAN_POINT ( 'NONE',  ( 1.800000000000000044, 11.40000000000000036, 1.600000000000000089 ) ) ;
#3132=CARTESIAN_POINT ( 'NONE',  ( -2.500000000000000000, 11.29999999999999893, 1.600000000000000089 ) ) ;
#3133=EDGE_LOOP ( 'NONE', ( #14486, #8062, #7965 ) ) ;
#3135=ORIENTED_EDGE ( 'NONE', *, *, #9697, .T. ) ;
#3136=CARTESIAN_POINT ( 'NONE',  ( 11.62823001646920140, 2.147437156844530270E-14, -1.123545700920659934E-13 ) ) ;
#3137=EDGE_CURVE ( 'NONE', #410, #4501, #17126, .T. ) ;
#3138=ORIENTED_EDGE ( 'NONE', *, *, #11966, .F. ) ;
#3149=CARTESIAN_POINT ( 'NONE',  ( -1.289999999999999813, 4.099999999999999645, 3.000000000000001776 ) ) ;
#3157=CARTESIAN_POINT ( 'NONE',  ( -2.500000000000000000, 3.996802888650570054E-16, 9.955530934770520091 ) ) ;
#3163=ORIENTED_EDGE ( 'NONE', *, *, #10051, .F. ) ;
#3165=VECTOR ( 'NONE', #5158, 1000.000000000000000 ) ;
#3172=EDGE_CURVE ( 'NONE', #8719, #2042, #11318, .T. ) ;
#3173=ORIENTED_EDGE ( 'NONE', *, *, #17275, .T. ) ;
#3174=FACE_OUTER_BOUND ( 'NONE', #3259, .T. ) ;
#3178=ORIENTED_EDGE ( 'NONE', *, *, #3951, .T. ) ;
#3179=AXIS2_PLACEMENT_3D ( 'NONE', #14283, #15850, #1604 ) ;
#3189=ORIENTED_EDGE ( 'NONE', *, *, #1049, .F. ) ;
#3190=VECTOR ( 'NONE', #17756, 1000.000000000000000 ) ;
#3193=VECTOR ( 'NONE', #7406, 1000.000000000000000 ) ;
#3196=EDGE_CURVE ( 'NONE', #1235, #13357, #16484, .T. ) ;
#3206=ORIENTED_EDGE ( 'NONE', *, *, #9000, .T. ) ;
#3207=VECTOR ( 'NONE', #17429, 1000.000000000000000 ) ;
#3208=LINE ( 'NONE', #14319, #543 ) ;
#3211=FACE_OUTER_BOUND ( 'NONE', #15985, .T. ) ;
#3214=VERTEX_POINT ( 'NONE', #14275 ) ;
#3215=CARTESIAN_POINT ( 'NONE',  ( 2.500000000000000000, 2.799999999999999822, 1.600000000000000089 ) ) ;
#3223=LINE ( 'NONE', #8955, #12945 ) ;
#3226=EDGE_CURVE ( 'NONE', #1639, #14807, #10022, .T. ) ;
#3231=FACE_BOUND ( 'NONE', #12525, .T. ) ;
#3235=VERTEX_POINT ( 'NONE', #2857 ) ;
#3236=CARTESIAN_POINT ( 'NONE',  ( 1.899999999999999911, 2.481229107598850043E-16, 3.278889744907200310 ) ) ;
#3240=DIRECTION ( 'NONE',  ( 5.551115123125780730E-16, 0.000000000000000000, 1.000000000000000000 ) ) ;
#3241=ORIENTED_EDGE ( 'NONE', *, *, #12998, .F. ) ;
#3253=CIRCLE ( 'NONE', #7121, 0.5999999999999998668 ) ;
#3259=EDGE_LOOP ( 'NONE', ( #7078, #14668, #11387 ) ) ;
#3263=LINE ( 'NONE', #8905, #10014 ) ;
#3264=ORIENTED_EDGE ( 'NONE', *, *, #9028, .F. ) ;
#3270=VECTOR ( 'NONE', #15729, 1000.000000000000000 ) ;
#3280=LINE ( 'NONE', #1713, #13811 ) ;
#3283=VECTOR ( 'NONE', #12379, 1000.000000000000000 ) ;
#3291=CARTESIAN_POINT ( 'NONE',  ( -1.899999999999999911, 9.199999999999999289, 0.6099999999999999867 ) ) ;
#3295=ORIENTED_EDGE ( 'NONE', *, *, #8241, .F. ) ;
#3296=LINE ( 'NONE', #1383, #11459 ) ;
#3308=CARTESIAN_POINT ( 'NONE',  ( 2.500000000000000000, -6.661338147750919275E-17, 9.955530934770520091 ) ) ;
#3314=CARTESIAN_POINT ( 'NONE',  ( 2.616666666666660035, 8.899094389694600942E-17, 4.000000000000000000 ) ) ;
#3318=DIRECTION ( 'NONE',  ( 1.000000000000000000, 0.000000000000000000, 0.000000000000000000 ) ) ;
#3320=DIRECTION ( 'NONE',  ( 7.401486830834380223E-16, 1.769136588914770194E-30, -1.000000000000000000 ) ) ;
#3322=CARTESIAN_POINT ( 'NONE',  ( -1.899999999999999911, 10.00000000000000000, 7.286648454926749993E-16 ) ) ;
#3323=ORIENTED_EDGE ( 'NONE', *, *, #4848, .T. ) ;
#3324=CARTESIAN_POINT ( 'NONE',  ( 1.875000000000000000, 12.00000000000000000, 8.300000000000000711 ) ) ;
#3326=ORIENTED_EDGE ( 'NONE', *, *, #8472, .F. ) ;
#3328=CARTESIAN_POINT ( 'NONE',  ( 1.899999999999999911, 0.8000000000000000444, -1.333009822025779987E-15 ) ) ;
#3335=SPHERICAL_SURFACE ( 'NONE', #15082, 0.4166666666666670182 ) ;
#3339=VERTEX_POINT ( 'NONE', #17291 ) ;
#3340=ORIENTED_EDGE ( 'NONE', *, *, #16621, .F. ) ;
#3355=ORIENTED_EDGE ( 'NONE', *, *, #1782, .F. ) ;
#3357=PLANE ( 'NONE',  #6453 ) ;
#3358=CARTESIAN_POINT ( 'NONE',  ( 4.265698758777729940E-16, 2.350000000000000089, 7.700000000000000178 ) ) ;
#3376=CARTESIAN_POINT ( 'NONE',  ( -1.899999999999999911, -2.607830583485270085E-17, -8.881784197001250351E-16 ) ) ;
#3382=DIRECTION ( 'NONE',  ( 0.9622640697945192834, -0.2721173643531200614, 0.000000000000000000 ) ) ;
#3383=DIRECTION ( 'NONE',  ( 0.000000000000000000, -1.000000000000000000, 1.807003620809174385E-16 ) ) ;
#3387=CARTESIAN_POINT ( 'NONE',  ( -1.875000000000000000, 12.00000000000000000, 8.300000000000000711 ) ) ;
#3392=EDGE_CURVE ( 'NONE', #1178, #9534, #5573, .T. ) ;
#3393=DIRECTION ( 'NONE',  ( 0.000000000000000000, 0.000000000000000000, -1.000000000000000000 ) ) ;
#3395=DIRECTION ( 'NONE',  ( 0.000000000000000000, 0.000000000000000000, 1.000000000000000000 ) ) ;
#3397=ORIENTED_EDGE ( 'NONE', *, *, #17367, .F. ) ;
#3399=CARTESIAN_POINT ( 'NONE',  ( 1.899999999999999911, 4.700000000000000178, 1.600000000000000089 ) ) ;
#3407=CARTESIAN_POINT ( 'NONE',  ( 1.889999999999999902, 4.700000000000000178, 0.6099999999999999867 ) ) ;
#3413=FACE_OUTER_BOUND ( 'NONE', #14009, .T. ) ;
#3418=ORIENTED_EDGE ( 'NONE', *, *, #4617, .T. ) ;
#3422=CARTESIAN_POINT ( 'NONE',  ( 2.500000000000000000, 11.15000000000000036, -1.135674796306499891E-15 ) ) ;
#3425=CARTESIAN_POINT ( 'NONE',  ( -0.03000000000000110217, 11.40000000000000036, 7.649999999999999467 ) ) ;
#3426=DIRECTION ( 'NONE',  ( 0.000000000000000000, 1.000000000000000000, -1.110223024625159992E-16 ) ) ;
#3434=VECTOR ( 'NONE', #16823, 1000.000000000000000 ) ;
#3451=CARTESIAN_POINT ( 'NONE',  ( 1.800000000000000044, 12.00000000000000000, 7.649999999999999467 ) ) ;
#3453=FACE_BOUND ( 'NONE', #18208, .T. ) ;
#3456=LINE ( 'NONE', #10699, #7619 ) ;
#3457=VECTOR ( 'NONE', #12795, 1000.000000000000000 ) ;
#3462=EDGE_LOOP ( 'NONE', ( #13580, #13123, #13586, #6365 ) ) ;
#3464=LINE ( 'NONE', #14772, #11349 ) ;
#3466=FACE_OUTER_BOUND ( 'NONE', #9370, .T. ) ;
#3469=EDGE_CURVE ( 'NONE', #15324, #12277, #5142, .T. ) ;
#3474=CYLINDRICAL_SURFACE ( 'NONE', #1686, 0.4000000000000000222 ) ;
#3475=EDGE_CURVE ( 'NONE', #9567, #9752, #224, .T. ) ;
#3480=SPHERICAL_SURFACE ( 'NONE', #14169, 1.016666666666670160 ) ;
#3489=ORIENTED_EDGE ( 'NONE', *, *, #7338, .T. ) ;
#3490=DIRECTION ( 'NONE',  ( -3.315303352997239924E-31, 1.000000000000000000, -8.588360937600549480E-46 ) ) ;
#3492=CARTESIAN_POINT ( 'NONE',  ( -1.800000000000000044, 11.40000000000000036, 1.600000000000000089 ) ) ;
#3497=DIRECTION ( 'NONE',  ( 0.000000000000000000, -1.000000000000000000, 0.000000000000000000 ) ) ;
#3504=DIRECTION ( 'NONE',  ( 2.960594732333750117E-15, 2.960594732333750117E-15, -1.000000000000000000 ) ) ;
#3519=EDGE_CURVE ( 'NONE', #435, #1178, #9301, .T. ) ;
#3524=ORIENTED_EDGE ( 'NONE', *, *, #13668, .T. ) ;
#3525=DIRECTION ( 'NONE',  ( -1.000000000000000000, -4.014365738757630620E-15, -1.254489293361759815E-16 ) ) ;
#3526=VERTEX_POINT ( 'NONE', #2279 ) ;
#3527=PLANE ( 'NONE',  #3004 ) ;
#3532=AXIS2_PLACEMENT_3D ( 'NONE', #16020, #6271, #10170 ) ;
#3535=ORIENTED_EDGE ( 'NONE', *, *, #7921, .T. ) ;
#3537=ORIENTED_EDGE ( 'NONE', *, *, #3623, .F. ) ;
#3542=CIRCLE ( 'NONE', #10071, 0.6999999999999992895 ) ;
#3545=ORIENTED_EDGE ( 'NONE', *, *, #17166, .T. ) ;
#3548=CARTESIAN_POINT ( 'NONE',  ( 1.889999999999999902, 4.100000000000000533, 0.5999999999999999778 ) ) ;
#3549=DIRECTION ( 'NONE',  ( 2.936127007273139866E-16, 0.000000000000000000, -1.000000000000000000 ) ) ;
#3556=DIRECTION ( 'NONE',  ( 0.000000000000000000, -1.000000000000000000, 1.110223024625159992E-16 ) ) ;
#3562=DIRECTION ( 'NONE',  ( -1.000000000000000000, 0.000000000000000000, 0.000000000000000000 ) ) ;
#3564=ORIENTED_EDGE ( 'NONE', *, *, #13003, .T. ) ;
#3567=FACE_OUTER_BOUND ( 'NONE', #14925, .T. ) ;
#3574=EDGE_CURVE ( 'NONE', #7200, #15044, #10543, .T. ) ;
#3575=DIRECTION ( 'NONE',  ( -2.960594732333750117E-16, -1.000000000000000000, 0.000000000000000000 ) ) ;
#3579=EDGE_CURVE ( 'NONE', #2390, #13806, #8786, .T. ) ;
#3580=CARTESIAN_POINT ( 'NONE',  ( -1.899999999999999911, 11.15000000000000036, 2.137972338849589826E-15 ) ) ;
#3601=CARTESIAN_POINT ( 'NONE',  ( -1.899999999999999911, 4.700000000000000178, 1.600000000000000089 ) ) ;
#3604=EDGE_CURVE ( 'NONE', #13146, #389, #8393, .T. ) ;
#3610=VERTEX_POINT ( 'NONE', #188 ) ;
#3621=PLANE ( 'NONE',  #11736 ) ;
#3622=VERTEX_POINT ( 'NONE', #13053 ) ;
#3623=EDGE_CURVE ( 'NONE', #10942, #15772, #15571, .T. ) ;
#3624=LINE ( 'NONE', #8273, #7611 ) ;
#3630=ORIENTED_EDGE ( 'NONE', *, *, #11312, .T. ) ;
#3635=ORIENTED_EDGE ( 'NONE', *, *, #6228, .T. ) ;
#3636=CARTESIAN_POINT ( 'NONE',  ( 2.241103642439659443E-15, 9.099999999999999645, 7.700000000000000178 ) ) ;
#3638=ADVANCED_FACE ( 'NONE', ( #11393 ), #11656, .F. ) ;
#3641=LINE ( 'NONE', #10493, #2306 ) ;
#3642=CYLINDRICAL_SURFACE ( 'NONE', #2343, 0.6000000000000000888 ) ;
#3644=EDGE_LOOP ( 'NONE', ( #4944, #9300, #15904, #13361 ) ) ;
#3650=ORIENTED_EDGE ( 'NONE', *, *, #12443, .F. ) ;
#3655=ORIENTED_EDGE ( 'NONE', *, *, #14908, .F. ) ;
#3659=DIRECTION ( 'NONE',  ( 3.700743415417190112E-16, 1.000000000000000000, -1.850371707708589879E-16 ) ) ;
#3667=LINE ( 'NONE', #2199, #11478 ) ;
#3668=CARTESIAN_POINT ( 'NONE',  ( -2.500000000000000000, 2.000000000000000000, 2.755455298081550201E-16 ) ) ;
#3681=CARTESIAN_POINT ( 'NONE',  ( -1.399999999999999911, 5.799999999999999822, 7.700000000000000178 ) ) ;
#3686=EDGE_CURVE ( 'NONE', #4246, #3854, #1764, .T. ) ;
#3694=CARTESIAN_POINT ( 'NONE',  ( -1.889999999999999902, 7.900000000000000355, 3.000000000000000000 ) ) ;
#3699=VECTOR ( 'NONE', #6516, 1000.000000000000000 ) ;
#3705=ORIENTED_EDGE ( 'NONE', *, *, #6178, .T. ) ;
#3706=DIRECTION ( 'NONE',  ( 1.059690869644410208E-14, 1.000000000000000000, -1.027162637006522002E-32 ) ) ;
#3709=DIRECTION ( 'NONE',  ( 1.000000000000000000, 0.000000000000000000, 0.000000000000000000 ) ) ;
#3711=AXIS2_PLACEMENT_3D ( 'NONE', #17892, #6615, #5042 ) ;
#3713=DIRECTION ( 'NONE',  ( 0.000000000000000000, -1.000000000000000000, 0.000000000000000000 ) ) ;
#3717=ORIENTED_EDGE ( 'NONE', *, *, #2565, .T. ) ;
#3721=FACE_OUTER_BOUND ( 'NONE', #5602, .T. ) ;
#3723=AXIS2_PLACEMENT_3D ( 'NONE', #3548, #9195, #5130 ) ;
#3727=VERTEX_POINT ( 'NONE', #10643 ) ;
#3733=VECTOR ( 'NONE', #5842, 1000.000000000000000 ) ;
#3736=PLANE ( 'NONE',  #4405 ) ;
#3746=AXIS2_PLACEMENT_3D ( 'NONE', #9139, #15098, #10725 ) ;
#3750=ORIENTED_EDGE ( 'NONE', *, *, #7232, .T. ) ;
#3751=EDGE_CURVE ( 'NONE', #11239, #7262, #18207, .T. ) ;
#3760=LINE ( 'NONE', #9423, #13888 ) ;
#3762=LINE ( 'NONE', #3387, #8235 ) ;
#3766=AXIS2_PLACEMENT_3D ( 'NONE', #3901, #15214, #18048 ) ;
#3773=DIRECTION ( 'NONE',  ( 2.220446049250309876E-16, 1.000000000000000000, 0.000000000000000000 ) ) ;
#3774=VECTOR ( 'NONE', #4566, 1000.000000000000000 ) ;
#3777=LINE ( 'NONE', #9609, #11025 ) ;
#3785=AXIS2_PLACEMENT_3D ( 'NONE', #11468, #8774, #7482 ) ;
#3792=CARTESIAN_POINT ( 'NONE',  ( -1.800000000000000044, 11.29999999999999893, 7.649999999999999467 ) ) ;
#3795=VECTOR ( 'NONE', #2109, 1000.000000000000000 ) ;
#3796=DIRECTION ( 'NONE',  ( 0.000000000000000000, -1.000000000000000000, 0.000000000000000000 ) ) ;
#3804=ORIENTED_EDGE ( 'NONE', *, *, #17656, .T. ) ;
#3808=ORIENTED_EDGE ( 'NONE', *, *, #16592, .F. ) ;
#3813=VECTOR ( 'NONE', #7499, 1000.000000000000000 ) ;
#3816=EDGE_LOOP ( 'NONE', ( #12509, #16636, #15774, #6623 ) ) ;
#3824=VERTEX_POINT ( 'NONE', #3399 ) ;
#3828=EDGE_CURVE ( 'NONE', #13806, #10942, #13414, .T. ) ;
#3830=VERTEX_POINT ( 'NONE', #13143 ) ;
#3837=AXIS2_PLACEMENT_3D ( 'NONE', #17277, #10257, #4787 ) ;
#3840=CARTESIAN_POINT ( 'NONE',  ( -1.875000000000000000, 0.7500000000000000000, 8.300000000000000711 ) ) ;
#3842=DIRECTION ( 'NONE',  ( -0.000000000000000000, 1.000000000000000000, 0.000000000000000000 ) ) ;
#3844=ORIENTED_EDGE ( 'NONE', *, *, #17696, .T. ) ;
#3846=DIRECTION ( 'NONE',  ( -2.478176394252584099E-15, 1.000000000000000000, 0.000000000000000000 ) ) ;
#3852=CYLINDRICAL_SURFACE ( 'NONE', #595, 0.3499999999999999778 ) ;
#3854=VERTEX_POINT ( 'NONE', #16379 ) ;
#3858=ORIENTED_EDGE ( 'NONE', *, *, #17628, .F. ) ;
#3861=DIRECTION ( 'NONE',  ( -1.054711873393900133E-14, -1.000000000000000000, 0.000000000000000000 ) ) ;
#3870=DIRECTION ( 'NONE',  ( 0.000000000000000000, 1.000000000000000000, 1.665334536937730077E-15 ) ) ;
#3873=LINE ( 'NONE', #10727, #13380 ) ;
#3881=DIRECTION ( 'NONE',  ( -1.000000000000000000, 0.000000000000000000, 0.000000000000000000 ) ) ;
#3882=VERTEX_POINT ( 'NONE', #7496 ) ;
#3884=DIRECTION ( 'NONE',  ( 1.000000000000000000, 0.000000000000000000, -4.265713465516738421E-15 ) ) ;
#3886=FACE_OUTER_BOUND ( 'NONE', #11950, .T. ) ;
#3887=DIRECTION ( 'NONE',  ( -2.993800930630270167E-16, -6.049014748177290126E-16, 1.000000000000000000 ) ) ;
#3892=DIRECTION ( 'NONE',  ( -1.000000000000000000, 1.776356839399099990E-14, 0.000000000000000000 ) ) ;
#3896=VERTEX_POINT ( 'NONE', #3324 ) ;
#3899=LINE ( 'NONE', #15302, #15653 ) ;
#3901=CARTESIAN_POINT ( 'NONE',  ( 1.889999999999999902, 4.100000000000000533, 0.5999999999999999778 ) ) ;
#3909=ORIENTED_EDGE ( 'NONE', *, *, #1782, .T. ) ;
#3912=CARTESIAN_POINT ( 'NONE',  ( -1.599999999999869971, 12.00000000000000000, 1.600000000000000089 ) ) ;
#3915=EDGE_CURVE ( 'NONE', #7890, #1801, #13319, .T. ) ;
#3919=AXIS2_PLACEMENT_3D ( 'NONE', #2465, #6713, #13749 ) ;
#3926=CARTESIAN_POINT ( 'NONE',  ( -1.899999999999999911, 3.500000000000000000, 0.6099999999999999867 ) ) ;
#3936=ORIENTED_EDGE ( 'NONE', *, *, #6066, .T. ) ;
#3948=VECTOR ( 'NONE', #8945, 1000.000000000000000 ) ;
#3951=EDGE_CURVE ( 'NONE', #9752, #6669, #3964, .T. ) ;
#3954=ORIENTED_EDGE ( 'NONE', *, *, #3172, .F. ) ;
#3956=VECTOR ( 'NONE', #371, 1000.000000000000000 ) ;
#3964=LINE ( 'NONE', #15277, #1660 ) ;
#3971=VECTOR ( 'NONE', #13530, 1000.000000000000000 ) ;
#3972=CARTESIAN_POINT ( 'NONE',  ( -1.875000000000000000, 0.7500000000000000000, 8.300000000000000711 ) ) ;
#3974=DIRECTION ( 'NONE',  ( 0.000000000000000000, 0.000000000000000000, 1.000000000000000000 ) ) ;
#3976=ADVANCED_FACE ( 'NONE', ( #5274 ), #10822, .T. ) ;
#3977=CARTESIAN_POINT ( 'NONE',  ( 0.02999999999999850009, 12.00000000000000000, 1.600000000000000089 ) ) ;
#3982=ORIENTED_EDGE ( 'NONE', *, *, #10149, .T. ) ;
#4010=EDGE_CURVE ( 'NONE', #12747, #12720, #8752, .T. ) ;
#4011=CARTESIAN_POINT ( 'NONE',  ( 1.889999999999999902, 4.700000000000000178, 0.5999999999999999778 ) ) ;
#4015=AXIS2_PLACEMENT_3D ( 'NONE', #13706, #6653, #6846 ) ;
#4016=ORIENTED_EDGE ( 'NONE', *, *, #15036, .F. ) ;
#4017=DIRECTION ( 'NONE',  ( -1.000000000000000000, 0.000000000000000000, 0.000000000000000000 ) ) ;
#4018=CARTESIAN_POINT ( 'NONE',  ( 0.2000000000000000111, 0.1000000000000000056, 8.300000000000000711 ) ) ;
#4021=ADVANCED_FACE ( 'NONE', ( #16573 ), #13781, .F. ) ;
#4027=DIRECTION ( 'NONE',  ( -2.220446049250309876E-16, -1.000000000000000000, -3.286920438420880041E-31 ) ) ;
#4035=LINE ( 'NONE', #2662, #5558 ) ;
#4037=DIRECTION ( 'NONE',  ( -6.123233995736779594E-17, -2.493473113004680074E-16, -1.000000000000000000 ) ) ;
#4038=EDGE_CURVE ( 'NONE', #389, #4246, #16736, .T. ) ;
#4041=AXIS2_PLACEMENT_3D ( 'NONE', #12558, #1265, #14227 ) ;
#4043=CARTESIAN_POINT ( 'NONE',  ( 1.000000000000002220, 9.099999999999999645, 8.300000000000000711 ) ) ;
#4045=EDGE_CURVE ( 'NONE', #8261, #7811, #18187, .T. ) ;
#4047=CARTESIAN_POINT ( 'NONE',  ( -1.899999999999999911, 0.7211102550927980248, 7.649999999999999467 ) ) ;
#4050=ORIENTED_EDGE ( 'NONE', *, *, #13543, .F. ) ;
#4052=LINE ( 'NONE', #4422, #7137 ) ;
#4053=CARTESIAN_POINT ( 'NONE',  ( 1.889999999999999902, 7.299999999999999822, 0.6099999999999999867 ) ) ;
#4064=AXIS2_PLACEMENT_3D ( 'NONE', #7464, #6153, #3105 ) ;
#4067=ADVANCED_FACE ( 'NONE', ( #5480 ), #8630, .F. ) ;
#4068=CARTESIAN_POINT ( 'NONE',  ( 4.898587196589409994E-17, 0.1000000000000000056, 8.300000000000000711 ) ) ;
#4070=ORIENTED_EDGE ( 'NONE', *, *, #216, .F. ) ;
#4073=AXIS2_PLACEMENT_3D ( 'NONE', #17465, #7572, #17546 ) ;
#4074=DIRECTION ( 'NONE',  ( 1.000000000000000000, 0.000000000000000000, 0.000000000000000000 ) ) ;
#4079=ORIENTED_EDGE ( 'NONE', *, *, #2944, .T. ) ;
#4080=CARTESIAN_POINT ( 'NONE',  ( -1.875000000000000000, 2.296212748401290437E-16, 8.300000000000000711 ) ) ;
#4082=FACE_OUTER_BOUND ( 'NONE', #1351, .T. ) ;
#4083=LINE ( 'NONE', #11399, #802 ) ;
#4085=AXIS2_PLACEMENT_3D ( 'NONE', #4923, #871, #5212 ) ;
#4092=VECTOR ( 'NONE', #15445, 1000.000000000000000 ) ;
#4096=VERTEX_POINT ( 'NONE', #4356 ) ;
#4099=VERTEX_POINT ( 'NONE', #6957 ) ;
#4100=AXIS2_PLACEMENT_3D ( 'NONE', #11217, #13807, #15486 ) ;
#4102=CARTESIAN_POINT ( 'NONE',  ( -1.800000000000000044, 12.00000000000000000, 7.649999999999999467 ) ) ;
#4103=ORIENTED_EDGE ( 'NONE', *, *, #10149, .F. ) ;
#4109=ORIENTED_EDGE ( 'NONE', *, *, #7557, .T. ) ;
#4116=CARTESIAN_POINT ( 'NONE',  ( -1.889999999999999902, 8.500000000000000000, 0.6099999999999999867 ) ) ;
#4127=CIRCLE ( 'NONE', #11224, 0.01000000000000002623 ) ;
#4130=CARTESIAN_POINT ( 'NONE',  ( 2.500000000000000000, 9.199999999999999289, 1.600000000000000089 ) ) ;
#4134=CARTESIAN_POINT ( 'NONE',  ( -0.9999999999999978906, 9.099999999999999645, 8.300000000000000711 ) ) ;
#4135=ORIENTED_EDGE ( 'NONE', *, *, #8669, .F. ) ;
#4146=DIRECTION ( 'NONE',  ( 1.000000000000000000, 0.000000000000000000, 0.000000000000000000 ) ) ;
#4149=AXIS2_PLACEMENT_3D ( 'NONE', #9505, #2471, #11998 ) ;
#4154=ADVANCED_FACE ( 'NONE', ( #2988 ), #5393, .F. ) ;
#4162=AXIS2_PLACEMENT_3D ( 'NONE', #10507, #16168, #11634 ) ;
#4168=ORIENTED_EDGE ( 'NONE', *, *, #3604, .T. ) ;
#4173=EDGE_CURVE ( 'NONE', #5456, #3896, #8442, .T. ) ;
#4176=DIRECTION ( 'NONE',  ( 0.000000000000000000, 0.000000000000000000, 1.000000000000000000 ) ) ;
#4178=CARTESIAN_POINT ( 'NONE',  ( -1.889999999999999902, 4.100000000000000533, 0.5999999999999999778 ) ) ;
#4185=LINE ( 'NONE', #3075, #10932 ) ;
#4186=ORIENTED_EDGE ( 'NONE', *, *, #1514, .F. ) ;
#4189=ORIENTED_EDGE ( 'NONE', *, *, #14908, .T. ) ;
#4190=ORIENTED_EDGE ( 'NONE', *, *, #3751, .T. ) ;
#4195=VERTEX_POINT ( 'NONE', #2893 ) ;
#4198=ORIENTED_EDGE ( 'NONE', *, *, #7643, .F. ) ;
#4199=LINE ( 'NONE', #3840, #8181 ) ;
#4204=CARTESIAN_POINT ( 'NONE',  ( -2.500000000000000000, 0.7500000000000000000, 7.649999999999999467 ) ) ;
#4206=CARTESIAN_POINT ( 'NONE',  ( 1.889999999999999902, 7.900000000000000355, 3.000000000000000000 ) ) ;
#4211=ORIENTED_EDGE ( 'NONE', *, *, #7129, .T. ) ;
#4212=VECTOR ( 'NONE', #5424, 1000.000000000000000 ) ;
#4214=CARTESIAN_POINT ( 'NONE',  ( 1.899999999999999911, 4.700000000000000178, 0.6099999999999999867 ) ) ;
#4215=DIRECTION ( 'NONE',  ( 0.000000000000000000, 1.000000000000000000, 0.000000000000000000 ) ) ;
#4218=DIRECTION ( 'NONE',  ( -1.000000000000000000, 0.000000000000000000, 3.700743415417190112E-16 ) ) ;
#4223=AXIS2_PLACEMENT_3D ( 'NONE', #5537, #2954, #11185 ) ;
#4224=ORIENTED_EDGE ( 'NONE', *, *, #16302, .F. ) ;
#4228=DIRECTION ( 'NONE',  ( -1.110223024625159992E-16, 0.000000000000000000, 1.000000000000000000 ) ) ;
#4243=CARTESIAN_POINT ( 'NONE',  ( 4.898587196589409994E-17, 0.1000000000000000056, 8.300000000000000711 ) ) ;
#4246=VERTEX_POINT ( 'NONE', #112 ) ;
#4252=VERTEX_POINT ( 'NONE', #6870 ) ;
#4253=EDGE_CURVE ( 'NONE', #3214, #15169, #4798, .T. ) ;
#4260=CARTESIAN_POINT ( 'NONE',  ( 2.500000000000000000, 9.199999999999999289, 0.6099999999999999867 ) ) ;
#4267=EDGE_CURVE ( 'NONE', #15324, #2153, #9969, .T. ) ;
#4271=DIRECTION ( 'NONE',  ( -4.318427418585891014E-15, 2.220446049250309876E-16, -1.000000000000000000 ) ) ;
#4272=VERTEX_POINT ( 'NONE', #4715 ) ;
#4289=DIRECTION ( 'NONE',  ( -1.000000000000000000, 1.480297366166869931E-15, 0.000000000000000000 ) ) ;
#4293=ORIENTED_EDGE ( 'NONE', *, *, #11615, .F. ) ;
#4294=PLANE ( 'NONE',  #17200 ) ;
#4296=EDGE_CURVE ( 'NONE', #14130, #10006, #17290, .T. ) ;
#4297=ORIENTED_EDGE ( 'NONE', *, *, #320, .T. ) ;
#4303=LINE ( 'NONE', #11530, #2884 ) ;
#4310=AXIS2_PLACEMENT_3D ( 'NONE', #8425, #15562, #176 ) ;
#4321=ORIENTED_EDGE ( 'NONE', *, *, #205, .T. ) ;
#4322=LINE ( 'NONE', #9804, #10968 ) ;
#4324=ORIENTED_EDGE ( 'NONE', *, *, #2700, .F. ) ;
#4337=AXIS2_PLACEMENT_3D ( 'NONE', #13400, #12204, #18009 ) ;
#4338=FACE_OUTER_BOUND ( 'NONE', #2189, .T. ) ;
#4344=CARTESIAN_POINT ( 'NONE',  ( -1.875000000000000000, 2.296212748401290437E-16, 7.700000000000000178 ) ) ;
#4353=LINE ( 'NONE', #10017, #6735 ) ;
#4356=CARTESIAN_POINT ( 'NONE',  ( -1.899999999999999911, 4.700000000000000178, 0.6099999999999999867 ) ) ;
#4357=DIRECTION ( 'NONE',  ( 1.000000000000000000, 0.000000000000000000, -7.401486830834370362E-16 ) ) ;
#4365=DIRECTION ( 'NONE',  ( 0.000000000000000000, 0.000000000000000000, -1.000000000000000000 ) ) ;
#4366=DIRECTION ( 'NONE',  ( 0.000000000000000000, 0.000000000000000000, 1.000000000000000000 ) ) ;
#4368=AXIS2_PLACEMENT_3D ( 'NONE', #17992, #14766, #3556 ) ;
#4377=STYLED_ITEM ( 'NONE', ( #15382 ), #8014 ) ;
#4378=VECTOR ( 'NONE', #1385, 1000.000000000000000 ) ;
#4379=VERTEX_POINT ( 'NONE', #8803 ) ;
#4383=ORIENTED_EDGE ( 'NONE', *, *, #11612, .F. ) ;
#4384=EDGE_CURVE ( 'NONE', #475, #7297, #11573, .T. ) ;
#4385=VECTOR ( 'NONE', #9784, 1000.000000000000000 ) ;
#4393=DIRECTION ( 'NONE',  ( 2.537652627714639929E-16, 1.000000000000000000, 0.000000000000000000 ) ) ;
#4398=CARTESIAN_POINT ( 'NONE',  ( 0.03000000000000110217, 11.40000000000000036, 7.649999999999999467 ) ) ;
#4402=DIRECTION ( 'NONE',  ( -1.000000000000000000, 0.000000000000000000, 0.000000000000000000 ) ) ;
#4405=AXIS2_PLACEMENT_3D ( 'NONE', #13663, #4942, #14763 ) ;
#4408=CARTESIAN_POINT ( 'NONE',  ( -1.899999999999999911, 9.199999999999999289, 1.600000000000000089 ) ) ;
#4410=DIRECTION ( 'NONE',  ( 0.000000000000000000, 0.000000000000000000, 1.000000000000000000 ) ) ;
#4421=VERTEX_POINT ( 'NONE', #7503 ) ;
#4422=CARTESIAN_POINT ( 'NONE',  ( 0.8740908734716299477, 4.154758922476410099, 7.700000000000000178 ) ) ;
#4424=ORIENTED_EDGE ( 'NONE', *, *, #10848, .T. ) ;
#4428=CARTESIAN_POINT ( 'NONE',  ( -2.500000000000000000, 9.199999999999999289, 1.600000000000000089 ) ) ;
#4429=VECTOR ( 'NONE', #722, 1000.000000000000000 ) ;
#4431=DIRECTION ( 'NONE',  ( -0.6614378277661479011, 3.218725199566341288E-16, -0.7499999999999997780 ) ) ;
#4434=ADVANCED_BREP_SHAPE_REPRESENTATION ( '', ( #8014, #17681 ), #12094 ) ;
#4436=DIRECTION ( 'NONE',  ( 1.000000000000000000, 0.000000000000000000, -5.332141831895923026E-16 ) ) ;
#4439=CARTESIAN_POINT ( 'NONE',  ( -1.899999999999999911, 4.700000000000000178, 1.600000000000000089 ) ) ;
#4448=CARTESIAN_POINT ( 'NONE',  ( 2.500000000000000000, 11.15000000000000036, 1.600000000000000089 ) ) ;
#4468=ORIENTED_EDGE ( 'NONE', *, *, #15265, .T. ) ;
#4469=PLANE ( 'NONE',  #198 ) ;
#4480=ADVANCED_FACE ( 'NONE', ( #5282 ), #16298, .F. ) ;
#4482=EDGE_CURVE ( 'NONE', #17750, #3610, #10740, .T. ) ;
#4483=FACE_OUTER_BOUND ( 'NONE', #1214, .T. ) ;
#4489=VECTOR ( 'NONE', #8246, 1000.000000000000000 ) ;
#4490=LINE ( 'NONE', #7466, #11748 ) ;
#4491=ORIENTED_EDGE ( 'NONE', *, *, #5731, .F. ) ;
#4501=VERTEX_POINT ( 'NONE', #933 ) ;
#4502=DIRECTION ( 'NONE',  ( -8.326672684688679970E-16, 0.000000000000000000, -1.000000000000000000 ) ) ;
#4505=CARTESIAN_POINT ( 'NONE',  ( -1.889999999999999902, 4.100000000000000533, -6.851683986394989688E-16 ) ) ;
#4519=ORIENTED_EDGE ( 'NONE', *, *, #2474, .T. ) ;
#4523=DIRECTION ( 'NONE',  ( 0.000000000000000000, 0.000000000000000000, 1.000000000000000000 ) ) ;
#4528=ADVANCED_FACE ( 'NONE', ( #3886 ), #9154, .F. ) ;
#4546=LINE ( 'NONE', #3087, #5551 ) ;
#4548=ORIENTED_EDGE ( 'NONE', *, *, #659, .F. ) ;
#4557=LINE ( 'NONE', #17331, #2066 ) ;
#4566=DIRECTION ( 'NONE',  ( 0.000000000000000000, -1.000000000000000000, -1.586032892321649771E-16 ) ) ;
#4574=CARTESIAN_POINT ( 'NONE',  ( -1.875000000000000000, 2.296212748401290437E-16, 8.300000000000000711 ) ) ;
#4577=VERTEX_POINT ( 'NONE', #15008 ) ;
#4581=ORIENTED_EDGE ( 'NONE', *, *, #13884, .T. ) ;
#4582=LINE ( 'NONE', #17457, #12689 ) ;
#4586=ADVANCED_FACE ( 'NONE', ( #1023 ), #6659, .F. ) ;
#4590=EDGE_CURVE ( 'NONE', #16860, #1432, #12776, .T. ) ;
#4601=DIRECTION ( 'NONE',  ( -1.000000000000000000, 0.000000000000000000, 0.000000000000000000 ) ) ;
#4603=CIRCLE ( 'NONE', #14983, 0.5999999999999998668 ) ;
#4604=AXIS2_PLACEMENT_3D ( 'NONE', #11144, #8106, #16798 ) ;
#4605=CARTESIAN_POINT ( 'NONE',  ( 1.899999999999999911, 2.000000000000000000, -1.259531014076939845E-15 ) ) ;
#4606=ORIENTED_EDGE ( 'NONE', *, *, #17581, .F. ) ;
#4613=EDGE_CURVE ( 'NONE', #15772, #6568, #16665, .T. ) ;
#4617=EDGE_CURVE ( 'NONE', #2627, #8501, #15470, .T. ) ;
#4618=VECTOR ( 'NONE', #914, 1000.000000000000000 ) ;
#4623=DIRECTION ( 'NONE',  ( 1.000000000000000000, 9.656020733808335804E-16, 0.000000000000000000 ) ) ;
#4626=DIRECTION ( 'NONE',  ( -1.000000000000000000, 2.220446049250309876E-16, 6.123233995736769734E-17 ) ) ;
#4633=CARTESIAN_POINT ( 'NONE',  ( 0.02999999999999939868, 12.00000000000000000, 7.649999999999999467 ) ) ;
#4635=ORIENTED_EDGE ( 'NONE', *, *, #13771, .F. ) ;
#4636=VECTOR ( 'NONE', #8270, 1000.000000000000000 ) ;
#4640=ORIENTED_EDGE ( 'NONE', *, *, #11175, .F. ) ;
#4641=CARTESIAN_POINT ( 'NONE',  ( 2.500000000000000000, 0.8000000000000000444, -2.399999999999999911 ) ) ;
#4642=AXIS2_PLACEMENT_3D ( 'NONE', #17963, #9559, #13914 ) ;
#4644=CIRCLE ( 'NONE', #7036, 0.01000000000000002623 ) ;
#4647=EDGE_CURVE ( 'NONE', #13169, #3824, #15283, .T. ) ;
#4653=AXIS2_PLACEMENT_3D ( 'NONE', #16152, #2177, #13373 ) ;
#4656=VECTOR ( 'NONE', #10515, 1000.000000000000000 ) ;
#4664=PLANE ( 'NONE',  #2691 ) ;
#4668=CIRCLE ( 'NONE', #13548, 0.7000000000000000666 ) ;
#4671=CARTESIAN_POINT ( 'NONE',  ( 2.500000000000000000, 0.7500000000000000000, 7.649999999999999467 ) ) ;
#4673=AXIS2_PLACEMENT_3D ( 'NONE', #10724, #3490, #818 ) ;
#4675=VECTOR ( 'NONE', #9381, 1000.000000000000000 ) ;
#4677=ORIENTED_EDGE ( 'NONE', *, *, #17430, .T. ) ;
#4688=VECTOR ( 'NONE', #1734, 1000.000000000000000 ) ;
#4694=DIRECTION ( 'NONE',  ( 2.220446049250309876E-16, 1.000000000000000000, 8.874685183736369893E-32 ) ) ;
#4702=LINE ( 'NONE', #10437, #6197 ) ;
#4703=EDGE_LOOP ( 'NONE', ( #13029, #11339, #10061, #7714 ) ) ;
#4705=ORIENTED_EDGE ( 'NONE', *, *, #556, .T. ) ;
#4708=EDGE_CURVE ( 'NONE', #3214, #6864, #12410, .T. ) ;
#4709=ORIENTED_EDGE ( 'NONE', *, *, #155, .F. ) ;
#4710=EDGE_CURVE ( 'NONE', #229, #17764, #16844, .T. ) ;
#4715=CARTESIAN_POINT ( 'NONE',  ( -1.000000000000000000, 5.400000000000000355, 8.300000000000000711 ) ) ;
#4726=ORIENTED_EDGE ( 'NONE', *, *, #8918, .F. ) ;
#4728=DIRECTION ( 'NONE',  ( -0.2800000000000001377, 0.9599999999999999645, 0.000000000000000000 ) ) ;
#4741=CARTESIAN_POINT ( 'NONE',  ( 1.875000000000000000, 11.25000000000000000, 8.300000000000000711 ) ) ;
#4746=AXIS2_PLACEMENT_3D ( 'NONE', #751, #3706, #13256 ) ;
#4748=DIRECTION ( 'NONE',  ( 0.000000000000000000, 0.000000000000000000, 1.000000000000000000 ) ) ;
#4750=DIRECTION ( 'NONE',  ( 1.000000000000000000, 4.157615153618229646E-15, 0.000000000000000000 ) ) ;
#4755=DIRECTION ( 'NONE',  ( -6.049014748177262516E-16, -8.531426931033445878E-16, -1.000000000000000000 ) ) ;
#4756=LINE ( 'NONE', #17341, #11972 ) ;
#4760=ORIENTED_EDGE ( 'NONE', *, *, #14335, .F. ) ;
#4764=ORIENTED_EDGE ( 'NONE', *, *, #2474, .F. ) ;
#4767=DIRECTION ( 'NONE',  ( 0.000000000000000000, 2.220446049250309876E-16, -1.000000000000000000 ) ) ;
#4769=EDGE_LOOP ( 'NONE', ( #16400, #10079, #5642, #13980 ) ) ;
#4771=ORIENTED_EDGE ( 'NONE', *, *, #13003, .F. ) ;
#4777=EDGE_CURVE ( 'NONE', #1639, #240, #6059, .T. ) ;
#4784=CARTESIAN_POINT ( 'NONE',  ( -1.399999999999999911, 6.400000000000000355, 8.300000000000000711 ) ) ;
#4787=DIRECTION ( 'NONE',  ( 1.224646799147340881E-16, 1.000000000000000000, 0.000000000000000000 ) ) ;
#4790=EDGE_LOOP ( 'NONE', ( #5247, #4764, #4886, #9134, #9211, #455, #615, #5862 ) ) ;
#4794=EDGE_CURVE ( 'NONE', #18164, #37, #4756, .T. ) ;
#4798=LINE ( 'NONE', #4448, #3733 ) ;
#4810=VERTEX_POINT ( 'NONE', #6154 ) ;
#4811=ORIENTED_EDGE ( 'NONE', *, *, #13193, .T. ) ;
#4814=CYLINDRICAL_SURFACE ( 'NONE', #4746, 0.3999999999999999667 ) ;
#4819=ORIENTED_EDGE ( 'NONE', *, *, #6530, .T. ) ;
#4829=EDGE_CURVE ( 'NONE', #14423, #5781, #7727, .T. ) ;
#4830=ADVANCED_FACE ( 'NONE', ( #5036 ), #14760, .T. ) ;
#4831=EDGE_LOOP ( 'NONE', ( #12548, #9706, #13268, #6034 ) ) ;
#4833=EDGE_CURVE ( 'NONE', #5409, #7679, #12085, .T. ) ;
#4838=CARTESIAN_POINT ( 'NONE',  ( 1.899999999999999911, 10.00000000000000000, 1.600000000000000089 ) ) ;
#4844=DIRECTION ( 'NONE',  ( -0.6614378277661479011, 3.218725199566341288E-16, -0.7499999999999997780 ) ) ;
#4847=CARTESIAN_POINT ( 'NONE',  ( -1.875000000000000000, 0.7500000000000000000, 7.700000000000000178 ) ) ;
#4848=EDGE_CURVE ( 'NONE', #15692, #3854, #7542, .T. ) ;
#4861=PLANE ( 'NONE',  #4162 ) ;
#4866=DIRECTION ( 'NONE',  ( -4.265713465516724418E-16, -1.000000000000000000, 0.000000000000000000 ) ) ;
#4869=CARTESIAN_POINT ( 'NONE',  ( 1.600000000000000089, 3.147362922373949982E-16, 4.000000000000000000 ) ) ;
#4876=DIRECTION ( 'NONE',  ( 1.554023113895890109E-14, -1.000000000000000000, -1.110223024626929998E-16 ) ) ;
#4883=ORIENTED_EDGE ( 'NONE', *, *, #9718, .T. ) ;
#4886=ORIENTED_EDGE ( 'NONE', *, *, #14388, .T. ) ;
#4888=DIRECTION ( 'NONE',  ( -6.344131569286580347E-16, -1.000000000000000000, 1.586032892321649771E-16 ) ) ;
#4890=CARTESIAN_POINT ( 'NONE',  ( -1.899999999999999911, 2.664535259100380036E-16, 9.955530934770520091 ) ) ;
#4898=EDGE_LOOP ( 'NONE', ( #15119, #2518, #15485, #12345 ) ) ;
#4903=ORIENTED_EDGE ( 'NONE', *, *, #13611, .T. ) ;
#4908=VECTOR ( 'NONE', #7918, 1000.000000000000000 ) ;
#4911=ORIENTED_EDGE ( 'NONE', *, *, #199, .T. ) ;
#4921=VECTOR ( 'NONE', #5665, 1000.000000000000000 ) ;
#4923=CARTESIAN_POINT ( 'NONE',  ( 1.889999999999999902, 7.299999999999999822, -3.330669073875469621E-16 ) ) ;
#4931=ORIENTED_EDGE ( 'NONE', *, *, #10489, .F. ) ;
#4933=ADVANCED_FACE ( 'NONE', ( #684 ), #423, .T. ) ;
#4935=ADVANCED_FACE ( 'NONE', ( #10590 ), #16244, .F. ) ;
#4937=FACE_OUTER_BOUND ( 'NONE', #16503, .T. ) ;
#4942=DIRECTION ( 'NONE',  ( -1.000000000000000000, -4.379659758543260954E-15, -5.767392335715200210E-18 ) ) ;
#4944=ORIENTED_EDGE ( 'NONE', *, *, #10962, .T. ) ;
#4955=EDGE_LOOP ( 'NONE', ( #9507, #13430, #2038, #121 ) ) ;
#4958=LINE ( 'NONE', #2286, #12744 ) ;
#4959=CARTESIAN_POINT ( 'NONE',  ( -2.500000000000000000, -4.577131790655780032E-16, 4.000000000000000000 ) ) ;
#4967=VECTOR ( 'NONE', #7050, 1000.000000000000000 ) ;
#4968=CARTESIAN_POINT ( 'NONE',  ( -1.889999999999999902, 4.700000000000000178, -6.736680183027569082E-16 ) ) ;
#4971=CARTESIAN_POINT ( 'NONE',  ( -1.899999999999999911, 4.218847493575600080E-16, -1.799976276337670169E-31 ) ) ;
#4973=CARTESIAN_POINT ( 'NONE',  ( 2.500000000000000000, 4.700000000000000178, 0.6099999999999999867 ) ) ;
#4977=DIRECTION ( 'NONE',  ( 1.142385477618690076E-14, -1.110223024625153952E-16, 1.000000000000000000 ) ) ;
#4986=EDGE_CURVE ( 'NONE', #16040, #13169, #884, .T. ) ;
#4990=CARTESIAN_POINT ( 'NONE',  ( -1.889999999999999902, 7.299999999999999822, 0.6099999999999999867 ) ) ;
#4994=EDGE_LOOP ( 'NONE', ( #4297, #17280, #6359, #11695 ) ) ;
#4996=DIRECTION ( 'NONE',  ( 1.054711873393900133E-14, 1.000000000000000000, 0.000000000000000000 ) ) ;
#5000=EDGE_CURVE ( 'NONE', #14551, #11214, #6609, .T. ) ;
#5005=FACE_OUTER_BOUND ( 'NONE', #16882, .T. ) ;
#5010=AXIS2_PLACEMENT_3D ( 'NONE', #3157, #4626, #7509 ) ;
#5012=DIRECTION ( 'NONE',  ( 3.097720492815730124E-16, 1.000000000000000000, 0.000000000000000000 ) ) ;
#5014=EDGE_LOOP ( 'NONE', ( #15078, #7514, #15427, #17303, #10988, #1343, #7575, #7766 ) ) ;
#5019=AXIS2_PLACEMENT_3D ( 'NONE', #2673, #5538, #17002 ) ;
#5022=ORIENTED_EDGE ( 'NONE', *, *, #7232, .F. ) ;
#5027=CARTESIAN_POINT ( 'NONE',  ( -0.03000000000000050196, 11.40000000000000036, 1.600000000000000089 ) ) ;
#5028=CIRCLE ( 'NONE', #317, 1.016666666666670160 ) ;
#5035=CARTESIAN_POINT ( 'NONE',  ( -1.599999999999880185, 11.40000000000000036, -2.399999999999999911 ) ) ;
#5036=FACE_OUTER_BOUND ( 'NONE', #6640, .T. ) ;
#5038=FACE_OUTER_BOUND ( 'NONE', #132, .T. ) ;
#5039=DIRECTION ( 'NONE',  ( -4.377285571048150598E-15, 1.000000000000000000, 0.000000000000000000 ) ) ;
#5042=DIRECTION ( 'NONE',  ( 1.000000000000000000, 0.000000000000000000, 0.000000000000000000 ) ) ;
#5044=CARTESIAN_POINT ( 'NONE',  ( 1.899999999999999911, 0.7500000000000000000, 7.649999999999999467 ) ) ;
#5054=EDGE_LOOP ( 'NONE', ( #2880, #1928, #10963, #11973 ) ) ;
#5055=EDGE_LOOP ( 'NONE', ( #11550, #10659, #7515, #6788 ) ) ;
#5062=DIRECTION ( 'NONE',  ( 1.000000000000000000, -1.059690869644410208E-14, 0.000000000000000000 ) ) ;
#5064=CARTESIAN_POINT ( 'NONE',  ( 0.02999999999999850009, 12.00000000000000000, 7.649999999999999467 ) ) ;
#5067=FACE_OUTER_BOUND ( 'NONE', #8819, .T. ) ;
#5070=CARTESIAN_POINT ( 'NONE',  ( 0.5372984490435490645, 4.599999999999999645, 7.700000000000000178 ) ) ;
#5073=LINE ( 'NONE', #11929, #13514 ) ;
#5079=ORIENTED_EDGE ( 'NONE', *, *, #7667, .F. ) ;
#5085=EDGE_CURVE ( 'NONE', #6674, #4421, #15150, .T. ) ;
#5110=ORIENTED_EDGE ( 'NONE', *, *, #13568, .F. ) ;
#5112=LINE ( 'NONE', #18132, #15622 ) ;
#5115=EDGE_CURVE ( 'NONE', #14832, #9752, #6893, .T. ) ;
#5126=ORIENTED_EDGE ( 'NONE', *, *, #17463, .F. ) ;
#5130=DIRECTION ( 'NONE',  ( -2.529805069132844337E-15, 1.000000000000000000, 1.807003620809174385E-16 ) ) ;
#5131=CARTESIAN_POINT ( 'NONE',  ( -2.500000000000000000, 5.551115123125779744E-16, -1.799976276337670169E-31 ) ) ;
#5134=DIRECTION ( 'NONE',  ( -1.000000000000000000, 2.891205793294678228E-15, 3.614007241618347587E-15 ) ) ;
#5136=ORIENTED_EDGE ( 'NONE', *, *, #5197, .T. ) ;
#5138=CYLINDRICAL_SURFACE ( 'NONE', #17375, 0.01000000000000002623 ) ;
#5142=LINE ( 'NONE', #17612, #1104 ) ;
#5146=ORIENTED_EDGE ( 'NONE', *, *, #4829, .T. ) ;
#5148=PLANE ( 'NONE',  #8518 ) ;
#5153=PLANE ( 'NONE',  #15959 ) ;
#5154=CARTESIAN_POINT ( 'NONE',  ( 1.208047591394629925E-13, 11.40000000000000036, -5.003920418925160367E-17 ) ) ;
#5158=DIRECTION ( 'NONE',  ( 2.220446049250309876E-16, 1.000000000000000000, -1.268826313857319964E-16 ) ) ;
#5172=DIRECTION ( 'NONE',  ( 0.000000000000000000, 1.359631073446889961E-32, -1.000000000000000000 ) ) ;
#5173=DIRECTION ( 'NONE',  ( 1.233581138472399909E-16, -5.135813185032649012E-32, 1.000000000000000000 ) ) ;
#5175=ORIENTED_EDGE ( 'NONE', *, *, #17723, .T. ) ;
#5188=DIRECTION ( 'NONE',  ( -0.000000000000000000, 1.000000000000000000, 0.000000000000000000 ) ) ;
#5197=EDGE_CURVE ( 'NONE', #6584, #2212, #2738, .T. ) ;
#5198=ORIENTED_EDGE ( 'NONE', *, *, #13042, .F. ) ;
#5204=AXIS2_PLACEMENT_3D ( 'NONE', #4243, #15744, #9815 ) ;
#5207=AXIS2_PLACEMENT_3D ( 'NONE', #3792, #14912, #14816 ) ;
#5211=CARTESIAN_POINT ( 'NONE',  ( 1.850000000000000089, 0.7500000000000000000, 8.300000000000000711 ) ) ;
#5212=DIRECTION ( 'NONE',  ( 0.000000000000000000, 3.548581835996780230E-45, -1.000000000000000000 ) ) ;
#5213=AXIS2_PLACEMENT_3D ( 'NONE', #13567, #9291, #4844 ) ;
#5217=EDGE_CURVE ( 'NONE', #18244, #13417, #14018, .T. ) ;
#5218=EDGE_LOOP ( 'NONE', ( #4491, #13445, #4189, #2909 ) ) ;
#5228=AXIS2_PLACEMENT_3D ( 'NONE', #2686, #1574, #4431 ) ;
#5231=DIRECTION ( 'NONE',  ( 1.823160359065819982E-16, 0.000000000000000000, -1.000000000000000000 ) ) ;
#5239=VECTOR ( 'NONE', #17161, 1000.000000000000000 ) ;
#5245=DIRECTION ( 'NONE',  ( 0.000000000000000000, 0.000000000000000000, -1.000000000000000000 ) ) ;
#5247=ORIENTED_EDGE ( 'NONE', *, *, #540, .T. ) ;
#5252=DIRECTION ( 'NONE',  ( 2.220446049250309876E-16, 1.000000000000000000, 0.000000000000000000 ) ) ;
#5254=DIRECTION ( 'NONE',  ( -1.224646799147341867E-16, -1.000000000000000000, 0.000000000000000000 ) ) ;
#5260=DIRECTION ( 'NONE',  ( 0.000000000000000000, 1.110223024625159992E-16, -1.000000000000000000 ) ) ;
#5264=CARTESIAN_POINT ( 'NONE',  ( -1.000000000000000000, 5.799999999999999822, 7.700000000000000178 ) ) ;
#5271=ORIENTED_EDGE ( 'NONE', *, *, #17952, .F. ) ;
#5274=FACE_OUTER_BOUND ( 'NONE', #12442, .T. ) ;
#5275=LINE ( 'NONE', #5455, #14735 ) ;
#5277=VECTOR ( 'NONE', #6291, 1000.000000000000000 ) ;
#5282=FACE_OUTER_BOUND ( 'NONE', #8334, .T. ) ;
#5285=VECTOR ( 'NONE', #515, 1000.000000000000000 ) ;
#5286=CYLINDRICAL_SURFACE ( 'NONE', #12606, 0.6000000000000000888 ) ;
#5287=VECTOR ( 'NONE', #7769, 1000.000000000000000 ) ;
#5289=DIRECTION ( 'NONE',  ( 3.315303352997239924E-31, -1.000000000000000000, 8.588360937600549480E-46 ) ) ;
#5304=LINE ( 'NONE', #951, #14705 ) ;
#5308=ADVANCED_FACE ( 'NONE', ( #12734 ), #9947, .F. ) ;
#5312=EDGE_CURVE ( 'NONE', #4421, #2415, #16976, .T. ) ;
#5330=DIRECTION ( 'NONE',  ( 1.000000000000000000, 0.000000000000000000, -7.401486830834370362E-16 ) ) ;
#5332=DIRECTION ( 'NONE',  ( 0.000000000000000000, 0.000000000000000000, -1.000000000000000000 ) ) ;
#5336=EDGE_LOOP ( 'NONE', ( #10609, #14089, #7080, #13092 ) ) ;
#5337=DIRECTION ( 'NONE',  ( 0.000000000000000000, 0.000000000000000000, 1.000000000000000000 ) ) ;
#5345=CARTESIAN_POINT ( 'NONE',  ( 1.889999999999999902, 3.500000000000000000, 0.5999999999999999778 ) ) ;
#5348=ORIENTED_EDGE ( 'NONE', *, *, #7667, .T. ) ;
#5357=DIRECTION ( 'NONE',  ( 6.162975822039159109E-32, 1.000000000000000000, 1.110223024625159992E-16 ) ) ;
#5358=ORIENTED_EDGE ( 'NONE', *, *, #7772, .T. ) ;
#5360=CARTESIAN_POINT ( 'NONE',  ( -0.7999999999998790301, 11.40000000000000036, -9.797174393178840942E-17 ) ) ;
#5363=DIRECTION ( 'NONE',  ( 7.401486830834370362E-16, 0.000000000000000000, 1.000000000000000000 ) ) ;
#5366=ORIENTED_EDGE ( 'NONE', *, *, #8711, .F. ) ;
#5380=LINE ( 'NONE', #16669, #6974 ) ;
#5382=DIRECTION ( 'NONE',  ( -1.000000000000000000, 0.000000000000000000, -2.843808977011158816E-15 ) ) ;
#5390=DIRECTION ( 'NONE',  ( 0.000000000000000000, 1.000000000000000000, 0.000000000000000000 ) ) ;
#5393=PLANE ( 'NONE',  #6988 ) ;
#5409=VERTEX_POINT ( 'NONE', #18202 ) ;
#5410=EDGE_CURVE ( 'NONE', #2252, #2787, #12061, .T. ) ;
#5415=EDGE_CURVE ( 'NONE', #3830, #6319, #14525, .T. ) ;
#5416=LINE ( 'NONE', #16892, #1372 ) ;
#5421=EDGE_CURVE ( 'NONE', #7849, #8434, #7759, .T. ) ;
#5423=ORIENTED_EDGE ( 'NONE', *, *, #16756, .F. ) ;
#5424=DIRECTION ( 'NONE',  ( 0.000000000000000000, 4.485749594445070317E-16, 1.000000000000000000 ) ) ;
#5433=FACE_OUTER_BOUND ( 'NONE', #5906, .T. ) ;
#5435=VERTEX_POINT ( 'NONE', #12018 ) ;
#5439=ADVANCED_FACE ( 'NONE', ( #9954 ), #6457, .F. ) ;
#5440=DIRECTION ( 'NONE',  ( 6.083413833562510128E-16, -1.647588903766454767E-16, 1.000000000000000000 ) ) ;
#5443=ORIENTED_EDGE ( 'NONE', *, *, #15088, .F. ) ;
#5445=AXIS2_PLACEMENT_3D ( 'NONE', #3322, #8966, #2019 ) ;
#5451=ORIENTED_EDGE ( 'NONE', *, *, #15168, .F. ) ;
#5455=CARTESIAN_POINT ( 'NONE',  ( -2.500000000000000000, 0.4000000000000000222, 7.649999999999999467 ) ) ;
#5456=VERTEX_POINT ( 'NONE', #8003 ) ;
#5462=DIRECTION ( 'NONE',  ( -1.000000000000000000, 0.000000000000000000, 7.401486830834370362E-16 ) ) ;
#5465=CARTESIAN_POINT ( 'NONE',  ( 1.000000000000000000, 5.799999999999999822, 7.700000000000000178 ) ) ;
#5468=CARTESIAN_POINT ( 'NONE',  ( 1.399999999999999911, 5.799999999999999822, 7.700000000000000178 ) ) ;
#5470=CARTESIAN_POINT ( 'NONE',  ( 1.000000000000000000, 6.400000000000000355, 8.300000000000000711 ) ) ;
#5474=VERTEX_POINT ( 'NONE', #7621 ) ;
#5480=FACE_OUTER_BOUND ( 'NONE', #13735, .T. ) ;
#5482=CARTESIAN_POINT ( 'NONE',  ( 2.500000000000000000, 10.00000000000000000, -1.110223024625159893E-15 ) ) ;
#5486=ORIENTED_EDGE ( 'NONE', *, *, #12230, .T. ) ;
#5489=ORIENTED_EDGE ( 'NONE', *, *, #5518, .T. ) ;
#5495=ORIENTED_EDGE ( 'NONE', *, *, #9585, .F. ) ;
#5503=DIRECTION ( 'NONE',  ( 1.000000000000000000, 0.000000000000000000, -6.049014748177260544E-16 ) ) ;
#5504=AXIS2_PLACEMENT_3D ( 'NONE', #1102, #18023, #18107 ) ;
#5509=VECTOR ( 'NONE', #9296, 1000.000000000000000 ) ;
#5515=VERTEX_POINT ( 'NONE', #11231 ) ;
#5518=EDGE_CURVE ( 'NONE', #11846, #9094, #2626, .T. ) ;
#5519=DIRECTION ( 'NONE',  ( 4.485749594445070317E-16, 0.000000000000000000, 1.000000000000000000 ) ) ;
#5520=DIRECTION ( 'NONE',  ( -1.000000000000000000, 1.224646799147341128E-16, 0.000000000000000000 ) ) ;
#5522=ORIENTED_EDGE ( 'NONE', *, *, #11147, .T. ) ;
#5527=CYLINDRICAL_SURFACE ( 'NONE', #13491, 0.4166666666666670737 ) ;
#5534=CARTESIAN_POINT ( 'NONE',  ( -2.500000000000000000, 3.500000000000000000, 0.6099999999999999867 ) ) ;
#5537=CARTESIAN_POINT ( 'NONE',  ( -1.889999999999999902, 7.900000000000000355, 2.126957699879220439E-15 ) ) ;
#5538=DIRECTION ( 'NONE',  ( 0.000000000000000000, 0.000000000000000000, -1.000000000000000000 ) ) ;
#5540=ORIENTED_EDGE ( 'NONE', *, *, #7049, .F. ) ;
#5541=EDGE_CURVE ( 'NONE', #16962, #410, #7076, .T. ) ;
#5544=EDGE_LOOP ( 'NONE', ( #3326, #924, #17544, #10702 ) ) ;
#5547=CARTESIAN_POINT ( 'NONE',  ( -1.889999999999999902, 7.299999999999999822, 1.321762070856419966E-15 ) ) ;
#5549=ORIENTED_EDGE ( 'NONE', *, *, #7534, .T. ) ;
#5551=VECTOR ( 'NONE', #6303, 1000.000000000000000 ) ;
#5554=CARTESIAN_POINT ( 'NONE',  ( -0.8740908734716290596, 4.154758922476410099, 8.300000000000000711 ) ) ;
#5555=CARTESIAN_POINT ( 'NONE',  ( 1.889999999999999902, 4.700000000000000178, 0.6099999999999999867 ) ) ;
#5558=VECTOR ( 'NONE', #18007, 1000.000000000000000 ) ;
#5566=AXIS2_PLACEMENT_3D ( 'NONE', #4068, #13627, #15392 ) ;
#5570=AXIS2_PLACEMENT_3D ( 'NONE', #15438, #18159, #6814 ) ;
#5573=CIRCLE ( 'NONE', #15045, 0.6100000000000000977 ) ;
#5577=CARTESIAN_POINT ( 'NONE',  ( -2.500000000000000000, 0.7500000000000000000, 7.649999999999999467 ) ) ;
#5586=DIRECTION ( 'NONE',  ( -1.000000000000000000, -4.014365738757630620E-15, -1.254489293361759815E-16 ) ) ;
#5590=ADVANCED_FACE ( 'NONE', ( #7427 ), #119, .F. ) ;
#5592=ORIENTED_EDGE ( 'NONE', *, *, #11971, .T. ) ;
#5595=ORIENTED_EDGE ( 'NONE', *, *, #13568, .T. ) ;
#5602=EDGE_LOOP ( 'NONE', ( #11424, #948, #9260, #17946 ) ) ;
#5610=CARTESIAN_POINT ( 'NONE',  ( -2.616666666666669805, -4.318079751576579732E-16, 4.000000000000000000 ) ) ;
#5615=ORIENTED_EDGE ( 'NONE', *, *, #5421, .F. ) ;
#5618=ORIENTED_EDGE ( 'NONE', *, *, #6937, .T. ) ;
#5622=CARTESIAN_POINT ( 'NONE',  ( -1.889999999999999902, 7.299999999999999822, 0.6099999999999999867 ) ) ;
#5623=ORIENTED_EDGE ( 'NONE', *, *, #4045, .F. ) ;
#5626=LINE ( 'NONE', #11269, #13827 ) ;
#5628=EDGE_CURVE ( 'NONE', #5515, #6950, #15897, .T. ) ;
#5629=ORIENTED_EDGE ( 'NONE', *, *, #4986, .F. ) ;
#5632=DIRECTION ( 'NONE',  ( 1.850371707708589879E-16, 0.000000000000000000, -1.000000000000000000 ) ) ;
#5636=LINE ( 'NONE', #15648, #16273 ) ;
#5639=ORIENTED_EDGE ( 'NONE', *, *, #5918, .T. ) ;
#5642=ORIENTED_EDGE ( 'NONE', *, *, #18149, .F. ) ;
#5651=CARTESIAN_POINT ( 'NONE',  ( 1.889999999999999902, 8.500000000000000000, 1.696109213374460111E-16 ) ) ;
#5657=DIRECTION ( 'NONE',  ( 0.000000000000000000, 0.000000000000000000, 1.000000000000000000 ) ) ;
#5661=ORIENTED_EDGE ( 'NONE', *, *, #10723, .F. ) ;
#5662=FACE_OUTER_BOUND ( 'NONE', #15465, .T. ) ;
#5664=ORIENTED_EDGE ( 'NONE', *, *, #4590, .F. ) ;
#5665=DIRECTION ( 'NONE',  ( 0.000000000000000000, 0.000000000000000000, 1.000000000000000000 ) ) ;
#5672=CARTESIAN_POINT ( 'NONE',  ( -2.616666666666669805, -4.318079751576579732E-16, 4.000000000000000000 ) ) ;
#5680=PLANE ( 'NONE',  #13280 ) ;
#5684=VERTEX_POINT ( 'NONE', #17212 ) ;
#5685=VERTEX_POINT ( 'NONE', #13153 ) ;
#5696=EDGE_CURVE ( 'NONE', #5685, #4195, #11409, .T. ) ;
#5698=PLANE ( 'NONE',  #867 ) ;
#5708=EDGE_LOOP ( 'NONE', ( #2495, #6723, #1540, #13155 ) ) ;
#5710=DIRECTION ( 'NONE',  ( -1.110223024625160090E-15, -1.000000000000000000, 0.000000000000000000 ) ) ;
#5711=CARTESIAN_POINT ( 'NONE',  ( -1.000000000000000000, 5.400000000000000355, 8.300000000000000711 ) ) ;
#5715=CYLINDRICAL_SURFACE ( 'NONE', #5840, 0.4000000000000001887 ) ;
#5718=ORIENTED_EDGE ( 'NONE', *, *, #16364, .T. ) ;
#5719=LINE ( 'NONE', #5360, #8539 ) ;
#5725=ORIENTED_EDGE ( 'NONE', *, *, #7772, .F. ) ;
#5727=PLANE ( 'NONE',  #7424 ) ;
#5728=CYLINDRICAL_SURFACE ( 'NONE', #16526, 0.7000000000000000666 ) ;
#5731=EDGE_CURVE ( 'NONE', #6864, #7679, #13833, .T. ) ;
#5733=SURFACE_STYLE_FILL_AREA ( #87 ) ;
#5743=ORIENTED_EDGE ( 'NONE', *, *, #10841, .F. ) ;
#5748=EDGE_LOOP ( 'NONE', ( #101, #3135, #17789, #8554 ) ) ;
#5749=LINE ( 'NONE', #7155, #17663 ) ;
#5751=ORIENTED_EDGE ( 'NONE', *, *, #5731, .T. ) ;
#5753=EDGE_CURVE ( 'NONE', #8619, #9205, #6736, .T. ) ;
#5757=DIRECTION ( 'NONE',  ( 0.000000000000000000, 0.000000000000000000, -1.000000000000000000 ) ) ;
#5768=ORIENTED_EDGE ( 'NONE', *, *, #4038, .T. ) ;
#5769=EDGE_CURVE ( 'NONE', #16414, #17164, #6112, .T. ) ;
#5772=EDGE_LOOP ( 'NONE', ( #12046, #14211, #7034, #9793, #8949, #8943 ) ) ;
#5781=VERTEX_POINT ( 'NONE', #843 ) ;
#5782=DIRECTION ( 'NONE',  ( 1.000000000000000000, 0.000000000000000000, -7.273661547324610053E-16 ) ) ;
#5792=AXIS2_PLACEMENT_3D ( 'NONE', #9744, #11223, #12605 ) ;
#5795=ORIENTED_EDGE ( 'NONE', *, *, #7900, .T. ) ;
#5796=LINE ( 'NONE', #11440, #17335 ) ;
#5798=CARTESIAN_POINT ( 'NONE',  ( 1.800000000000000044, 11.40000000000000036, 7.649999999999999467 ) ) ;
#5802=DIRECTION ( 'NONE',  ( 1.480297366166869931E-15, 1.000000000000000000, -1.314768175368350090E-30 ) ) ;
#5807=CARTESIAN_POINT ( 'NONE',  ( -2.500000000000000000, 10.00000000000000000, 5.075305255429290705E-16 ) ) ;
#5810=ORIENTED_EDGE ( 'NONE', *, *, #10528, .F. ) ;
#5811=CARTESIAN_POINT ( 'NONE',  ( 1.889999999999999902, 8.500000000000000000, 0.5999999999999999778 ) ) ;
#5812=DIRECTION ( 'NONE',  ( 0.000000000000000000, 1.000000000000000000, -1.110223024625159745E-16 ) ) ;
#5825=VECTOR ( 'NONE', #9882, 1000.000000000000000 ) ;
#5826=LINE ( 'NONE', #6005, #4967 ) ;
#5833=CIRCLE ( 'NONE', #1702, 1.016666666666670160 ) ;
#5838=VECTOR ( 'NONE', #7920, 1000.000000000000000 ) ;
#5840=AXIS2_PLACEMENT_3D ( 'NONE', #3022, #1897, #14581 ) ;
#5842=DIRECTION ( 'NONE',  ( -1.000000000000000000, 0.000000000000000000, 7.401486830834370362E-16 ) ) ;
#5858=AXIS2_PLACEMENT_3D ( 'NONE', #16538, #10598, #3846 ) ;
#5862=ORIENTED_EDGE ( 'NONE', *, *, #2122, .T. ) ;
#5873=DIRECTION ( 'NONE',  ( 0.000000000000000000, 1.000000000000000000, 1.295260195396020040E-15 ) ) ;
#5880=DIRECTION ( 'NONE',  ( -1.224646799147341867E-16, -1.000000000000000000, 0.000000000000000000 ) ) ;
#5892=LINE ( 'NONE', #5798, #13536 ) ;
#5899=AXIS2_PLACEMENT_3D ( 'NONE', #6708, #12365, #2739 ) ;
#5903=CARTESIAN_POINT ( 'NONE',  ( -1.000000000000000000, 5.400000000000000355, 7.700000000000000178 ) ) ;
#5905=ORIENTED_EDGE ( 'NONE', *, *, #10853, .T. ) ;
#5906=EDGE_LOOP ( 'NONE', ( #6619, #6176, #9363, #12869 ) ) ;
#5907=LINE ( 'NONE', #10236, #8605 ) ;
#5917=LINE ( 'NONE', #363, #8489 ) ;
#5918=EDGE_CURVE ( 'NONE', #8572, #14730, #13336, .T. ) ;
#5926=ORIENTED_EDGE ( 'NONE', *, *, #11294, .T. ) ;
#5948=ORIENTED_EDGE ( 'NONE', *, *, #10412, .T. ) ;
#5955=FACE_OUTER_BOUND ( 'NONE', #13234, .T. ) ;
#5962=ORIENTED_EDGE ( 'NONE', *, *, #6088, .F. ) ;
#5971=EDGE_CURVE ( 'NONE', #9567, #5409, #12324, .T. ) ;
#5973=VERTEX_POINT ( 'NONE', #13894 ) ;
#5978=ADVANCED_FACE ( 'NONE', ( #17943 ), #1029, .T. ) ;
#5983=CARTESIAN_POINT ( 'NONE',  ( 0.5291502622129179434, 0.1000000000000000056, 7.700000000000000178 ) ) ;
#5985=AXIS2_PLACEMENT_3D ( 'NONE', #16537, #15342, #8112 ) ;
#5986=VECTOR ( 'NONE', #1160, 1000.000000000000000 ) ;
#5988=DIRECTION ( 'NONE',  ( 1.000000000000000000, -1.224646799147350002E-16, 0.000000000000000000 ) ) ;
#5989=CARTESIAN_POINT ( 'NONE',  ( -1.889999999999999902, 7.900000000000000355, 0.5999999999999999778 ) ) ;
#5991=VERTEX_POINT ( 'NONE', #13977 ) ;
#5992=ORIENTED_EDGE ( 'NONE', *, *, #15088, .T. ) ;
#5993=PLANE ( 'NONE',  #15117 ) ;
#5996=EDGE_LOOP ( 'NONE', ( #437, #17057, #17511, #12351 ) ) ;
#6001=DIRECTION ( 'NONE',  ( -1.000000000000000000, 1.153478467143200106E-14, -8.997169018144999103E-17 ) ) ;
#6005=CARTESIAN_POINT ( 'NONE',  ( 1.899999999999999911, 11.15000000000000036, -3.616154994493369454E-16 ) ) ;
#6008=VERTEX_POINT ( 'NONE', #16483 ) ;
#6010=CARTESIAN_POINT ( 'NONE',  ( -1.875000000000000000, 11.25000000000000000, 7.700000000000000178 ) ) ;
#6012=DIRECTION ( 'NONE',  ( -3.700743415417179758E-16, -1.000000000000000000, -1.665334536937730077E-15 ) ) ;
#6013=CARTESIAN_POINT ( 'NONE',  ( -1.289999999999999813, 7.900000000000014566, 4.318333862165718414E-15 ) ) ;
#6014=EDGE_CURVE ( 'NONE', #14398, #1432, #8157, .T. ) ;
#6034=ORIENTED_EDGE ( 'NONE', *, *, #17646, .F. ) ;
#6035=DIRECTION ( 'NONE',  ( -6.049014748177260544E-16, 2.493473113004675144E-16, -1.000000000000000000 ) ) ;
#6050=DIRECTION ( 'NONE',  ( -1.000000000000000000, 1.668003342285391304E-16, 0.000000000000000000 ) ) ;
#6051=EDGE_LOOP ( 'NONE', ( #2060, #5443, #2855, #591 ) ) ;
#6059=LINE ( 'NONE', #3291, #1635 ) ;
#6062=FACE_OUTER_BOUND ( 'NONE', #1193, .T. ) ;
#6065=VECTOR ( 'NONE', #11035, 1000.000000000000000 ) ;
#6066=EDGE_CURVE ( 'NONE', #4195, #8282, #8529, .T. ) ;
#6072=EDGE_CURVE ( 'NONE', #4501, #18124, #9455, .T. ) ;
#6073=DIRECTION ( 'NONE',  ( 0.000000000000000000, 1.000000000000000000, 0.000000000000000000 ) ) ;
#6080=ORIENTED_EDGE ( 'NONE', *, *, #12799, .T. ) ;
#6081=CARTESIAN_POINT ( 'NONE',  ( 1.899999999999999911, 11.29999999999999893, 7.649999999999999467 ) ) ;
#6085=VECTOR ( 'NONE', #10933, 1000.000000000000000 ) ;
#6088=EDGE_CURVE ( 'NONE', #7297, #14593, #7353, .T. ) ;
#6090=CARTESIAN_POINT ( 'NONE',  ( 1.889999999999999902, 7.299999999999999822, 0.6099999999999999867 ) ) ;
#6092=EDGE_CURVE ( 'NONE', #3526, #17345, #11173, .T. ) ;
#6093=PLANE ( 'NONE',  #7680 ) ;
#6102=PLANE ( 'NONE',  #14409 ) ;
#6112=LINE ( 'NONE', #9060, #12355 ) ;
#6114=AXIS2_PLACEMENT_3D ( 'NONE', #13032, #7656, #3383 ) ;
#6122=AXIS2_PLACEMENT_3D ( 'NONE', #16534, #3842, #9198 ) ;
#6128=CARTESIAN_POINT ( 'NONE',  ( -1.875000000000000000, 2.296212748401290437E-16, 7.700000000000000178 ) ) ;
#6131=ORIENTED_EDGE ( 'NONE', *, *, #18056, .F. ) ;
#6133=EDGE_CURVE ( 'NONE', #1501, #17047, #2915, .T. ) ;
#6134=DIRECTION ( 'NONE',  ( 3.861645303044030038E-16, 1.000000000000000000, 1.268826313857319964E-16 ) ) ;
#6141=EDGE_LOOP ( 'NONE', ( #10578, #8582, #7132, #10372 ) ) ;
#6144=DIRECTION ( 'NONE',  ( -8.971499188890128802E-16, 4.485749594445070317E-16, -1.000000000000000000 ) ) ;
#6151=AXIS2_PLACEMENT_3D ( 'NONE', #10462, #9069, #5012 ) ;
#6153=DIRECTION ( 'NONE',  ( 4.440892098500620245E-16, -3.700743415417219694E-16, 1.000000000000000000 ) ) ;
#6154=CARTESIAN_POINT ( 'NONE',  ( -0.02999999999999400022, 12.00000000000000000, 7.649999999999999467 ) ) ;
#6155=VECTOR ( 'NONE', #12932, 1000.000000000000000 ) ;
#6158=AXIS2_PLACEMENT_3D ( 'NONE', #2110, #4977, #4876 ) ;
#6160=DIRECTION ( 'NONE',  ( 0.000000000000000000, -1.000000000000000000, -1.586032892321649771E-16 ) ) ;
#6165=ORIENTED_EDGE ( 'NONE', *, *, #11335, .T. ) ;
#6169=EDGE_CURVE ( 'NONE', #5684, #9295, #5826, .T. ) ;
#6171=VERTEX_POINT ( 'NONE', #10003 ) ;
#6173=CARTESIAN_POINT ( 'NONE',  ( 2.500000000000000000, 9.199999999999999289, 0.6099999999999999867 ) ) ;
#6175=DIRECTION ( 'NONE',  ( -6.049014748177260544E-16, 0.000000000000000000, -1.000000000000000000 ) ) ;
#6176=ORIENTED_EDGE ( 'NONE', *, *, #9764, .T. ) ;
#6178=EDGE_CURVE ( 'NONE', #16414, #18253, #1580, .T. ) ;
#6180=DIRECTION ( 'NONE',  ( 0.000000000000000000, 0.000000000000000000, 1.000000000000000000 ) ) ;
#6181=DIRECTION ( 'NONE',  ( 0.000000000000000000, 0.000000000000000000, 1.000000000000000000 ) ) ;
#6182=ADVANCED_FACE ( 'NONE', ( #2874 ), #10169, .F. ) ;
#6186=CIRCLE ( 'NONE', #16549, 0.1000000000000000472 ) ;
#6187=FACE_BOUND ( 'NONE', #10442, .T. ) ;
#6194=CARTESIAN_POINT ( 'NONE',  ( -1.875000000000000000, 0.7500000000000000000, 7.700000000000000178 ) ) ;
#6197=VECTOR ( 'NONE', #9039, 1000.000000000000000 ) ;
#6201=DIRECTION ( 'NONE',  ( -1.000000000000000000, 6.437450399132682577E-16, 0.000000000000000000 ) ) ;
#6211=ORIENTED_EDGE ( 'NONE', *, *, #3226, .T. ) ;
#6215=LINE ( 'NONE', #2045, #2921 ) ;
#6216=EDGE_CURVE ( 'NONE', #4195, #2455, #10255, .T. ) ;
#6217=ORIENTED_EDGE ( 'NONE', *, *, #10146, .T. ) ;
#6218=DIRECTION ( 'NONE',  ( -7.401486830834380223E-16, -1.000000000000000000, 1.110223024625159992E-16 ) ) ;
#6220=EDGE_CURVE ( 'NONE', #5991, #10145, #8697, .T. ) ;
#6227=ORIENTED_EDGE ( 'NONE', *, *, #3392, .T. ) ;
#6228=EDGE_CURVE ( 'NONE', #6669, #6864, #14174, .T. ) ;
#6236=EDGE_CURVE ( 'NONE', #12277, #9534, #7310, .T. ) ;
#6237=ORIENTED_EDGE ( 'NONE', *, *, #1890, .T. ) ;
#6242=LINE ( 'NONE', #974, #12054 ) ;
#6244=VERTEX_POINT ( 'NONE', #12694 ) ;
#6251=DIRECTION ( 'NONE',  ( 1.445602896647339508E-15, -1.000000000000000000, -1.264902534566422168E-15 ) ) ;
#6256=DIRECTION ( 'NONE',  ( 1.000000000000000000, -2.220446049250309876E-16, -6.123233995736769734E-17 ) ) ;
#6258=ORIENTED_EDGE ( 'NONE', *, *, #16171, .T. ) ;
#6260=LINE ( 'NONE', #10805, #829 ) ;
#6267=DIRECTION ( 'NONE',  ( -1.000000000000000000, 0.000000000000000000, 0.000000000000000000 ) ) ;
#6271=DIRECTION ( 'NONE',  ( 6.123233995736769734E-17, 2.493473113004670213E-16, 1.000000000000000000 ) ) ;
#6277=DIRECTION ( 'NONE',  ( 1.807003620809174583E-15, 1.000000000000000000, 1.807003620809174385E-16 ) ) ;
#6279=VECTOR ( 'NONE', #10208, 1000.000000000000000 ) ;
#6286=ADVANCED_FACE ( 'NONE', ( #4338 ), #15922, .T. ) ;
#6291=DIRECTION ( 'NONE',  ( -1.000000000000000000, 1.776356839399180454E-14, 0.000000000000000000 ) ) ;
#6302=VECTOR ( 'NONE', #13292, 1000.000000000000000 ) ;
#6303=DIRECTION ( 'NONE',  ( -1.000000000000000000, 0.000000000000000000, 7.273661547324610053E-16 ) ) ;
#6305=ORIENTED_EDGE ( 'NONE', *, *, #2237, .T. ) ;
#6309=EDGE_LOOP ( 'NONE', ( #666, #10664, #4581, #11281 ) ) ;
#6311=EDGE_CURVE ( 'NONE', #3727, #12747, #13528, .T. ) ;
#6315=DIRECTION ( 'NONE',  ( 1.000000000000000000, -1.480297366166879989E-15, 0.000000000000000000 ) ) ;
#6319=VERTEX_POINT ( 'NONE', #11951 ) ;
#6325=DIRECTION ( 'NONE',  ( 0.000000000000000000, -1.000000000000000000, -1.359631073446889961E-32 ) ) ;
#6327=ORIENTED_EDGE ( 'NONE', *, *, #1673, .T. ) ;
#6334=FACE_OUTER_BOUND ( 'NONE', #17770, .T. ) ;
#6337=ORIENTED_EDGE ( 'NONE', *, *, #11074, .F. ) ;
#6340=DIRECTION ( 'NONE',  ( 1.000000000000000000, -2.220446049250309876E-16, -7.273661547324610053E-16 ) ) ;
#6344=DIRECTION ( 'NONE',  ( -6.123233995736769734E-17, 2.611996170812411923E-32, -1.000000000000000000 ) ) ;
#6346=CARTESIAN_POINT ( 'NONE',  ( 1.000000000000002220, 9.099999999999999645, 7.700000000000000178 ) ) ;
#6353=EDGE_CURVE ( 'NONE', #3882, #6244, #16305, .T. ) ;
#6355=DIRECTION ( 'NONE',  ( 0.000000000000000000, 0.000000000000000000, 1.000000000000000000 ) ) ;
#6357=LINE ( 'NONE', #16285, #17131 ) ;
#6359=ORIENTED_EDGE ( 'NONE', *, *, #3604, .F. ) ;
#6365=ORIENTED_EDGE ( 'NONE', *, *, #7277, .T. ) ;
#6368=FACE_OUTER_BOUND ( 'NONE', #3644, .T. ) ;
#6377=CARTESIAN_POINT ( 'NONE',  ( -2.500000000000000000, 11.29999999999999893, 7.649999999999999467 ) ) ;
#6384=ORIENTED_EDGE ( 'NONE', *, *, #5971, .T. ) ;
#6401=ORIENTED_EDGE ( 'NONE', *, *, #11854, .F. ) ;
#6415=VECTOR ( 'NONE', #9315, 1000.000000000000000 ) ;
#6416=DIRECTION ( 'NONE',  ( 5.103860808646520231E-18, -6.123233995736769734E-17, -1.000000000000000000 ) ) ;
#6422=EDGE_LOOP ( 'NONE', ( #6131, #4771, #7735, #13474 ) ) ;
#6423=FACE_OUTER_BOUND ( 'NONE', #7467, .T. ) ;
#6425=VECTOR ( 'NONE', #719, 1000.000000000000000 ) ;
#6431=DIRECTION ( 'NONE',  ( 0.000000000000000000, 0.000000000000000000, 1.000000000000000000 ) ) ;
#6438=FACE_OUTER_BOUND ( 'NONE', #11881, .T. ) ;
#6446=DIRECTION ( 'NONE',  ( 1.059690869644410208E-14, 1.000000000000000000, -1.041146930477340028E-32 ) ) ;
#6450=CARTESIAN_POINT ( 'NONE',  ( -2.500000000000000000, 4.700000000000000178, 1.600000000000000089 ) ) ;
#6453=AXIS2_PLACEMENT_3D ( 'NONE', #13362, #4748, #13274 ) ;
#6454=PLANE ( 'NONE',  #16230 ) ;
#6457=PLANE ( 'NONE',  #7615 ) ;
#6458=DIRECTION ( 'NONE',  ( 0.000000000000000000, 0.000000000000000000, 1.000000000000000000 ) ) ;
#6467=EDGE_CURVE ( 'NONE', #11652, #15772, #11438, .T. ) ;
#6468=CARTESIAN_POINT ( 'NONE',  ( -1.889999999999999902, 4.100000000000000533, -6.851683986394989688E-16 ) ) ;
#6470=DIRECTION ( 'NONE',  ( 0.2721173643531200059, -0.9622640697945191723, 0.000000000000000000 ) ) ;
#6471=DIRECTION ( 'NONE',  ( 0.000000000000000000, 0.000000000000000000, -1.000000000000000000 ) ) ;
#6483=CARTESIAN_POINT ( 'NONE',  ( 2.616666666666660035, 8.899094389694600942E-17, 4.000000000000000000 ) ) ;
#6492=CARTESIAN_POINT ( 'NONE',  ( -1.899999999999999911, 2.000000000000000000, 2.388061258337340122E-16 ) ) ;
#6494=LINE ( 'NONE', #17772, #16599 ) ;
#6498=FACE_OUTER_BOUND ( 'NONE', #330, .T. ) ;
#6499=EDGE_LOOP ( 'NONE', ( #5718, #7029, #16325, #4903, #7440, #8677, #9151, #17926, #7531, #5618, #3524, #3418, #6946, #12329, #16991, #14478 ) ) ;
#6501=CARTESIAN_POINT ( 'NONE',  ( 1.000000000000000000, 5.400000000000000355, 8.300000000000000711 ) ) ;
#6506=ORIENTED_EDGE ( 'NONE', *, *, #11612, .T. ) ;
#6508=ORIENTED_EDGE ( 'NONE', *, *, #782, .F. ) ;
#6512=AXIS2_PLACEMENT_3D ( 'NONE', #15530, #2831, #8478 ) ;
#6516=DIRECTION ( 'NONE',  ( -3.700743415417180054E-15, -1.000000000000000000, -1.850371707708589879E-16 ) ) ;
#6522=CARTESIAN_POINT ( 'NONE',  ( -2.500000000000000000, 1.071484571201660082E-16, 3.600000000000000089 ) ) ;
#6530=EDGE_CURVE ( 'NONE', #17179, #7642, #12372, .T. ) ;
#6533=VERTEX_POINT ( 'NONE', #8506 ) ;
#6538=ORIENTED_EDGE ( 'NONE', *, *, #1464, .F. ) ;
#6547=CYLINDRICAL_SURFACE ( 'NONE', #14470, 0.04999999999999969746 ) ;
#6549=DIRECTION ( 'NONE',  ( 1.000000000000000000, -1.059690869644410208E-14, 0.000000000000000000 ) ) ;
#6556=CARTESIAN_POINT ( 'NONE',  ( 1.899999999999999911, 8.500000000000000000, 0.6099999999999999867 ) ) ;
#6566=DIRECTION ( 'NONE',  ( -6.239269890455420182E-16, 5.872254014546280719E-16, -1.000000000000000000 ) ) ;
#6567=CYLINDRICAL_SURFACE ( 'NONE', #6765, 0.6000000000000000888 ) ;
#6568=VERTEX_POINT ( 'NONE', #15813 ) ;
#6572=DIRECTION ( 'NONE',  ( 6.123233995736769734E-17, 0.000000000000000000, 1.000000000000000000 ) ) ;
#6578=ORIENTED_EDGE ( 'NONE', *, *, #2845, .T. ) ;
#6580=EDGE_CURVE ( 'NONE', #16962, #7679, #3041, .T. ) ;
#6584=VERTEX_POINT ( 'NONE', #5547 ) ;
#6585=UNCERTAINTY_MEASURE_WITH_UNIT (LENGTH_MEASURE( 1.000000000000000082E-05 ), #12259, 'distance_accuracy_value', 'NONE');
#6587=CARTESIAN_POINT ( 'NONE',  ( 1.399999999999999911, 5.799999999999999822, 7.700000000000000178 ) ) ;
#6589=DIRECTION ( 'NONE',  ( 1.445602896647339508E-15, 1.000000000000000000, 1.332267629550190412E-15 ) ) ;
#6609=LINE ( 'NONE', #5131, #7886 ) ;
#6614=ORIENTED_EDGE ( 'NONE', *, *, #9737, .F. ) ;
#6615=DIRECTION ( 'NONE',  ( 0.000000000000000000, 0.000000000000000000, 1.000000000000000000 ) ) ;
#6616=CARTESIAN_POINT ( 'NONE',  ( -1.399999999999999911, 6.400000000000000355, 7.700000000000000178 ) ) ;
#6619=ORIENTED_EDGE ( 'NONE', *, *, #17391, .T. ) ;
#6623=ORIENTED_EDGE ( 'NONE', *, *, #540, .F. ) ;
#6624=EDGE_LOOP ( 'NONE', ( #13541, #17238, #14907, #5486 ) ) ;
#6625=DIRECTION ( 'NONE',  ( 1.000000000000000000, 5.782411586589356455E-15, 3.614007241618347587E-15 ) ) ;
#6640=EDGE_LOOP ( 'NONE', ( #2984, #12102, #3717, #4931 ) ) ;
#6643=FACE_OUTER_BOUND ( 'NONE', #673, .T. ) ;
#6650=DIRECTION ( 'NONE',  ( -2.986159789035700404E-15, 1.110223024625159992E-16, 1.000000000000000000 ) ) ;
#6653=DIRECTION ( 'NONE',  ( -7.401486830834380223E-16, -1.769136588914770194E-30, 1.000000000000000000 ) ) ;
#6657=EDGE_CURVE ( 'NONE', #1091, #12787, #16162, .T. ) ;
#6659=CYLINDRICAL_SURFACE ( 'NONE', #7751, 0.04999999999999969746 ) ;
#6661=FACE_OUTER_BOUND ( 'NONE', #15607, .T. ) ;
#6663=EDGE_CURVE ( 'NONE', #6008, #14845, #11450, .T. ) ;
#6668=CARTESIAN_POINT ( 'NONE',  ( -1.599999999999869971, 12.00000000000000000, 1.600000000000000089 ) ) ;
#6669=VERTEX_POINT ( 'NONE', #8867 ) ;
#6674=VERTEX_POINT ( 'NONE', #14779 ) ;
#6675=ORIENTED_EDGE ( 'NONE', *, *, #3008, .T. ) ;
#6683=ADVANCED_FACE ( 'NONE', ( #11916 ), #16007, .T. ) ;
#6684=LINE ( 'NONE', #5482, #12043 ) ;
#6693=PLANE ( 'NONE',  #538 ) ;
#6700=CARTESIAN_POINT ( 'NONE',  ( -0.02999999999999379899, 12.00000000000000000, -2.869354249208270301E-17 ) ) ;
#6701=ADVANCED_FACE ( 'NONE', ( #10425 ), #355, .T. ) ;
#6703=AXIS2_PLACEMENT_3D ( 'NONE', #15292, #2604, #16753 ) ;
#6708=CARTESIAN_POINT ( 'NONE',  ( -1.199999999999869837, 12.00000000000000000, -2.399999999999999911 ) ) ;
#6710=CARTESIAN_POINT ( 'NONE',  ( -2.500000000000000000, 2.799999999999999822, 0.6099999999999999867 ) ) ;
#6711=VECTOR ( 'NONE', #16455, 1000.000000000000000 ) ;
#6712=VERTEX_POINT ( 'NONE', #16085 ) ;
#6713=DIRECTION ( 'NONE',  ( 0.000000000000000000, 0.000000000000000000, 1.000000000000000000 ) ) ;
#6719=DIRECTION ( 'NONE',  ( 2.220446049250309876E-16, 1.000000000000000000, -1.850371707708599740E-16 ) ) ;
#6721=CYLINDRICAL_SURFACE ( 'NONE', #6512, 0.6000000000000000888 ) ;
#6723=ORIENTED_EDGE ( 'NONE', *, *, #3137, .T. ) ;
#6724=LINE ( 'NONE', #7940, #3283 ) ;
#6735=VECTOR ( 'NONE', #1307, 1000.000000000000000 ) ;
#6736=CIRCLE ( 'NONE', #18233, 1.016666666666670160 ) ;
#6751=AXIS2_PLACEMENT_3D ( 'NONE', #9314, #13492, #13596 ) ;
#6752=ADVANCED_FACE ( 'NONE', ( #16170 ), #3474, .T. ) ;
#6753=VECTOR ( 'NONE', #9628, 1000.000000000000000 ) ;
#6754=ORIENTED_EDGE ( 'NONE', *, *, #536, .T. ) ;
#6758=CIRCLE ( 'NONE', #1450, 0.04999999999999991257 ) ;
#6765=AXIS2_PLACEMENT_3D ( 'NONE', #17835, #9618, #12490 ) ;
#6768=DIRECTION ( 'NONE',  ( -0.9622640697945192834, -0.2721173643531200614, 0.000000000000000000 ) ) ;
#6769=VERTEX_POINT ( 'NONE', #9215 ) ;
#6776=ADVANCED_FACE ( 'NONE', ( #10799 ), #10903, .T. ) ;
#6780=AXIS2_PLACEMENT_3D ( 'NONE', #14317, #11711, #7544 ) ;
#6788=ORIENTED_EDGE ( 'NONE', *, *, #15164, .T. ) ;
#6791=ORIENTED_EDGE ( 'NONE', *, *, #2571, .T. ) ;
#6794=ORIENTED_EDGE ( 'NONE', *, *, #16940, .T. ) ;
#6806=LINE ( 'NONE', #12363, #14984 ) ;
#6810=LINE ( 'NONE', #12547, #10865 ) ;
#6814=DIRECTION ( 'NONE',  ( 1.000000000000000000, 0.000000000000000000, 0.000000000000000000 ) ) ;
#6821=VERTEX_POINT ( 'NONE', #12469 ) ;
#6824=CARTESIAN_POINT ( 'NONE',  ( -1.800000000000000044, 12.00000000000000000, 7.649999999999999467 ) ) ;
#6835=VECTOR ( 'NONE', #12583, 1000.000000000000114 ) ;
#6843=PRODUCT_DEFINITION_SHAPE ( 'NONE', 'NONE',  #15039 ) ;
#6846=DIRECTION ( 'NONE',  ( -2.168404344971021884E-15, 1.000000000000000000, 0.000000000000000000 ) ) ;
#6848=EDGE_LOOP ( 'NONE', ( #10132, #6971, #966, #17283 ) ) ;
#6858=CARTESIAN_POINT ( 'NONE',  ( 1.875000000000000000, 12.00000000000000000, 7.700000000000000178 ) ) ;
#6863=ORIENTED_EDGE ( 'NONE', *, *, #13276, .T. ) ;
#6864=VERTEX_POINT ( 'NONE', #10991 ) ;
#6865=EDGE_LOOP ( 'NONE', ( #1623, #11346, #8842, #11336 ) ) ;
#6866=CARTESIAN_POINT ( 'NONE',  ( 1.850000000000000089, 11.25000000000000000, 8.300000000000000711 ) ) ;
#6870=CARTESIAN_POINT ( 'NONE',  ( 2.500000000000000000, 10.00000000000000000, 1.600000000000000089 ) ) ;
#6884=DIRECTION ( 'NONE',  ( -2.242874797222539596E-16, 0.000000000000000000, -1.000000000000000000 ) ) ;
#6893=LINE ( 'NONE', #18153, #5986 ) ;
#6894=FACE_OUTER_BOUND ( 'NONE', #11682, .T. ) ;
#6900=LINE ( 'NONE', #12550, #11765 ) ;
#6909=CARTESIAN_POINT ( 'NONE',  ( 1.875000000000000000, 11.25000000000000000, 7.700000000000000178 ) ) ;
#6928=FACE_OUTER_BOUND ( 'NONE', #691, .T. ) ;
#6931=ORIENTED_EDGE ( 'NONE', *, *, #15715, .T. ) ;
#6933=SURFACE_SIDE_STYLE ('',( #5733 ) ) ;
#6937=EDGE_CURVE ( 'NONE', #11364, #2762, #11356, .T. ) ;
#6946=ORIENTED_EDGE ( 'NONE', *, *, #15234, .T. ) ;
#6950=VERTEX_POINT ( 'NONE', #14127 ) ;
#6957=CARTESIAN_POINT ( 'NONE',  ( 1.399999999999999911, 6.400000000000000355, 7.700000000000000178 ) ) ;
#6966=ORIENTED_EDGE ( 'NONE', *, *, #15845, .F. ) ;
#6971=ORIENTED_EDGE ( 'NONE', *, *, #15217, .F. ) ;
#6974=VECTOR ( 'NONE', #10834, 1000.000000000000000 ) ;
#6975=ADVANCED_FACE ( 'NONE', ( #248 ), #15630, .T. ) ;
#6976=ORIENTED_EDGE ( 'NONE', *, *, #15995, .T. ) ;
#6978=ADVANCED_FACE ( 'NONE', ( #1454 ), #7111, .T. ) ;
#6983=DIRECTION ( 'NONE',  ( 3.700743415417199972E-16, -1.000000000000000000, -3.581736239852560511E-31 ) ) ;
#6986=DIRECTION ( 'NONE',  ( 1.025799815460950140E-14, 1.000000000000000000, 0.000000000000000000 ) ) ;
#6988=AXIS2_PLACEMENT_3D ( 'NONE', #4260, #14273, #16769 ) ;
#6989=ORIENTED_EDGE ( 'NONE', *, *, #2845, .F. ) ;
#6991=DIRECTION ( 'NONE',  ( 0.000000000000000000, 0.000000000000000000, -1.000000000000000000 ) ) ;
#6993=AXIS2_PLACEMENT_3D ( 'NONE', #5465, #3974, #3796 ) ;
#6999=ORIENTED_EDGE ( 'NONE', *, *, #6353, .F. ) ;
#7000=EDGE_CURVE ( 'NONE', #3076, #4272, #12653, .T. ) ;
#7002=CARTESIAN_POINT ( 'NONE',  ( 1.906474350327903052E-15, 10.16754446796632649, 7.700000000000000178 ) ) ;
#7006=DIRECTION ( 'NONE',  ( 0.000000000000000000, 0.000000000000000000, -1.000000000000000000 ) ) ;
#7007=EDGE_CURVE ( 'NONE', #13279, #4421, #4303, .T. ) ;
#7009=EDGE_CURVE ( 'NONE', #16249, #13226, #10534, .T. ) ;
#7013=VECTOR ( 'NONE', #6470, 1000.000000000000114 ) ;
#7014=ADVANCED_FACE ( 'NONE', ( #4483 ), #1545, .T. ) ;
#7017=VECTOR ( 'NONE', #9361, 1000.000000000000000 ) ;
#7018=CIRCLE ( 'NONE', #7302, 0.6500000000000000222 ) ;
#7023=LINE ( 'NONE', #10076, #13101 ) ;
#7024=CARTESIAN_POINT ( 'NONE',  ( -2.500000000000000000, 1.071484571201660082E-16, -4.257195078628519890E-16 ) ) ;
#7029=ORIENTED_EDGE ( 'NONE', *, *, #5421, .T. ) ;
#7033=ADVANCED_FACE ( 'NONE', ( #15535 ), #9965, .T. ) ;
#7034=ORIENTED_EDGE ( 'NONE', *, *, #18192, .T. ) ;
#7036=AXIS2_PLACEMENT_3D ( 'NONE', #8628, #7158, #14271 ) ;
#7038=VECTOR ( 'NONE', #1620, 1000.000000000000000 ) ;
#7049=EDGE_CURVE ( 'NONE', #18253, #8865, #7018, .T. ) ;
#7050=DIRECTION ( 'NONE',  ( -1.930822651522009842E-16, -1.000000000000000000, -1.268826313857319964E-16 ) ) ;
#7057=DIRECTION ( 'NONE',  ( 6.661338147750940229E-16, -1.710569414459004727E-47, 1.000000000000000000 ) ) ;
#7058=ORIENTED_EDGE ( 'NONE', *, *, #14259, .F. ) ;
#7059=DIRECTION ( 'NONE',  ( -0.000000000000000000, 1.000000000000000000, 0.000000000000000000 ) ) ;
#7060=LINE ( 'NONE', #14344, #1443 ) ;
#7062=VECTOR ( 'NONE', #8389, 1000.000000000000000 ) ;
#7067=PLANE ( 'NONE',  #17928 ) ;
#7070=DIRECTION ( 'NONE',  ( 0.000000000000000000, -1.000000000000000000, -1.332267629550190018E-15 ) ) ;
#7076=LINE ( 'NONE', #18235, #17348 ) ;
#7078=ORIENTED_EDGE ( 'NONE', *, *, #5217, .F. ) ;
#7080=ORIENTED_EDGE ( 'NONE', *, *, #14124, .T. ) ;
#7081=AXIS2_PLACEMENT_3D ( 'NONE', #2076, #17889, #7730 ) ;
#7092=DIRECTION ( 'NONE',  ( 3.700743415417190309E-15, 1.480297366166879989E-15, -1.000000000000000000 ) ) ;
#7094=FACE_OUTER_BOUND ( 'NONE', #4831, .T. ) ;
#7095=CIRCLE ( 'NONE', #5899, 0.3999999999999999667 ) ;
#7100=CARTESIAN_POINT ( 'NONE',  ( -2.500000000000000000, 2.799999999999999822, 1.600000000000000089 ) ) ;
#7103=PRODUCT_DEFINITION_FORMATION_WITH_SPECIFIED_SOURCE ( 'ANY', '', #9637, .NOT_KNOWN. ) ;
#7111=SPHERICAL_SURFACE ( 'NONE', #14104, 1.100000000000000089 ) ;
#7112=ORIENTED_EDGE ( 'NONE', *, *, #4777, .F. ) ;
#7119=EDGE_CURVE ( 'NONE', #17218, #10817, #5796, .T. ) ;
#7120=EDGE_LOOP ( 'NONE', ( #3241, #15298, #10416, #1129 ) ) ;
#7121=AXIS2_PLACEMENT_3D ( 'NONE', #5989, #17354, #6251 ) ;
#7128=CARTESIAN_POINT ( 'NONE',  ( 1.899999999999999911, 1.010812223616570040E-16, 4.000000000000000000 ) ) ;
#7129=EDGE_CURVE ( 'NONE', #6319, #5435, #9367, .T. ) ;
#7130=CARTESIAN_POINT ( 'NONE',  ( -1.899999999999999911, 11.15000000000000036, 1.600000000000000089 ) ) ;
#7132=ORIENTED_EDGE ( 'NONE', *, *, #17696, .F. ) ;
#7134=DIRECTION ( 'NONE',  ( -4.810966440042350793E-15, 0.000000000000000000, -1.000000000000000000 ) ) ;
#7137=VECTOR ( 'NONE', #14051, 1000.000000000000000 ) ;
#7148=DIRECTION ( 'NONE',  ( 0.000000000000000000, 0.000000000000000000, 1.000000000000000000 ) ) ;
#7154=ORIENTED_EDGE ( 'NONE', *, *, #16095, .T. ) ;
#7155=CARTESIAN_POINT ( 'NONE',  ( 1.399999999999999911, 5.799999999999999822, 8.300000000000000711 ) ) ;
#7156=ORIENTED_EDGE ( 'NONE', *, *, #12310, .T. ) ;
#7158=DIRECTION ( 'NONE',  ( -4.794417550286630491E-31, 1.000000000000000000, 1.774290917998389804E-45 ) ) ;
#7159=CARTESIAN_POINT ( 'NONE',  ( -0.5291502622129179434, 0.1000000000000000056, 7.700000000000000178 ) ) ;
#7162=CARTESIAN_POINT ( 'NONE',  ( -1.875000000000000000, 12.00000000000000000, 7.700000000000000178 ) ) ;
#7167=EDGE_CURVE ( 'NONE', #7523, #8572, #16816, .T. ) ;
#7179=EDGE_LOOP ( 'NONE', ( #14648, #17228, #14420, #5795 ) ) ;
#7187=CARTESIAN_POINT ( 'NONE',  ( -1.800000000000000044, 11.29999999999999893, 7.649999999999999467 ) ) ;
#7191=AXIS2_PLACEMENT_3D ( 'NONE', #4116, #18158, #4017 ) ;
#7200=VERTEX_POINT ( 'NONE', #12835 ) ;
#7207=ORIENTED_EDGE ( 'NONE', *, *, #14655, .F. ) ;
#7209=CARTESIAN_POINT ( 'NONE',  ( 1.899999999999999911, 2.799999999999999822, 0.6099999999999999867 ) ) ;
#7215=CARTESIAN_POINT ( 'NONE',  ( 0.03000000000000110217, 11.40000000000000036, 7.649999999999999467 ) ) ;
#7220=DIRECTION ( 'NONE',  ( -2.220446049250309876E-16, -1.000000000000000000, 1.110223024625159992E-16 ) ) ;
#7226=LINE ( 'NONE', #8527, #585 ) ;
#7227=ORIENTED_EDGE ( 'NONE', *, *, #9115, .F. ) ;
#7232=EDGE_CURVE ( 'NONE', #8344, #7890, #12923, .T. ) ;
#7233=EDGE_LOOP ( 'NONE', ( #1926, #8035, #10295, #11428 ) ) ;
#7237=LINE ( 'NONE', #14188, #9991 ) ;
#7262=VERTEX_POINT ( 'NONE', #14399 ) ;
#7266=CARTESIAN_POINT ( 'NONE',  ( 2.500000000000000000, 2.000000000000000000, 1.600000000000000089 ) ) ;
#7273=DIRECTION ( 'NONE',  ( -4.037174635000570090E-16, 0.000000000000000000, 1.000000000000000000 ) ) ;
#7274=EDGE_CURVE ( 'NONE', #8790, #1178, #8730, .T. ) ;
#7276=DIRECTION ( 'NONE',  ( 2.500805593834189724E-46, 1.000000000000000000, 1.332267629550190018E-15 ) ) ;
#7277=EDGE_CURVE ( 'NONE', #12789, #5684, #4546, .T. ) ;
#7286=LINE ( 'NONE', #157, #839 ) ;
#7290=CARTESIAN_POINT ( 'NONE',  ( 1.899999999999999911, 2.000000000000000000, 1.600000000000000089 ) ) ;
#7293=ORIENTED_EDGE ( 'NONE', *, *, #11294, .F. ) ;
#7297=VERTEX_POINT ( 'NONE', #1701 ) ;
#7298=AXIS2_PLACEMENT_3D ( 'NONE', #17794, #779, #10589 ) ;
#7302=AXIS2_PLACEMENT_3D ( 'NONE', #14035, #9876, #10058 ) ;
#7303=EDGE_CURVE ( 'NONE', #5456, #8719, #483, .T. ) ;
#7308=CIRCLE ( 'NONE', #5228, 0.8000000000000000444 ) ;
#7310=LINE ( 'NONE', #17193, #12331 ) ;
#7313=LINE ( 'NONE', #2017, #13900 ) ;
#7314=ORIENTED_EDGE ( 'NONE', *, *, #7643, .T. ) ;
#7318=CARTESIAN_POINT ( 'NONE',  ( -0.3367924244280810497, 2.254758922476410188, 7.700000000000000178 ) ) ;
#7319=LINE ( 'NONE', #11567, #8828 ) ;
#7320=VECTOR ( 'NONE', #14451, 1000.000000000000000 ) ;
#7323=LINE ( 'NONE', #14449, #9435 ) ;
#7329=DIRECTION ( 'NONE',  ( -6.049014748177250683E-16, 2.493473113004675144E-16, -1.000000000000000000 ) ) ;
#7338=EDGE_CURVE ( 'NONE', #1995, #8433, #11597, .T. ) ;
#7343=AXIS2_PLACEMENT_3D ( 'NONE', #9202, #7926, #13577 ) ;
#7347=ADVANCED_FACE ( 'NONE', ( #5955 ), #8990, .F. ) ;
#7352=CIRCLE ( 'NONE', #2016, 0.6100000000000000977 ) ;
#7353=CIRCLE ( 'NONE', #6703, 0.7211102550927981358 ) ;
#7355=DIRECTION ( 'NONE',  ( -1.000000000000000000, 0.000000000000000000, 0.000000000000000000 ) ) ;
#7357=ORIENTED_EDGE ( 'NONE', *, *, #6133, .T. ) ;
#7365=AXIS2_PLACEMENT_3D ( 'NONE', #11540, #5802, #14586 ) ;
#7366=LINE ( 'NONE', #11429, #17096 ) ;
#7380=DIRECTION ( 'NONE',  ( 0.000000000000000000, -1.000000000000000000, 2.493473113004670213E-16 ) ) ;
#7384=ORIENTED_EDGE ( 'NONE', *, *, #10722, .F. ) ;
#7385=ADVANCED_FACE ( 'NONE', ( #3174 ), #8830, .F. ) ;
#7386=CARTESIAN_POINT ( 'NONE',  ( 2.500000000000000000, 7.299999999999999822, 0.6099999999999999867 ) ) ;
#7387=AXIS2_PLACEMENT_3D ( 'NONE', #15953, #2037, #17564 ) ;
#7401=VECTOR ( 'NONE', #9799, 1000.000000000000000 ) ;
#7405=FACE_BOUND ( 'NONE', #5772, .T. ) ;
#7406=DIRECTION ( 'NONE',  ( 1.000000000000000000, 0.000000000000000000, -7.401486830834380223E-16 ) ) ;
#7409=ORIENTED_EDGE ( 'NONE', *, *, #12418, .F. ) ;
#7410=CARTESIAN_POINT ( 'NONE',  ( 1.889999999999999902, 7.299999999999999822, 0.5999999999999999778 ) ) ;
#7411=AXIS2_PLACEMENT_3D ( 'NONE', #11826, #3035, #4767 ) ;
#7412=PLANE ( 'NONE',  #15051 ) ;
#7414=ORIENTED_EDGE ( 'NONE', *, *, #15014, .T. ) ;
#7416=DIRECTION ( 'NONE',  ( 2.590520390792030218E-15, 0.000000000000000000, -1.000000000000000000 ) ) ;
#7419=DIRECTION ( 'NONE',  ( -6.049014748177260544E-16, 0.000000000000000000, -1.000000000000000000 ) ) ;
#7424=AXIS2_PLACEMENT_3D ( 'NONE', #11373, #8678, #18189 ) ;
#7427=FACE_OUTER_BOUND ( 'NONE', #16262, .T. ) ;
#7428=CARTESIAN_POINT ( 'NONE',  ( -2.616666666666669805, -4.318079751576579732E-16, 4.000000000000000000 ) ) ;
#7434=VERTEX_POINT ( 'NONE', #3425 ) ;
#7435=DIRECTION ( 'NONE',  ( 1.000000000000000000, 0.000000000000000000, -7.273661547324610053E-16 ) ) ;
#7440=ORIENTED_EDGE ( 'NONE', *, *, #1271, .T. ) ;
#7441=DIRECTION ( 'NONE',  ( -1.850371707708599740E-16, -1.000000000000000000, -9.251858538542959255E-17 ) ) ;
#7444=EDGE_CURVE ( 'NONE', #15692, #11846, #16485, .T. ) ;
#7451=ORIENTED_EDGE ( 'NONE', *, *, #16364, .F. ) ;
#7452=DIRECTION ( 'NONE',  ( -1.000000000000000000, 0.000000000000000000, -1.739311637268509859E-16 ) ) ;
#7456=LINE ( 'NONE', #13097, #13023 ) ;
#7464=CARTESIAN_POINT ( 'NONE',  ( 1.800000000000000044, 11.29999999999999893, 1.600000000000000089 ) ) ;
#7466=CARTESIAN_POINT ( 'NONE',  ( 2.500000000000000000, 11.29999999999999893, 7.649999999999999467 ) ) ;
#7467=EDGE_LOOP ( 'NONE', ( #12808, #7943, #3858, #17637 ) ) ;
#7475=ORIENTED_EDGE ( 'NONE', *, *, #3951, .F. ) ;
#7476=ORIENTED_EDGE ( 'NONE', *, *, #6014, .T. ) ;
#7477=CARTESIAN_POINT ( 'NONE',  ( 0.5372984490435490645, 4.599999999999999645, 7.700000000000000178 ) ) ;
#7482=DIRECTION ( 'NONE',  ( -1.000000000000000000, 1.480297366166879989E-15, 0.000000000000000000 ) ) ;
#7496=CARTESIAN_POINT ( 'NONE',  ( 1.289999999999999813, 7.900000000000003908, 2.878305776370009209E-15 ) ) ;
#7497=PLANE ( 'NONE',  #841 ) ;
#7498=ORIENTED_EDGE ( 'NONE', *, *, #14566, .F. ) ;
#7499=DIRECTION ( 'NONE',  ( -1.000000000000000000, 0.000000000000000000, 0.000000000000000000 ) ) ;
#7501=EDGE_CURVE ( 'NONE', #14262, #12160, #5304, .T. ) ;
#7503=CARTESIAN_POINT ( 'NONE',  ( -2.500000000000000000, 11.15000000000000036, 1.600000000000000089 ) ) ;
#7509=DIRECTION ( 'NONE',  ( 6.123233995736769734E-17, 0.000000000000000000, 1.000000000000000000 ) ) ;
#7514=ORIENTED_EDGE ( 'NONE', *, *, #10489, .T. ) ;
#7515=ORIENTED_EDGE ( 'NONE', *, *, #6236, .F. ) ;
#7521=DIRECTION ( 'NONE',  ( 1.000000000000000000, -1.224646799147350002E-16, 0.000000000000000000 ) ) ;
#7523=VERTEX_POINT ( 'NONE', #14837 ) ;
#7524=PLANE ( 'NONE',  #2290 ) ;
#7525=DIRECTION ( 'NONE',  ( -4.440892098500630106E-16, 0.000000000000000000, -1.000000000000000000 ) ) ;
#7531=ORIENTED_EDGE ( 'NONE', *, *, #8286, .T. ) ;
#7534=EDGE_CURVE ( 'NONE', #16854, #15324, #2299, .T. ) ;
#7535=CARTESIAN_POINT ( 'NONE',  ( 13.63407075111029876, 11.40000000000000036, 9.955530934770520091 ) ) ;
#7536=EDGE_CURVE ( 'NONE', #14839, #17750, #4353, .T. ) ;
#7539=ORIENTED_EDGE ( 'NONE', *, *, #3828, .T. ) ;
#7542=LINE ( 'NONE', #13371, #11613 ) ;
#7544=DIRECTION ( 'NONE',  ( -1.000000000000000000, 0.000000000000000000, 4.318427418585891014E-15 ) ) ;
#7546=ORIENTED_EDGE ( 'NONE', *, *, #2275, .F. ) ;
#7547=ADVANCED_FACE ( 'NONE', ( #4082 ), #15677, .T. ) ;
#7548=CARTESIAN_POINT ( 'NONE',  ( -1.889999999999999902, 8.500000000000000000, 0.5999999999999999778 ) ) ;
#7552=LINE ( 'NONE', #3376, #14305 ) ;
#7557=EDGE_CURVE ( 'NONE', #8790, #12277, #4644, .T. ) ;
#7563=ORIENTED_EDGE ( 'NONE', *, *, #17653, .T. ) ;
#7565=VECTOR ( 'NONE', #1207, 1000.000000000000000 ) ;
#7566=FACE_OUTER_BOUND ( 'NONE', #13919, .T. ) ;
#7567=CARTESIAN_POINT ( 'NONE',  ( 2.500000000000000000, 4.700000000000000178, 0.6099999999999999867 ) ) ;
#7572=DIRECTION ( 'NONE',  ( 0.000000000000000000, -1.000000000000000000, -1.359631073446889961E-32 ) ) ;
#7575=ORIENTED_EDGE ( 'NONE', *, *, #8015, .T. ) ;
#7578=DIRECTION ( 'NONE',  ( -5.865000419954259844E-16, 9.550139141648499357E-32, -1.000000000000000000 ) ) ;
#7579=ORIENTED_EDGE ( 'NONE', *, *, #8688, .F. ) ;
#7581=CARTESIAN_POINT ( 'NONE',  ( 13.63407075111029876, 12.00000000000000000, 9.955530934770520091 ) ) ;
#7586=DIRECTION ( 'NONE',  ( 6.771944841082658606E-17, -4.886939904639989483E-32, 1.000000000000000000 ) ) ;
#7590=AXIS2_PLACEMENT_3D ( 'NONE', #1625, #12911, #5880 ) ;
#7603=DIRECTION ( 'NONE',  ( 0.9622640697945186172, -0.2721173643531222264, 0.000000000000000000 ) ) ;
#7604=CIRCLE ( 'NONE', #13221, 0.6099999999999999867 ) ;
#7611=VECTOR ( 'NONE', #3713, 1000.000000000000000 ) ;
#7612=LINE ( 'NONE', #16129, #14689 ) ;
#7613=VECTOR ( 'NONE', #7355, 1000.000000000000000 ) ;
#7615=AXIS2_PLACEMENT_3D ( 'NONE', #5070, #1538, #8921 ) ;
#7619=VECTOR ( 'NONE', #13377, 1000.000000000000000 ) ;
#7621=CARTESIAN_POINT ( 'NONE',  ( -1.899999999999999911, 8.500000000000000000, 0.6099999999999999867 ) ) ;
#7630=CARTESIAN_POINT ( 'NONE',  ( 1.899999999999999911, 0.8000000000000000444, -1.674850734291659957E-15 ) ) ;
#7634=AXIS2_PLACEMENT_3D ( 'NONE', #8006, #13829, #9655 ) ;
#7636=CARTESIAN_POINT ( 'NONE',  ( -0.02999999999999939868, 11.40000000000000036, 1.600000000000000089 ) ) ;
#7642=VERTEX_POINT ( 'NONE', #15306 ) ;
#7643=EDGE_CURVE ( 'NONE', #11239, #11698, #12644, .T. ) ;
#7651=ORIENTED_EDGE ( 'NONE', *, *, #10288, .T. ) ;
#7656=DIRECTION ( 'NONE',  ( 2.986159789035700404E-15, -1.110223024625159992E-16, -1.000000000000000000 ) ) ;
#7658=FACE_OUTER_BOUND ( 'NONE', #13158, .T. ) ;
#7660=EDGE_CURVE ( 'NONE', #10817, #14318, #2710, .T. ) ;
#7661=FACE_OUTER_BOUND ( 'NONE', #5996, .T. ) ;
#7662=LINE ( 'NONE', #17540, #18240 ) ;
#7667=EDGE_CURVE ( 'NONE', #14593, #6821, #7237, .T. ) ;
#7668=VECTOR ( 'NONE', #15394, 1000.000000000000000 ) ;
#7671=DIRECTION ( 'NONE',  ( 1.036208156316810036E-14, 1.000000000000000000, 0.000000000000000000 ) ) ;
#7676=ORIENTED_EDGE ( 'NONE', *, *, #8407, .T. ) ;
#7679=VERTEX_POINT ( 'NONE', #18128 ) ;
#7680=AXIS2_PLACEMENT_3D ( 'NONE', #11752, #3395, #8964 ) ;
#7683=CARTESIAN_POINT ( 'NONE',  ( -1.899999999999999911, 11.29999999999999893, 7.649999999999999467 ) ) ;
#7691=CIRCLE ( 'NONE', #9470, 0.04999999999999969746 ) ;
#7699=DIRECTION ( 'NONE',  ( 0.000000000000000000, 0.000000000000000000, 1.000000000000000000 ) ) ;
#7700=ORIENTED_EDGE ( 'NONE', *, *, #11971, .F. ) ;
#7706=VECTOR ( 'NONE', #17810, 1000.000000000000000 ) ;
#7709=ADVANCED_FACE ( 'NONE', ( #17203 ), #6102, .F. ) ;
#7710=CARTESIAN_POINT ( 'NONE',  ( 1.889999999999999902, 4.700000000000000178, -5.846397852431180656E-16 ) ) ;
#7714=ORIENTED_EDGE ( 'NONE', *, *, #4777, .T. ) ;
#7727=LINE ( 'NONE', #14582, #14636 ) ;
#7729=FACE_BOUND ( 'NONE', #16231, .T. ) ;
#7730=DIRECTION ( 'NONE',  ( 0.000000000000000000, -1.000000000000000000, 9.633757521571540356E-31 ) ) ;
#7735=ORIENTED_EDGE ( 'NONE', *, *, #3579, .F. ) ;
#7742=CARTESIAN_POINT ( 'NONE',  ( -1.889999999999999902, 7.900000000000000355, 3.000000000000000000 ) ) ;
#7743=DIRECTION ( 'NONE',  ( 0.000000000000000000, 0.000000000000000000, -1.000000000000000000 ) ) ;
#7751=AXIS2_PLACEMENT_3D ( 'NONE', #2326, #13623, #7975 ) ;
#7752=CARTESIAN_POINT ( 'NONE',  ( -11.62823001646920140, 1.398466485101550089E-14, -4.396483177515619900E-14 ) ) ;
#7753=DIRECTION ( 'NONE',  ( 0.000000000000000000, 0.000000000000000000, 1.000000000000000000 ) ) ;
#7755=DIRECTION ( 'NONE',  ( 0.000000000000000000, 0.000000000000000000, -1.000000000000000000 ) ) ;
#7758=ORIENTED_EDGE ( 'NONE', *, *, #18053, .F. ) ;
#7759=LINE ( 'NONE', #13404, #6425 ) ;
#7766=ORIENTED_EDGE ( 'NONE', *, *, #10051, .T. ) ;
#7769=DIRECTION ( 'NONE',  ( -1.000000000000000000, 2.220446049250309876E-16, 0.000000000000000000 ) ) ;
#7770=EDGE_CURVE ( 'NONE', #13022, #10426, #8973, .T. ) ;
#7772=EDGE_CURVE ( 'NONE', #13357, #10192, #3064, .T. ) ;
#7773=VERTEX_POINT ( 'NONE', #3328 ) ;
#7775=LINE ( 'NONE', #15195, #17081 ) ;
#7781=DIRECTION ( 'NONE',  ( -4.810966440042350793E-15, 0.000000000000000000, -1.000000000000000000 ) ) ;
#7788=ORIENTED_EDGE ( 'NONE', *, *, #5769, .F. ) ;
#7790=ADVANCED_FACE ( 'NONE', ( #12970 ), #557, .T. ) ;
#7796=DIRECTION ( 'NONE',  ( -3.652293603810800245E-15, -1.332267629550183904E-15, 1.000000000000000000 ) ) ;
#7803=ORIENTED_EDGE ( 'NONE', *, *, #5085, .T. ) ;
#7805=ORIENTED_EDGE ( 'NONE', *, *, #17646, .T. ) ;
#7811=VERTEX_POINT ( 'NONE', #9052 ) ;
#7816=CARTESIAN_POINT ( 'NONE',  ( 2.500000000000000000, 11.29999999999999893, 1.600000000000000089 ) ) ;
#7817=DIRECTION ( 'NONE',  ( 0.000000000000000000, -1.000000000000000000, 1.110223024625159992E-16 ) ) ;
#7819=CARTESIAN_POINT ( 'NONE',  ( 1.850000000000000089, 0.7500000000000000000, 7.700000000000000178 ) ) ;
#7833=EDGE_CURVE ( 'NONE', #240, #14839, #7775, .T. ) ;
#7843=LINE ( 'NONE', #593, #15032 ) ;
#7846=LINE ( 'NONE', #4971, #3165 ) ;
#7849=VERTEX_POINT ( 'NONE', #2220 ) ;
#7860=CARTESIAN_POINT ( 'NONE',  ( -1.600000000000000089, -9.269168731236250681E-17, 7.649999999999999467 ) ) ;
#7863=ORIENTED_EDGE ( 'NONE', *, *, #11714, .T. ) ;
#7872=VECTOR ( 'NONE', #6181, 1000.000000000000000 ) ;
#7878=CARTESIAN_POINT ( 'NONE',  ( -2.500000000000000000, 11.15000000000000036, 8.358214404180679581E-16 ) ) ;
#7883=EDGE_LOOP ( 'NONE', ( #571, #15095, #14612, #8643 ) ) ;
#7884=FACE_OUTER_BOUND ( 'NONE', #17299, .T. ) ;
#7886=VECTOR ( 'NONE', #16427, 1000.000000000000000 ) ;
#7888=CIRCLE ( 'NONE', #18204, 0.4000000000000000222 ) ;
#7890=VERTEX_POINT ( 'NONE', #642 ) ;
#7892=ADVANCED_FACE ( 'NONE', ( #6368 ), #834, .F. ) ;
#7895=VECTOR ( 'NONE', #4218, 1000.000000000000000 ) ;
#7896=EDGE_CURVE ( 'NONE', #1884, #6712, #9447, .T. ) ;
#7900=EDGE_CURVE ( 'NONE', #11111, #5685, #10650, .T. ) ;
#7908=AXIS2_PLACEMENT_3D ( 'NONE', #4178, #8544, #12800 ) ;
#7909=VECTOR ( 'NONE', #14376, 1000.000000000000000 ) ;
#7918=DIRECTION ( 'NONE',  ( -2.537652627714639929E-16, -1.000000000000000000, 0.000000000000000000 ) ) ;
#7920=DIRECTION ( 'NONE',  ( 0.000000000000000000, 0.000000000000000000, 1.000000000000000000 ) ) ;
#7921=EDGE_CURVE ( 'NONE', #13368, #3854, #14424, .T. ) ;
#7922=DIRECTION ( 'NONE',  ( 3.700743415417190309E-15, -6.579099405186109509E-16, 1.000000000000000000 ) ) ;
#7926=DIRECTION ( 'NONE',  ( 1.059690869644410208E-14, 1.000000000000000000, -1.041146930477340028E-32 ) ) ;
#7929=VECTOR ( 'NONE', #10456, 1000.000000000000000 ) ;
#7932=ORIENTED_EDGE ( 'NONE', *, *, #6216, .T. ) ;
#7935=DIRECTION ( 'NONE',  ( 6.083413833562510128E-16, -1.647588903766459698E-16, 1.000000000000000000 ) ) ;
#7940=CARTESIAN_POINT ( 'NONE',  ( 2.500000000000000000, 10.00000000000000000, 1.600000000000000089 ) ) ;
#7941=CARTESIAN_POINT ( 'NONE',  ( 1.875000000000000000, 11.25000000000000000, 7.700000000000000178 ) ) ;
#7943=ORIENTED_EDGE ( 'NONE', *, *, #7557, .F. ) ;
#7945=VECTOR ( 'NONE', #12513, 1000.000000000000000 ) ;
#7946=VECTOR ( 'NONE', #3504, 1000.000000000000000 ) ;
#7948=DIRECTION ( 'NONE',  ( 5.181040781584069903E-15, 1.000000000000000000, 0.000000000000000000 ) ) ;
#7949=PLANE ( 'NONE',  #11172 ) ;
#7952=LINE ( 'NONE', #13599, #4618 ) ;
#7965=ORIENTED_EDGE ( 'NONE', *, *, #2642, .F. ) ;
#7970=VERTEX_POINT ( 'NONE', #18196 ) ;
#7972=DIRECTION ( 'NONE',  ( -9.588835100573269740E-31, 1.000000000000000000, 3.548581835996780230E-45 ) ) ;
#7974=AXIS2_PLACEMENT_3D ( 'NONE', #11411, #14002, #9502 ) ;
#7975=DIRECTION ( 'NONE',  ( 0.000000000000000000, 0.000000000000000000, 1.000000000000000000 ) ) ;
#7998=CARTESIAN_POINT ( 'NONE',  ( 1.875000000000000000, 11.25000000000000000, 7.700000000000000178 ) ) ;
#8003=CARTESIAN_POINT ( 'NONE',  ( 1.875000000000000000, 12.00000000000000000, 7.700000000000000178 ) ) ;
#8006=CARTESIAN_POINT ( 'NONE',  ( -1.850000000000000089, 0.7500000000000000000, 8.300000000000000711 ) ) ;
#8008=VECTOR ( 'NONE', #8120, 1000.000000000000000 ) ;
#8014=MANIFOLD_SOLID_BREP ( 'Stock-MAS-687-1', #481 ) ;
#8015=EDGE_CURVE ( 'NONE', #9909, #6712, #12581, .T. ) ;
#8018=CARTESIAN_POINT ( 'NONE',  ( -1.899999999999999911, 3.500000000000000000, 0.6099999999999999867 ) ) ;
#8035=ORIENTED_EDGE ( 'NONE', *, *, #12425, .F. ) ;
#8041=ADVANCED_FACE ( 'NONE', ( #7566 ), #11641, .F. ) ;
#8053=ORIENTED_EDGE ( 'NONE', *, *, #10379, .F. ) ;
#8062=ORIENTED_EDGE ( 'NONE', *, *, #15584, .T. ) ;
#8067=ORIENTED_EDGE ( 'NONE', *, *, #3196, .T. ) ;
#8079=CARTESIAN_POINT ( 'NONE',  ( -0.7999999999998790301, 11.40000000000000036, -2.399999999999999911 ) ) ;
#8089=CYLINDRICAL_SURFACE ( 'NONE', #4642, 0.6100000000000000977 ) ;
#8092=ORIENTED_EDGE ( 'NONE', *, *, #9115, .T. ) ;
#8094=ORIENTED_EDGE ( 'NONE', *, *, #7274, .T. ) ;
#8098=CIRCLE ( 'NONE', #9869, 0.6500000000000003553 ) ;
#8106=DIRECTION ( 'NONE',  ( 0.000000000000000000, 0.000000000000000000, -1.000000000000000000 ) ) ;
#8107=DIRECTION ( 'NONE',  ( 0.000000000000000000, -1.000000000000000000, 0.000000000000000000 ) ) ;
#8112=DIRECTION ( 'NONE',  ( 0.000000000000000000, 0.000000000000000000, 1.000000000000000000 ) ) ;
#8116=CARTESIAN_POINT ( 'NONE',  ( 1.889999999999999902, 3.500000000000000000, 0.6099999999999999867 ) ) ;
#8120=DIRECTION ( 'NONE',  ( -1.000000000000000000, 0.000000000000000000, 0.000000000000000000 ) ) ;
#8121=VECTOR ( 'NONE', #7578, 1000.000000000000000 ) ;
#8132=EDGE_CURVE ( 'NONE', #4379, #10381, #3223, .T. ) ;
#8138=ADVANCED_FACE ( 'NONE', ( #2100 ), #10714, .F. ) ;
#8141=ADVANCED_FACE ( 'NONE', ( #807 ), #910, .F. ) ;
#8146=CARTESIAN_POINT ( 'NONE',  ( -2.500000000000000000, 11.25000000000000000, 7.649999999999999467 ) ) ;
#8148=ORIENTED_EDGE ( 'NONE', *, *, #211, .F. ) ;
#8150=CARTESIAN_POINT ( 'NONE',  ( -0.7999999999998790301, 11.40000000000000036, -2.399999999999999911 ) ) ;
#8154=DIRECTION ( 'NONE',  ( 4.318427418585891014E-15, -2.220446049250315053E-16, 1.000000000000000000 ) ) ;
#8156=ADVANCED_FACE ( 'NONE', ( #9222 ), #14885, .F. ) ;
#8157=LINE ( 'NONE', #1209, #831 ) ;
#8164=ORIENTED_EDGE ( 'NONE', *, *, #17275, .F. ) ;
#8169=ORIENTED_EDGE ( 'NONE', *, *, #13884, .F. ) ;
#8174=ADVANCED_FACE ( 'NONE', ( #7661 ), #12201, .F. ) ;
#8180=PLANE ( 'NONE',  #7634 ) ;
#8181=VECTOR ( 'NONE', #16530, 1000.000000000000000 ) ;
#8186=LINE ( 'NONE', #16527, #16419 ) ;
#8197=FACE_OUTER_BOUND ( 'NONE', #352, .T. ) ;
#8198=CIRCLE ( 'NONE', #17051, 0.6500000000000000222 ) ;
#8209=LINE ( 'NONE', #2477, #9714 ) ;
#8212=VECTOR ( 'NONE', #6986, 1000.000000000000000 ) ;
#8219=AXIS2_PLACEMENT_3D ( 'NONE', #10830, #16296, #17658 ) ;
#8222=CARTESIAN_POINT ( 'NONE',  ( -1.599999999999880185, 11.40000000000000036, -2.399999999999999911 ) ) ;
#8225=CARTESIAN_POINT ( 'NONE',  ( -1.899999999999999911, 11.15000000000000036, 1.600000000000000089 ) ) ;
#8229=CARTESIAN_POINT ( 'NONE',  ( -0.2000000000000000111, 0.1000000000000000056, 8.300000000000000711 ) ) ;
#8230=ORIENTED_EDGE ( 'NONE', *, *, #5541, .F. ) ;
#8231=ORIENTED_EDGE ( 'NONE', *, *, #12648, .F. ) ;
#8233=DIRECTION ( 'NONE',  ( 1.000000000000000000, 0.000000000000000000, 0.000000000000000000 ) ) ;
#8235=VECTOR ( 'NONE', #3575, 1000.000000000000000 ) ;
#8237=EDGE_CURVE ( 'NONE', #1235, #14775, #3667, .T. ) ;
#8241=EDGE_CURVE ( 'NONE', #1999, #13226, #17539, .T. ) ;
#8243=( NAMED_UNIT ( * ) PLANE_ANGLE_UNIT ( ) SI_UNIT ( $, .RADIAN. ) );
#8246=DIRECTION ( 'NONE',  ( -1.110223024625159992E-16, 0.000000000000000000, 1.000000000000000000 ) ) ;
#8247=EDGE_CURVE ( 'NONE', #3727, #17764, #6260, .T. ) ;
#8251=CYLINDRICAL_SURFACE ( 'NONE', #6993, 0.4000000000000001887 ) ;
#8252=AXIS2_PLACEMENT_3D ( 'NONE', #8333, #10823, #3881 ) ;
#8261=VERTEX_POINT ( 'NONE', #17818 ) ;
#8264=LINE ( 'NONE', #18046, #9722 ) ;
#8268=ADVANCED_FACE ( 'NONE', ( #14985 ), #7949, .T. ) ;
#8269=CARTESIAN_POINT ( 'NONE',  ( -2.500000000000000000, 9.199999999999999289, 1.600000000000000089 ) ) ;
#8270=DIRECTION ( 'NONE',  ( -6.083413833562510128E-16, 1.520853458390629997E-16, -1.000000000000000000 ) ) ;
#8273=CARTESIAN_POINT ( 'NONE',  ( 1.899999999999999911, 11.29999999999999893, 1.600000000000000089 ) ) ;
#8279=ORIENTED_EDGE ( 'NONE', *, *, #15234, .F. ) ;
#8282=VERTEX_POINT ( 'NONE', #4968 ) ;
#8286=EDGE_CURVE ( 'NONE', #1735, #11364, #3762, .T. ) ;
#8297=EDGE_CURVE ( 'NONE', #14464, #17808, #7843, .T. ) ;
#8310=PLANE ( 'NONE',  #11179 ) ;
#8319=DIRECTION ( 'NONE',  ( -1.000000000000000000, 1.073215590470990073E-14, -1.110223024625159992E-16 ) ) ;
#8320=ORIENTED_EDGE ( 'NONE', *, *, #8581, .T. ) ;
#8322=SHAPE_REPRESENTATION ( 'Switch Metal Shield Frame', ( #17681 ), #12094 ) ;
#8327=ORIENTED_EDGE ( 'NONE', *, *, #11796, .T. ) ;
#8330=ORIENTED_EDGE ( 'NONE', *, *, #1555, .T. ) ;
#8331=EDGE_CURVE ( 'NONE', #10942, #14423, #9403, .T. ) ;
#8333=CARTESIAN_POINT ( 'NONE',  ( -1.000000000000000000, 5.799999999999999822, 7.700000000000000178 ) ) ;
#8334=EDGE_LOOP ( 'NONE', ( #17219, #2234, #17813, #1689, #5079, #5962, #12297, #6976, #3750, #9786, #8320, #10748, #13859, #7805, #1949, #923, #10648, #15516, #6211, #2163, #15395, #8526, #10293, #15297 ) ) ;
#8344=VERTEX_POINT ( 'NONE', #17333 ) ;
#8346=ORIENTED_EDGE ( 'NONE', *, *, #782, .T. ) ;
#8352=ORIENTED_EDGE ( 'NONE', *, *, #8922, .T. ) ;
#8354=FACE_OUTER_BOUND ( 'NONE', #5218, .T. ) ;
#8356=DIRECTION ( 'NONE',  ( 6.083413833562498788E-17, 3.041706916781249394E-17, 1.000000000000000000 ) ) ;
#8359=CARTESIAN_POINT ( 'NONE',  ( -1.899999999999999911, 10.00000000000000000, 5.075305255429290705E-16 ) ) ;
#8365=AXIS2_PLACEMENT_3D ( 'NONE', #18016, #5363, #18101 ) ;
#8381=ORIENTED_EDGE ( 'NONE', *, *, #13906, .F. ) ;
#8382=DIRECTION ( 'NONE',  ( -7.340317518182859527E-17, 0.000000000000000000, -1.000000000000000000 ) ) ;
#8386=CARTESIAN_POINT ( 'NONE',  ( -0.03000000000000110217, 11.40000000000000036, 7.649999999999999467 ) ) ;
#8389=DIRECTION ( 'NONE',  ( -1.101047627727429853E-16, 0.000000000000000000, 1.000000000000000000 ) ) ;
#8391=EDGE_CURVE ( 'NONE', #17750, #10646, #675, .T. ) ;
#8393=LINE ( 'NONE', #14029, #13512 ) ;
#8395=EDGE_LOOP ( 'NONE', ( #5595, #287, #1909, #15814 ) ) ;
#8398=DIRECTION ( 'NONE',  ( -1.224646799147341128E-16, -1.000000000000000000, 0.000000000000000000 ) ) ;
#8402=ADVANCED_FACE ( 'NONE', ( #9477 ), #17875, .T. ) ;
#8407=EDGE_CURVE ( 'NONE', #16536, #1995, #10580, .T. ) ;
#8412=LINE ( 'NONE', #9983, #6 ) ;
#8417=CARTESIAN_POINT ( 'NONE',  ( 1.889999999999999902, 8.500000000000000000, 0.6099999999999999867 ) ) ;
#8418=DIRECTION ( 'NONE',  ( -2.986159789035700404E-15, 1.110223024625159992E-16, 1.000000000000000000 ) ) ;
#8425=CARTESIAN_POINT ( 'NONE',  ( 1.000000000000000000, 6.400000000000000355, 7.700000000000000178 ) ) ;
#8431=ORIENTED_EDGE ( 'NONE', *, *, #10600, .F. ) ;
#8433=VERTEX_POINT ( 'NONE', #11394 ) ;
#8434=VERTEX_POINT ( 'NONE', #17117 ) ;
#8440=DIRECTION ( 'NONE',  ( 6.083413833562510128E-16, -1.647588903766454767E-16, 1.000000000000000000 ) ) ;
#8442=LINE ( 'NONE', #1404, #14090 ) ;
#8450=CARTESIAN_POINT ( 'NONE',  ( 1.000000000000000000, 5.799999999999999822, 8.300000000000000711 ) ) ;
#8460=ORIENTED_EDGE ( 'NONE', *, *, #6216, .F. ) ;
#8466=ADVANCED_FACE ( 'NONE', ( #3060 ), #7412, .T. ) ;
#8472=EDGE_CURVE ( 'NONE', #14839, #2212, #7352, .T. ) ;
#8473=CARTESIAN_POINT ( 'NONE',  ( -1.899999999999999911, 11.15000000000000036, 7.990820364436479856E-16 ) ) ;
#8475=DIRECTION ( 'NONE',  ( -0.6614378277661479011, 8.100277186087908528E-17, -0.7499999999999997780 ) ) ;
#8477=AXIS2_PLACEMENT_3D ( 'NONE', #10202, #8833, #15781 ) ;
#8478=DIRECTION ( 'NONE',  ( 1.000000000000000000, -1.445602896647339114E-15, 2.891205793294678228E-15 ) ) ;
#8482=DIRECTION ( 'NONE',  ( 1.000000000000000000, -2.960594732333750117E-16, 0.000000000000000000 ) ) ;
#8488=ADVANCED_FACE ( 'NONE', ( #10101 ), #15753, .T. ) ;
#8489=VECTOR ( 'NONE', #6001, 1000.000000000000000 ) ;
#8494=AXIS2_PLACEMENT_3D ( 'NONE', #11727, #10341, #14514 ) ;
#8501=VERTEX_POINT ( 'NONE', #14445 ) ;
#8502=VECTOR ( 'NONE', #8756, 1000.000000000000000 ) ;
#8504=VERTEX_POINT ( 'NONE', #6013 ) ;
#8505=DIRECTION ( 'NONE',  ( -1.000000000000000000, 1.480297366166879989E-15, 0.000000000000000000 ) ) ;
#8506=CARTESIAN_POINT ( 'NONE',  ( -2.500000000000000000, 10.00000000000000000, 7.654042494670959579E-16 ) ) ;
#8508=AXIS2_PLACEMENT_3D ( 'NONE', #1680, #7329, #9837 ) ;
#8512=EDGE_CURVE ( 'NONE', #2252, #2042, #12873, .T. ) ;
#8518=AXIS2_PLACEMENT_3D ( 'NONE', #16445, #3382, #7743 ) ;
#8524=AXIS2_PLACEMENT_3D ( 'NONE', #5154, #9032, #6549 ) ;
#8525=VECTOR ( 'NONE', #8107, 1000.000000000000000 ) ;
#8526=ORIENTED_EDGE ( 'NONE', *, *, #211, .T. ) ;
#8527=CARTESIAN_POINT ( 'NONE',  ( -1.899999999999999911, 11.25000000000000000, 7.649999999999999467 ) ) ;
#8528=VERTEX_POINT ( 'NONE', #2791 ) ;
#8529=CIRCLE ( 'NONE', #10283, 0.6100000000000000977 ) ;
#8530=CARTESIAN_POINT ( 'NONE',  ( 1.000000000000000000, 5.799999999999999822, 7.700000000000000178 ) ) ;
#8534=VECTOR ( 'NONE', #5519, 1000.000000000000000 ) ;
#8539=VECTOR ( 'NONE', #5632, 1000.000000000000000 ) ;
#8541=CIRCLE ( 'NONE', #1732, 0.01000000000000002623 ) ;
#8542=LINE ( 'NONE', #8359, #11993 ) ;
#8544=DIRECTION ( 'NONE',  ( 2.986159789035700404E-15, -1.110223024625159992E-16, -1.000000000000000000 ) ) ;
#8551=ORIENTED_EDGE ( 'NONE', *, *, #6092, .F. ) ;
#8554=ORIENTED_EDGE ( 'NONE', *, *, #4173, .F. ) ;
#8555=VECTOR ( 'NONE', #344, 1000.000000000000000 ) ;
#8566=CARTESIAN_POINT ( 'NONE',  ( -1.889999999999999902, 7.299999999999999822, 1.327597122149119839E-15 ) ) ;
#8571=DIRECTION ( 'NONE',  ( 0.000000000000000000, 0.000000000000000000, -1.000000000000000000 ) ) ;
#8572=VERTEX_POINT ( 'NONE', #189 ) ;
#8581=EDGE_CURVE ( 'NONE', #13271, #14130, #7060, .T. ) ;
#8582=ORIENTED_EDGE ( 'NONE', *, *, #1112, .F. ) ;
#8587=LINE ( 'NONE', #15260, #5825 ) ;
#8590=EDGE_CURVE ( 'NONE', #13297, #13575, #5749, .T. ) ;
#8595=DIRECTION ( 'NONE',  ( 0.000000000000000000, 1.000000000000000000, 0.000000000000000000 ) ) ;
#8601=EDGE_CURVE ( 'NONE', #9483, #3235, #7319, .T. ) ;
#8605=VECTOR ( 'NONE', #14595, 1000.000000000000000 ) ;
#8616=DIRECTION ( 'NONE',  ( 5.421010862427519212E-16, 1.000000000000000000, 0.000000000000000000 ) ) ;
#8619=VERTEX_POINT ( 'NONE', #9148 ) ;
#8623=DIRECTION ( 'NONE',  ( 1.480297366166879989E-15, 2.476791224480679883E-30, 1.000000000000000000 ) ) ;
#8625=DIRECTION ( 'NONE',  ( -1.000000000000000000, 2.843808977011158816E-15, -3.554761221263948421E-15 ) ) ;
#8626=ORIENTED_EDGE ( 'NONE', *, *, #14858, .T. ) ;
#8628=CARTESIAN_POINT ( 'NONE',  ( 1.889999999999999902, 3.500000000000000000, 0.6099999999999999867 ) ) ;
#8630=PLANE ( 'NONE',  #12601 ) ;
#8638=ORIENTED_EDGE ( 'NONE', *, *, #2702, .T. ) ;
#8639=EDGE_CURVE ( 'NONE', #16536, #15044, #728, .T. ) ;
#8642=EDGE_LOOP ( 'NONE', ( #9330, #1762, #6989, #2020 ) ) ;
#8643=ORIENTED_EDGE ( 'NONE', *, *, #3137, .F. ) ;
#8651=DIRECTION ( 'NONE',  ( -3.042833474898580443E-15, 3.289549702593060178E-16, 1.000000000000000000 ) ) ;
#8654=EDGE_LOOP ( 'NONE', ( #17139, #9582, #16737, #14534 ) ) ;
#8659=AXIS2_PLACEMENT_3D ( 'NONE', #8838, #10312, #10574 ) ;
#8666=LINE ( 'NONE', #3107, #8502 ) ;
#8669=EDGE_CURVE ( 'NONE', #6244, #15780, #12385, .T. ) ;
#8670=PLANE ( 'NONE',  #7365 ) ;
#8673=DIRECTION ( 'NONE',  ( -1.000000000000000000, 2.220446049250315053E-16, 6.049014748177260544E-16 ) ) ;
#8677=ORIENTED_EDGE ( 'NONE', *, *, #11291, .T. ) ;
#8678=DIRECTION ( 'NONE',  ( 6.049014748177260544E-16, -2.493473113004680074E-16, 1.000000000000000000 ) ) ;
#8682=EDGE_CURVE ( 'NONE', #9295, #12680, #14532, .T. ) ;
#8688=EDGE_CURVE ( 'NONE', #13417, #2212, #9241, .T. ) ;
#8697=LINE ( 'NONE', #1661, #1958 ) ;
#8698=ADVANCED_FACE ( 'NONE', ( #1930 ), #7497, .T. ) ;
#8701=DIRECTION ( 'NONE',  ( -1.264200168623419965E-31, -8.540177112501209562E-17, 1.000000000000000000 ) ) ;
#8703=DIRECTION ( 'NONE',  ( -1.853875224168160112E-15, -1.000000000000000000, -2.960594732333760372E-15 ) ) ;
#8711=EDGE_CURVE ( 'NONE', #14368, #6950, #15931, .T. ) ;
#8712=CARTESIAN_POINT ( 'NONE',  ( 0.03000000000000110217, 11.40000000000000036, 1.600000000000000089 ) ) ;
#8713=LINE ( 'NONE', #9922, #12974 ) ;
#8719=VERTEX_POINT ( 'NONE', #11936 ) ;
#8725=ORIENTED_EDGE ( 'NONE', *, *, #1005, .T. ) ;
#8727=SHAPE_DEFINITION_REPRESENTATION ( #6843, #8322 ) ;
#8730=LINE ( 'NONE', #11687, #7909 ) ;
#8743=DIRECTION ( 'NONE',  ( -1.000000000000000000, 3.700743415417190112E-16, 7.273661547324619914E-16 ) ) ;
#8747=PLANE ( 'NONE',  #17155 ) ;
#8749=ORIENTED_EDGE ( 'NONE', *, *, #7009, .F. ) ;
#8752=CIRCLE ( 'NONE', #4015, 0.09999999999999939493 ) ;
#8756=DIRECTION ( 'NONE',  ( -5.551115123125780730E-16, -1.000000000000000000, 0.000000000000000000 ) ) ;
#8758=ORIENTED_EDGE ( 'NONE', *, *, #8918, .T. ) ;
#8760=EDGE_CURVE ( 'NONE', #18244, #10646, #8541, .T. ) ;
#8765=CARTESIAN_POINT ( 'NONE',  ( -0.5372984490435469551, 4.599999999999999645, 8.300000000000000711 ) ) ;
#8767=EDGE_LOOP ( 'NONE', ( #7357, #3844, #12593, #15204, #1155, #15124, #2773, #702 ) ) ;
#8774=DIRECTION ( 'NONE',  ( -1.480297366166879989E-15, -1.000000000000000000, 1.314768175368350090E-30 ) ) ;
#8783=AXIS2_PLACEMENT_3D ( 'NONE', #12840, #4037, #2566 ) ;
#8786=CIRCLE ( 'NONE', #2875, 0.3499999999999996447 ) ;
#8787=DIRECTION ( 'NONE',  ( 1.000000000000000000, -1.480297366166879989E-15, 0.000000000000000000 ) ) ;
#8790=VERTEX_POINT ( 'NONE', #18024 ) ;
#8791=DIRECTION ( 'NONE',  ( -1.142385477618690234E-14, 1.110223024625159992E-16, -1.000000000000000000 ) ) ;
#8796=EDGE_CURVE ( 'NONE', #5515, #16687, #5275, .T. ) ;
#8801=CARTESIAN_POINT ( 'NONE',  ( 4.898587196589409994E-17, 0.1000000000000000056, 8.300000000000000711 ) ) ;
#8803=CARTESIAN_POINT ( 'NONE',  ( 1.875000000000000000, 0.7500000000000000000, 7.700000000000000178 ) ) ;
#8811=DIRECTION ( 'NONE',  ( -0.000000000000000000, 1.000000000000000000, 0.000000000000000000 ) ) ;
#8819=EDGE_LOOP ( 'NONE', ( #10820, #8053, #14023, #4635 ) ) ;
#8820=ORIENTED_EDGE ( 'NONE', *, *, #13839, .F. ) ;
#8821=FACE_OUTER_BOUND ( 'NONE', #285, .T. ) ;
#8828=VECTOR ( 'NONE', #4523, 1000.000000000000000 ) ;
#8830=PLANE ( 'NONE',  #15896 ) ;
#8833=DIRECTION ( 'NONE',  ( 5.473822126269209268E-48, 1.000000000000000000, 1.332267629550190018E-15 ) ) ;
#8838=CARTESIAN_POINT ( 'NONE',  ( -1.899999999999999911, 9.199999999999999289, 1.600000000000000089 ) ) ;
#8842=ORIENTED_EDGE ( 'NONE', *, *, #6220, .F. ) ;
#8847=DIRECTION ( 'NONE',  ( 0.000000000000000000, 1.774290917998389804E-45, -1.000000000000000000 ) ) ;
#8850=AXIS2_PLACEMENT_3D ( 'NONE', #12631, #18258, #11250 ) ;
#8856=ORIENTED_EDGE ( 'NONE', *, *, #3172, .T. ) ;
#8860=LINE ( 'NONE', #2085, #3948 ) ;
#8865=VERTEX_POINT ( 'NONE', #16380 ) ;
#8867=CARTESIAN_POINT ( 'NONE',  ( 1.899999999999999911, 11.29999999999999893, 1.600000000000000089 ) ) ;
#8875=FACE_OUTER_BOUND ( 'NONE', #6499, .T. ) ;
#8882=VECTOR ( 'NONE', #8999, 1000.000000000000000 ) ;
#8891=CARTESIAN_POINT ( 'NONE',  ( 0.8740908734716299477, 4.154758922476410099, 8.300000000000000711 ) ) ;
#8892=AXIS2_PLACEMENT_3D ( 'NONE', #7742, #10612, #6625 ) ;
#8904=ORIENTED_EDGE ( 'NONE', *, *, #3196, .F. ) ;
#8905=CARTESIAN_POINT ( 'NONE',  ( -2.500000000000000000, 11.29999999999999893, 1.600000000000000089 ) ) ;
#8913=ADVANCED_FACE ( 'NONE', ( #2419 ), #6567, .T. ) ;
#8914=DIRECTION ( 'NONE',  ( 1.000000000000000000, -1.445602896647339114E-15, 2.891205793294678228E-15 ) ) ;
#8918=EDGE_CURVE ( 'NONE', #11214, #9511, #9710, .T. ) ;
#8921=DIRECTION ( 'NONE',  ( 1.000000000000000000, 0.000000000000000000, 0.000000000000000000 ) ) ;
#8922=EDGE_CURVE ( 'NONE', #15242, #18244, #17381, .T. ) ;
#8923=FACE_OUTER_BOUND ( 'NONE', #2736, .T. ) ;
#8924=EDGE_CURVE ( 'NONE', #2205, #15023, #11791, .T. ) ;
#8927=LINE ( 'NONE', #1718, #2683 ) ;
#8933=PLANE ( 'NONE',  #12940 ) ;
#8940=LINE ( 'NONE', #14237, #11788 ) ;
#8943=ORIENTED_EDGE ( 'NONE', *, *, #4613, .T. ) ;
#8945=DIRECTION ( 'NONE',  ( 1.216682766712499758E-16, 3.041706916781249394E-17, 1.000000000000000000 ) ) ;
#8946=DIRECTION ( 'NONE',  ( 0.000000000000000000, 0.000000000000000000, -1.000000000000000000 ) ) ;
#8949=ORIENTED_EDGE ( 'NONE', *, *, #6467, .T. ) ;
#8951=ORIENTED_EDGE ( 'NONE', *, *, #14397, .T. ) ;
#8955=CARTESIAN_POINT ( 'NONE',  ( 1.875000000000000000, 0.7500000000000000000, 7.700000000000000178 ) ) ;
#8964=DIRECTION ( 'NONE',  ( 1.000000000000000000, 0.000000000000000000, 0.000000000000000000 ) ) ;
#8966=DIRECTION ( 'NONE',  ( 6.123233995736759873E-17, -6.123233995736759873E-17, 1.000000000000000000 ) ) ;
#8967=ORIENTED_EDGE ( 'NONE', *, *, #15168, .T. ) ;
#8973=LINE ( 'NONE', #7683, #7320 ) ;
#8990=PLANE ( 'NONE',  #17945 ) ;
#8992=CARTESIAN_POINT ( 'NONE',  ( -2.616666666666669805, 1.330536610280860259E-16, 4.000000000000000000 ) ) ;
#8999=DIRECTION ( 'NONE',  ( 0.000000000000000000, 0.000000000000000000, 1.000000000000000000 ) ) ;
#9000=EDGE_CURVE ( 'NONE', #5973, #7773, #8713, .T. ) ;
#9004=ORIENTED_EDGE ( 'NONE', *, *, #11474, .F. ) ;
#9015=AXIS2_PLACEMENT_3D ( 'NONE', #10021, #11317, #14077 ) ;
#9020=DIRECTION ( 'NONE',  ( 1.000000000000000000, -2.220446049250309876E-16, -6.123233995736759873E-17 ) ) ;
#9021=CARTESIAN_POINT ( 'NONE',  ( -1.875000000000000000, 11.25000000000000000, 8.300000000000000711 ) ) ;
#9024=ORIENTED_EDGE ( 'NONE', *, *, #17656, .F. ) ;
#9025=LINE ( 'NONE', #6173, #1510 ) ;
#9026=CARTESIAN_POINT ( 'NONE',  ( -1.899999999999999911, 7.299999999999999822, 0.6099999999999999867 ) ) ;
#9028=EDGE_CURVE ( 'NONE', #7970, #5991, #11669, .T. ) ;
#9029=ORIENTED_EDGE ( 'NONE', *, *, #10055, .F. ) ;
#9032=DIRECTION ( 'NONE',  ( 1.059690869644410208E-14, 1.000000000000000000, -1.041146930477340028E-32 ) ) ;
#9033=LINE ( 'NONE', #444, #7872 ) ;
#9039=DIRECTION ( 'NONE',  ( 1.000000000000000000, 0.000000000000000000, 0.000000000000000000 ) ) ;
#9046=VERTEX_POINT ( 'NONE', #8891 ) ;
#9048=DIRECTION ( 'NONE',  ( -4.157615153618229646E-15, 1.000000000000000000, 1.972152263052530214E-30 ) ) ;
#9052=CARTESIAN_POINT ( 'NONE',  ( -2.500000000000000000, 0.4000000000000000222, 4.000000000000000000 ) ) ;
#9055=AXIS2_PLACEMENT_3D ( 'NONE', #12758, #8319, #2761 ) ;
#9060=CARTESIAN_POINT ( 'NONE',  ( 1.899999999999999911, 11.25000000000000000, 7.649999999999999467 ) ) ;
#9063=ORIENTED_EDGE ( 'NONE', *, *, #16035, .F. ) ;
#9067=ORIENTED_EDGE ( 'NONE', *, *, #2367, .F. ) ;
#9068=ORIENTED_EDGE ( 'NONE', *, *, #11229, .T. ) ;
#9069=DIRECTION ( 'NONE',  ( 0.000000000000000000, 0.000000000000000000, -1.000000000000000000 ) ) ;
#9078=ORIENTED_EDGE ( 'NONE', *, *, #11740, .F. ) ;
#9086=EDGE_LOOP ( 'NONE', ( #11886, #767, #10376, #12578 ) ) ;
#9091=FACE_OUTER_BOUND ( 'NONE', #8395, .T. ) ;
#9094=VERTEX_POINT ( 'NONE', #2105 ) ;
#9095=AXIS2_PLACEMENT_3D ( 'NONE', #9756, #12896, #41 ) ;
#9098=DIRECTION ( 'NONE',  ( 1.000000000000000000, -1.224646799147350002E-16, 0.000000000000000000 ) ) ;
#9101=VECTOR ( 'NONE', #5173, 1000.000000000000000 ) ;
#9106=PLANE ( 'NONE',  #4368 ) ;
#9108=CIRCLE ( 'NONE', #15951, 0.01000000000000002623 ) ;
#9112=ORIENTED_EDGE ( 'NONE', *, *, #17826, .T. ) ;
#9113=DIRECTION ( 'NONE',  ( -2.168404344971021884E-15, 1.000000000000000000, 0.000000000000000000 ) ) ;
#9115=EDGE_CURVE ( 'NONE', #7642, #1091, #17207, .T. ) ;
#9118=ORIENTED_EDGE ( 'NONE', *, *, #13793, .T. ) ;
#9126=FACE_OUTER_BOUND ( 'NONE', #5014, .T. ) ;
#9128=CARTESIAN_POINT ( 'NONE',  ( -1.899999999999999911, 2.000000000000000000, 1.600000000000000089 ) ) ;
#9129=CARTESIAN_POINT ( 'NONE',  ( 1.899999999999999911, 2.799999999999999822, 1.600000000000000089 ) ) ;
#9131=CARTESIAN_POINT ( 'NONE',  ( 2.500000000000000000, 7.299999999999999822, 1.600000000000000089 ) ) ;
#9134=ORIENTED_EDGE ( 'NONE', *, *, #1354, .T. ) ;
#9135=AXIS2_PLACEMENT_3D ( 'NONE', #18154, #6983, #2644 ) ;
#9138=FACE_OUTER_BOUND ( 'NONE', #11639, .T. ) ;
#9139=CARTESIAN_POINT ( 'NONE',  ( 2.241103642439659443E-15, 9.099999999999999645, 7.700000000000000178 ) ) ;
#9144=VERTEX_POINT ( 'NONE', #384 ) ;
#9148=CARTESIAN_POINT ( 'NONE',  ( 1.899999999999999911, 1.734980836410520254E-17, 3.278889744907200310 ) ) ;
#9151=ORIENTED_EDGE ( 'NONE', *, *, #16718, .T. ) ;
#9154=CYLINDRICAL_SURFACE ( 'NONE', #5207, 0.1000000000000000472 ) ;
#9164=LINE ( 'NONE', #11778, #16843 ) ;
#9170=CARTESIAN_POINT ( 'NONE',  ( 0.5372984490435490645, 4.250000000000000000, 8.300000000000000711 ) ) ;
#9172=CARTESIAN_POINT ( 'NONE',  ( -2.500000000000000000, 3.500000000000000000, 0.6099999999999999867 ) ) ;
#9179=CARTESIAN_POINT ( 'NONE',  ( 2.500000000000000000, 11.15000000000000036, -3.616154994493369454E-16 ) ) ;
#9186=ORIENTED_EDGE ( 'NONE', *, *, #13771, .T. ) ;
#9189=DIRECTION ( 'NONE',  ( -1.059337802663170094E-14, -1.000000000000000000, 0.000000000000000000 ) ) ;
#9192=VERTEX_POINT ( 'NONE', #17739 ) ;
#9195=DIRECTION ( 'NONE',  ( -1.142385477618690076E-14, 1.110223024625153952E-16, -1.000000000000000000 ) ) ;
#9198=DIRECTION ( 'NONE',  ( 1.000000000000000000, 0.000000000000000000, 0.000000000000000000 ) ) ;
#9199=DIRECTION ( 'NONE',  ( 0.000000000000000000, 0.000000000000000000, 1.000000000000000000 ) ) ;
#9202=CARTESIAN_POINT ( 'NONE',  ( -1.199999999999880052, 11.40000000000000036, -2.399999999999999911 ) ) ;
#9205=VERTEX_POINT ( 'NONE', #12391 ) ;
#9208=FACE_OUTER_BOUND ( 'NONE', #5544, .T. ) ;
#9211=ORIENTED_EDGE ( 'NONE', *, *, #8237, .F. ) ;
#9212=ORIENTED_EDGE ( 'NONE', *, *, #9697, .F. ) ;
#9215=CARTESIAN_POINT ( 'NONE',  ( 2.500000000000000000, 2.799999999999999822, 1.600000000000000089 ) ) ;
#9219=DIRECTION ( 'NONE',  ( 0.000000000000000000, 0.000000000000000000, 1.000000000000000000 ) ) ;
#9222=FACE_OUTER_BOUND ( 'NONE', #11176, .T. ) ;
#9230=ORIENTED_EDGE ( 'NONE', *, *, #14906, .F. ) ;
#9237=VERTEX_POINT ( 'NONE', #9429 ) ;
#9241=LINE ( 'NONE', #1853, #7946 ) ;
#9245=ADVANCED_FACE ( 'NONE', ( #5067 ), #6454, .T. ) ;
#9260=ORIENTED_EDGE ( 'NONE', *, *, #3574, .T. ) ;
#9266=CARTESIAN_POINT ( 'NONE',  ( -1.889999999999999902, 7.299999999999999822, 0.5999999999999999778 ) ) ;
#9267=ORIENTED_EDGE ( 'NONE', *, *, #3469, .F. ) ;
#9272=CARTESIAN_POINT ( 'NONE',  ( -1.850000000000000089, 11.25000000000000000, 7.700000000000000178 ) ) ;
#9274=FACE_OUTER_BOUND ( 'NONE', #1216, .T. ) ;
#9288=DIRECTION ( 'NONE',  ( 0.000000000000000000, 0.000000000000000000, 1.000000000000000000 ) ) ;
#9291=DIRECTION ( 'NONE',  ( -4.898587196589410857E-16, -1.000000000000000000, 3.081487911019575175E-31 ) ) ;
#9293=CARTESIAN_POINT ( 'NONE',  ( 1.889999999999999902, 7.900000000000000355, 3.000000000000000000 ) ) ;
#9295=VERTEX_POINT ( 'NONE', #9604 ) ;
#9296=DIRECTION ( 'NONE',  ( 1.000000000000000000, 3.700743415417199972E-16, 0.000000000000000000 ) ) ;
#9300=ORIENTED_EDGE ( 'NONE', *, *, #14858, .F. ) ;
#9301=LINE ( 'NONE', #10703, #14685 ) ;
#9310=ORIENTED_EDGE ( 'NONE', *, *, #14259, .T. ) ;
#9314=CARTESIAN_POINT ( 'NONE',  ( 1.000000000000000000, 6.400000000000000355, 7.700000000000000178 ) ) ;
#9315=DIRECTION ( 'NONE',  ( -3.416070845000479880E-16, -1.000000000000000000, -5.978123978750840407E-16 ) ) ;
#9318=DIRECTION ( 'NONE',  ( 0.000000000000000000, -1.000000000000000000, 0.000000000000000000 ) ) ;
#9325=DIRECTION ( 'NONE',  ( 7.300096600275009393E-16, -1.215710299141969852E-31, 1.000000000000000000 ) ) ;
#9330=ORIENTED_EDGE ( 'NONE', *, *, #6169, .F. ) ;
#9335=ORIENTED_EDGE ( 'NONE', *, *, #7444, .T. ) ;
#9349=DIRECTION ( 'NONE',  ( 1.000000000000000000, -7.401486830834380223E-16, 0.000000000000000000 ) ) ;
#9361=DIRECTION ( 'NONE',  ( 8.326672684688679970E-16, 0.000000000000000000, 1.000000000000000000 ) ) ;
#9363=ORIENTED_EDGE ( 'NONE', *, *, #4173, .T. ) ;
#9365=DIRECTION ( 'NONE',  ( -0.000000000000000000, 1.000000000000000000, 0.000000000000000000 ) ) ;
#9367=CIRCLE ( 'NONE', #12032, 0.4000000000000001887 ) ;
#9369=EDGE_CURVE ( 'NONE', #15033, #229, #15262, .T. ) ;
#9370=EDGE_LOOP ( 'NONE', ( #14755, #7676, #14865, #8279 ) ) ;
#9373=EDGE_CURVE ( 'NONE', #11111, #1650, #17520, .T. ) ;
#9378=VECTOR ( 'NONE', #17649, 1000.000000000000000 ) ;
#9381=DIRECTION ( 'NONE',  ( 0.000000000000000000, -1.000000000000000000, 0.000000000000000000 ) ) ;
#9386=AXIS2_PLACEMENT_3D ( 'NONE', #12981, #8811, #13068 ) ;
#9393=AXIS2_PLACEMENT_3D ( 'NONE', #9673, #15244, #2545 ) ;
#9394=CARTESIAN_POINT ( 'NONE',  ( -1.899999999999999911, 4.700000000000000178, 0.6099999999999999867 ) ) ;
#9397=DIRECTION ( 'NONE',  ( 0.000000000000000000, 0.000000000000000000, 1.000000000000000000 ) ) ;
#9400=ORIENTED_EDGE ( 'NONE', *, *, #11740, .T. ) ;
#9401=CARTESIAN_POINT ( 'NONE',  ( 1.899999999999999911, 0.7500000000000000000, 7.649999999999999467 ) ) ;
#9403=CIRCLE ( 'NONE', #11773, 0.3499999999999999778 ) ;
#9404=VECTOR ( 'NONE', #18037, 1000.000000000000000 ) ;
#9405=EDGE_CURVE ( 'NONE', #2627, #15044, #10494, .T. ) ;
#9421=AXIS2_PLACEMENT_3D ( 'NONE', #15376, #13707, #2680 ) ;
#9423=CARTESIAN_POINT ( 'NONE',  ( 0.5372984490435490645, 4.599999999999999645, 7.700000000000000178 ) ) ;
#9428=CIRCLE ( 'NONE', #14144, 0.4166666666666670737 ) ;
#9429=CARTESIAN_POINT ( 'NONE',  ( -0.5291502622129179434, 0.1000000000000000056, 7.700000000000000178 ) ) ;
#9433=LINE ( 'NONE', #628, #3795 ) ;
#9435=VECTOR ( 'NONE', #10177, 1000.000000000000000 ) ;
#9438=CARTESIAN_POINT ( 'NONE',  ( -1.899999999999999911, 0.7500000000000000000, 7.649999999999999467 ) ) ;
#9443=DIRECTION ( 'NONE',  ( 0.000000000000000000, 1.000000000000000000, 1.359631073446889961E-32 ) ) ;
#9445=EDGE_LOOP ( 'NONE', ( #14036, #5366, #4224, #8330, #12069, #13616 ) ) ;
#9447=LINE ( 'NONE', #8150, #10888 ) ;
#9452=EDGE_CURVE ( 'NONE', #8790, #11991, #14501, .T. ) ;
#9455=LINE ( 'NONE', #3977, #6753 ) ;
#9466=CARTESIAN_POINT ( 'NONE',  ( 1.875000000000000000, -2.296212748401290437E-16, 7.700000000000000178 ) ) ;
#9469=ADVANCED_FACE ( 'NONE', ( #6062 ), #1900, .F. ) ;
#9470=AXIS2_PLACEMENT_3D ( 'NONE', #350, #1643, #1907 ) ;
#9475=ORIENTED_EDGE ( 'NONE', *, *, #15981, .F. ) ;
#9477=FACE_OUTER_BOUND ( 'NONE', #14070, .T. ) ;
#9478=PLANE ( 'NONE',  #44 ) ;
#9483=VERTEX_POINT ( 'NONE', #17344 ) ;
#9487=ADVANCED_FACE ( 'NONE', ( #2178 ), #3736, .T. ) ;
#9490=CARTESIAN_POINT ( 'NONE',  ( -1.289999999999999813, 7.900000000000014566, 0.6000000000000020872 ) ) ;
#9492=EDGE_CURVE ( 'NONE', #2762, #6171, #10033, .T. ) ;
#9494=ADVANCED_FACE ( 'NONE', ( #2267 ), #10595, .T. ) ;
#9495=FACE_BOUND ( 'NONE', #8767, .T. ) ;
#9498=CYLINDRICAL_SURFACE ( 'NONE', #3919, 1.000000000000000000 ) ;
#9502=DIRECTION ( 'NONE',  ( 0.000000000000000000, -1.000000000000000000, -6.123233995736769734E-17 ) ) ;
#9504=DIRECTION ( 'NONE',  ( -4.794417550286630491E-31, 1.000000000000000000, 1.774290917998389804E-45 ) ) ;
#9505=CARTESIAN_POINT ( 'NONE',  ( -1.889999999999999902, 8.500000000000000000, 2.664535259100379641E-15 ) ) ;
#9507=ORIENTED_EDGE ( 'NONE', *, *, #983, .T. ) ;
#9508=CARTESIAN_POINT ( 'NONE',  ( -1.899999999999999911, 8.500000000000000000, 0.6099999999999999867 ) ) ;
#9509=LINE ( 'NONE', #4214, #4092 ) ;
#9511=VERTEX_POINT ( 'NONE', #6522 ) ;
#9529=CARTESIAN_POINT ( 'NONE',  ( 1.899999999999999911, 4.700000000000000178, 0.6099999999999999867 ) ) ;
#9534=VERTEX_POINT ( 'NONE', #783 ) ;
#9547=ORIENTED_EDGE ( 'NONE', *, *, #4613, .F. ) ;
#9553=DIRECTION ( 'NONE',  ( 0.000000000000000000, 0.000000000000000000, 1.000000000000000000 ) ) ;
#9555=DIRECTION ( 'NONE',  ( 8.971499188890150495E-16, 0.000000000000000000, 1.000000000000000000 ) ) ;
#9556=DIRECTION ( 'NONE',  ( -1.000000000000000000, -4.336808689942016947E-15, 1.084202172485504276E-14 ) ) ;
#9557=ORIENTED_EDGE ( 'NONE', *, *, #8132, .T. ) ;
#9559=DIRECTION ( 'NONE',  ( 4.707398764864359324E-46, -1.000000000000000000, -2.220446049250309876E-16 ) ) ;
#9567=VERTEX_POINT ( 'NONE', #2374 ) ;
#9569=VECTOR ( 'NONE', #11825, 1000.000000000000000 ) ;
#9573=ORIENTED_EDGE ( 'NONE', *, *, #14566, .T. ) ;
#9578=CARTESIAN_POINT ( 'NONE',  ( 2.500000000000000000, 7.299999999999999822, 1.600000000000000089 ) ) ;
#9582=ORIENTED_EDGE ( 'NONE', *, *, #1005, .F. ) ;
#9583=CARTESIAN_POINT ( 'NONE',  ( 2.500000000000000000, 3.500000000000000000, 0.6099999999999999867 ) ) ;
#9584=CARTESIAN_POINT ( 'NONE',  ( -1.889999999999999902, 3.500000000000000000, -6.080658959840581147E-16 ) ) ;
#9585=EDGE_CURVE ( 'NONE', #11828, #18124, #12090, .T. ) ;
#9593=ADVANCED_FACE ( 'NONE', ( #16338 ), #3642, .T. ) ;
#9601=CARTESIAN_POINT ( 'NONE',  ( -1.899999999999999911, 0.7211102550927970256, 4.000000000000000000 ) ) ;
#9604=CARTESIAN_POINT ( 'NONE',  ( 1.899999999999999911, 10.00000000000000000, -7.696722944179978717E-16 ) ) ;
#9609=CARTESIAN_POINT ( 'NONE',  ( 1.899999999999999911, 2.000000000000000000, -1.522591576628789972E-15 ) ) ;
#9618=DIRECTION ( 'NONE',  ( 1.060879779086260081E-14, -8.223874256482640091E-16, 1.000000000000000000 ) ) ;
#9621=( LENGTH_UNIT ( ) NAMED_UNIT ( * ) SI_UNIT ( .MILLI., .METRE. ) );
#9623=CARTESIAN_POINT ( 'NONE',  ( 2.500000000000000000, 11.29999999999999893, 1.600000000000000089 ) ) ;
#9628=DIRECTION ( 'NONE',  ( -5.734623061080349568E-18, 0.000000000000000000, 1.000000000000000000 ) ) ;
#9629=PLANE ( 'NONE',  #13000 ) ;
#9637=PRODUCT ( 'Switch Metal Shield Frame', 'Switch Metal Shield Frame', '', ( #10037 ) ) ;
#9644=LINE ( 'NONE', #13992, #12887 ) ;
#9646=DIRECTION ( 'NONE',  ( 1.000000000000000000, 0.000000000000000000, 0.000000000000000000 ) ) ;
#9654=EDGE_LOOP ( 'NONE', ( #11976, #9712, #4424 ) ) ;
#9655=DIRECTION ( 'NONE',  ( -1.000000000000000000, 2.220446049250309876E-16, 0.000000000000000000 ) ) ;
#9662=AXIS2_PLACEMENT_3D ( 'NONE', #5622, #7276, #4402 ) ;
#9664=DIRECTION ( 'NONE',  ( 7.401486830834370362E-16, 0.000000000000000000, 1.000000000000000000 ) ) ;
#9665=DIRECTION ( 'NONE',  ( 0.2800000000000001377, -0.9599999999999999645, 0.000000000000000000 ) ) ;
#9671=CARTESIAN_POINT ( 'NONE',  ( -1.399999999999999911, 5.799999999999999822, 7.700000000000000178 ) ) ;
#9673=CARTESIAN_POINT ( 'NONE',  ( 2.241103642439659443E-15, 9.099999999999999645, 7.700000000000000178 ) ) ;
#9682=DIRECTION ( 'NONE',  ( -1.224646799147341128E-16, -1.000000000000000000, 0.000000000000000000 ) ) ;
#9691=AXIS2_PLACEMENT_3D ( 'NONE', #9128, #712, #2295 ) ;
#9696=EDGE_LOOP ( 'NONE', ( #17531, #12914, #5948, #17969 ) ) ;
#9697=EDGE_CURVE ( 'NONE', #8719, #1735, #7323, .T. ) ;
#9705=ORIENTED_EDGE ( 'NONE', *, *, #11156, .F. ) ;
#9706=ORIENTED_EDGE ( 'NONE', *, *, #5696, .F. ) ;
#9708=DIRECTION ( 'NONE',  ( -9.588835100573269740E-31, 1.000000000000000000, 3.548581835996780230E-45 ) ) ;
#9710=LINE ( 'NONE', #18108, #9101 ) ;
#9711=AXIS2_PLACEMENT_3D ( 'NONE', #17387, #10360, #6277 ) ;
#9712=ORIENTED_EDGE ( 'NONE', *, *, #14472, .T. ) ;
#9714=VECTOR ( 'NONE', #18001, 1000.000000000000000 ) ;
#9718=EDGE_CURVE ( 'NONE', #12326, #8282, #1769, .T. ) ;
#9719=CARTESIAN_POINT ( 'NONE',  ( -1.889999999999999902, 4.700000000000000178, 0.6099999999999999867 ) ) ;
#9722=VECTOR ( 'NONE', #5390, 1000.000000000000000 ) ;
#9737=EDGE_CURVE ( 'NONE', #12188, #2390, #17285, .T. ) ;
#9742=CARTESIAN_POINT ( 'NONE',  ( 2.616666666666660035, -5.805074450128190455E-17, 4.000000000000000000 ) ) ;
#9743=DIRECTION ( 'NONE',  ( 0.000000000000000000, -1.000000000000000000, 0.000000000000000000 ) ) ;
#9744=CARTESIAN_POINT ( 'NONE',  ( 0.000000000000000000, 4.930380657631319405E-32, 8.300000000000000711 ) ) ;
#9752=VERTEX_POINT ( 'NONE', #6081 ) ;
#9755=VERTEX_POINT ( 'NONE', #11465 ) ;
#9756=CARTESIAN_POINT ( 'NONE',  ( 2.616666666666660035, -5.805074450128190455E-17, 4.000000000000000000 ) ) ;
#9764=EDGE_CURVE ( 'NONE', #7970, #5456, #4582, .T. ) ;
#9767=ORIENTED_EDGE ( 'NONE', *, *, #11156, .T. ) ;
#9774=DIRECTION ( 'NONE',  ( 3.315303352997239924E-31, -1.000000000000000000, 8.588360937600549480E-46 ) ) ;
#9779=CARTESIAN_POINT ( 'NONE',  ( -0.5372984490435469551, 4.250000000000000000, 7.700000000000000178 ) ) ;
#9784=DIRECTION ( 'NONE',  ( 4.485749594445080178E-16, 0.000000000000000000, 1.000000000000000000 ) ) ;
#9785=CARTESIAN_POINT ( 'NONE',  ( -1.850000000000000089, 11.25000000000000000, 8.300000000000000711 ) ) ;
#9786=ORIENTED_EDGE ( 'NONE', *, *, #252, .T. ) ;
#9790=VECTOR ( 'NONE', #7134, 1000.000000000000000 ) ;
#9792=DIRECTION ( 'NONE',  ( -1.000000000000000000, 0.000000000000000000, 7.401486830834380223E-16 ) ) ;
#9793=ORIENTED_EDGE ( 'NONE', *, *, #10841, .T. ) ;
#9798=DIRECTION ( 'NONE',  ( 0.000000000000000000, 1.000000000000000000, 0.000000000000000000 ) ) ;
#9799=DIRECTION ( 'NONE',  ( -1.387778780781439759E-16, -1.110223024625160090E-15, -1.000000000000000000 ) ) ;
#9804=CARTESIAN_POINT ( 'NONE',  ( -1.899999999999999911, 7.299999999999999822, 1.600000000000000089 ) ) ;
#9808=EDGE_CURVE ( 'NONE', #13413, #17808, #17537, .T. ) ;
#9813=DIRECTION ( 'NONE',  ( 0.000000000000000000, 0.000000000000000000, -1.000000000000000000 ) ) ;
#9815=DIRECTION ( 'NONE',  ( -1.000000000000000000, 6.098637220230962441E-16, 0.000000000000000000 ) ) ;
#9818=CARTESIAN_POINT ( 'NONE',  ( -1.889999999999999902, 4.700000000000000178, 0.6099999999999999867 ) ) ;
#9819=ORIENTED_EDGE ( 'NONE', *, *, #9452, .T. ) ;
#9823=CARTESIAN_POINT ( 'NONE',  ( -1.899999999999999911, 9.199999999999999289, 1.600000000000000089 ) ) ;
#9825=CARTESIAN_POINT ( 'NONE',  ( -1.850000000000000089, 11.25000000000000000, 7.700000000000000178 ) ) ;
#9827=ADVANCED_FACE ( 'NONE', ( #7658 ), #3480, .T. ) ;
#9828=ORIENTED_EDGE ( 'NONE', *, *, #13326, .T. ) ;
#9835=ADVANCED_FACE ( 'NONE', ( #9126 ), #909, .T. ) ;
#9836=FACE_OUTER_BOUND ( 'NONE', #6848, .T. ) ;
#9837=DIRECTION ( 'NONE',  ( -0.7049180327868849183, 0.7092887755011130224, 8.531426931033447850E-16 ) ) ;
#9841=ORIENTED_EDGE ( 'NONE', *, *, #11335, .F. ) ;
#9842=AXIS2_PLACEMENT_3D ( 'NONE', #5610, #15618, #11347 ) ;
#9848=ORIENTED_EDGE ( 'NONE', *, *, #9737, .T. ) ;
#9849=DIRECTION ( 'NONE',  ( 7.273661547324610053E-16, -6.123233995736769734E-17, 1.000000000000000000 ) ) ;
#9854=ADVANCED_FACE ( 'NONE', ( #995 ), #6547, .F. ) ;
#9863=DIRECTION ( 'NONE',  ( 2.960594732333750117E-16, 1.000000000000000000, 0.000000000000000000 ) ) ;
#9869=AXIS2_PLACEMENT_3D ( 'NONE', #14969, #16258, #18060 ) ;
#9870=FACE_OUTER_BOUND ( 'NONE', #11547, .T. ) ;
#9876=DIRECTION ( 'NONE',  ( -2.220446049250309876E-16, -1.000000000000000000, -3.286920438420880041E-31 ) ) ;
#9880=CARTESIAN_POINT ( 'NONE',  ( 2.200000000000000178, 1.684703763649490251E-16, 7.649999999999999467 ) ) ;
#9882=DIRECTION ( 'NONE',  ( 0.000000000000000000, 0.000000000000000000, 1.000000000000000000 ) ) ;
#9883=ORIENTED_EDGE ( 'NONE', *, *, #7119, .F. ) ;
#9889=CARTESIAN_POINT ( 'NONE',  ( -1.899999999999999911, 4.700000000000000178, 1.600000000000000089 ) ) ;
#9894=DIRECTION ( 'NONE',  ( 0.000000000000000000, 0.000000000000000000, -1.000000000000000000 ) ) ;
#9905=FACE_OUTER_BOUND ( 'NONE', #15733, .T. ) ;
#9909=VERTEX_POINT ( 'NONE', #14982 ) ;
#9911=ORIENTED_EDGE ( 'NONE', *, *, #6353, .T. ) ;
#9914=DIRECTION ( 'NONE',  ( 1.000000000000000000, 0.000000000000000000, 1.305527901448219810E-16 ) ) ;
#9920=LINE ( 'NONE', #16952, #6065 ) ;
#9922=CARTESIAN_POINT ( 'NONE',  ( 2.500000000000000000, 0.8000000000000000444, -1.776356839400249676E-15 ) ) ;
#9925=AXIS2_PLACEMENT_3D ( 'NONE', #15409, #7070, #2894 ) ;
#9926=ADVANCED_FACE ( 'NONE', ( #14782 ), #621, .F. ) ;
#9929=ADVANCED_FACE ( 'NONE', ( #16554 ), #5153, .T. ) ;
#9930=EDGE_CURVE ( 'NONE', #12188, #14967, #3760, .T. ) ;
#9942=CARTESIAN_POINT ( 'NONE',  ( 2.500000000000000000, 2.799999999999999822, 0.6099999999999999867 ) ) ;
#9946=CARTESIAN_POINT ( 'NONE',  ( 2.500000000000000000, 10.00000000000000000, -1.206091987257470116E-15 ) ) ;
#9947=SPHERICAL_SURFACE ( 'NONE', #11467, 0.4166666666666670182 ) ;
#9951=ADVANCED_FACE ( 'NONE', ( #6894 ), #10977, .T. ) ;
#9953=DIRECTION ( 'NONE',  ( 1.739311637268509859E-16, 6.049014748177290126E-16, -1.000000000000000000 ) ) ;
#9954=FACE_OUTER_BOUND ( 'NONE', #290, .T. ) ;
#9956=FACE_OUTER_BOUND ( 'NONE', #15448, .T. ) ;
#9965=CYLINDRICAL_SURFACE ( 'NONE', #9662, 0.6100000000000000977 ) ;
#9967=EDGE_LOOP ( 'NONE', ( #14086, #13376, #14181, #13635 ) ) ;
#9969=CIRCLE ( 'NONE', #14720, 0.01000000000000002623 ) ;
#9971=VECTOR ( 'NONE', #15177, 1000.000000000000000 ) ;
#9977=ORIENTED_EDGE ( 'NONE', *, *, #18053, .T. ) ;
#9983=CARTESIAN_POINT ( 'NONE',  ( 1.000000000000000000, 5.400000000000000355, 7.700000000000000178 ) ) ;
#9990=ORIENTED_EDGE ( 'NONE', *, *, #11714, .F. ) ;
#9991=VECTOR ( 'NONE', #8356, 1000.000000000000000 ) ;
#9998=EDGE_CURVE ( 'NONE', #12787, #10006, #4127, .T. ) ;
#9999=VECTOR ( 'NONE', #5245, 1000.000000000000000 ) ;
#10003=CARTESIAN_POINT ( 'NONE',  ( -2.500000000000000000, 11.25000000000000000, 7.649999999999999467 ) ) ;
#10006=VERTEX_POINT ( 'NONE', #3926 ) ;
#10009=CARTESIAN_POINT ( 'NONE',  ( 2.500000000000000000, 1.148961478048660025E-16, 3.600000000000000089 ) ) ;
#10010=FACE_OUTER_BOUND ( 'NONE', #5054, .T. ) ;
#10014=VECTOR ( 'NONE', #17409, 1000.000000000000000 ) ;
#10015=ORIENTED_EDGE ( 'NONE', *, *, #8669, .T. ) ;
#10017=CARTESIAN_POINT ( 'NONE',  ( -2.500000000000000000, 8.500000000000000000, 0.6099999999999999867 ) ) ;
#10018=DIRECTION ( 'NONE',  ( -1.000000000000000000, 0.000000000000000000, 0.000000000000000000 ) ) ;
#10019=AXIS2_PLACEMENT_3D ( 'NONE', #15181, #3773, #17639 ) ;
#10021=CARTESIAN_POINT ( 'NONE',  ( 1.983927814618709873E-15, 10.80000000000000071, 8.599999999999999645 ) ) ;
#10022=LINE ( 'NONE', #12975, #10871 ) ;
#10033=CIRCLE ( 'NONE', #17109, 0.6500000000000003553 ) ;
#10037=PRODUCT_CONTEXT ( 'NONE', #13728, 'mechanical' ) ;
#10039=ORIENTED_EDGE ( 'NONE', *, *, #16756, .T. ) ;
#10046=VECTOR ( 'NONE', #3892, 1000.000000000000000 ) ;
#10050=PLANE ( 'NONE',  #16480 ) ;
#10051=EDGE_CURVE ( 'NONE', #6712, #229, #7095, .T. ) ;
#10053=CARTESIAN_POINT ( 'NONE',  ( -1.899999999999999911, 0.7500000000000000000, 7.649999999999999467 ) ) ;
#10055=EDGE_CURVE ( 'NONE', #9144, #14593, #18002, .T. ) ;
#10058=DIRECTION ( 'NONE',  ( 1.000000000000000000, 0.000000000000000000, 0.000000000000000000 ) ) ;
#10060=ADVANCED_FACE ( 'NONE', ( #7094 ), #5698, .F. ) ;
#10061=ORIENTED_EDGE ( 'NONE', *, *, #3226, .F. ) ;
#10069=CARTESIAN_POINT ( 'NONE',  ( 1.850000000000000089, 11.25000000000000000, 7.649999999999999467 ) ) ;
#10070=ORIENTED_EDGE ( 'NONE', *, *, #6236, .T. ) ;
#10071=AXIS2_PLACEMENT_3D ( 'NONE', #2187, #13583, #16163 ) ;
#10076=CARTESIAN_POINT ( 'NONE',  ( -1.599999999999880185, 11.40000000000000036, -2.399999999999999911 ) ) ;
#10079=ORIENTED_EDGE ( 'NONE', *, *, #2622, .F. ) ;
#10080=ORIENTED_EDGE ( 'NONE', *, *, #13112, .T. ) ;
#10081=LINE ( 'NONE', #14153, #13035 ) ;
#10090=CARTESIAN_POINT ( 'NONE',  ( -0.3367924244280810497, 2.254758922476410188, 8.300000000000000711 ) ) ;
#10098=ORIENTED_EDGE ( 'NONE', *, *, #13830, .F. ) ;
#10099=FACE_OUTER_BOUND ( 'NONE', #7179, .T. ) ;
#10101=FACE_OUTER_BOUND ( 'NONE', #3133, .T. ) ;
#10132=ORIENTED_EDGE ( 'NONE', *, *, #15426, .F. ) ;
#10136=AXIS2_PLACEMENT_3D ( 'NONE', #2649, #1254, #8475 ) ;
#10137=DIRECTION ( 'NONE',  ( 4.794417550286630491E-31, -1.000000000000000000, -1.774290917998389804E-45 ) ) ;
#10144=ADVANCED_FACE ( 'NONE', ( #12719 ), #36, .F. ) ;
#10145=VERTEX_POINT ( 'NONE', #17043 ) ;
#10146=EDGE_CURVE ( 'NONE', #13575, #3076, #291, .T. ) ;
#10149=EDGE_CURVE ( 'NONE', #14423, #11652, #4185, .T. ) ;
#10156=ORIENTED_EDGE ( 'NONE', *, *, #13815, .T. ) ;
#10161=DIRECTION ( 'NONE',  ( 8.971499188890150495E-16, 0.000000000000000000, 1.000000000000000000 ) ) ;
#10169=CYLINDRICAL_SURFACE ( 'NONE', #10891, 0.3500000000000001998 ) ;
#10170=DIRECTION ( 'NONE',  ( 0.000000000000000000, -1.000000000000000000, 2.493473113004670213E-16 ) ) ;
#10174=DIRECTION ( 'NONE',  ( -1.305527901448219810E-16, 6.123233995736909017E-17, 1.000000000000000000 ) ) ;
#10175=ORIENTED_EDGE ( 'NONE', *, *, #15217, .T. ) ;
#10177=DIRECTION ( 'NONE',  ( 0.000000000000000000, 0.000000000000000000, 1.000000000000000000 ) ) ;
#10179=CARTESIAN_POINT ( 'NONE',  ( -1.899999999999999911, 2.799999999999999822, 0.6099999999999999867 ) ) ;
#10192=VERTEX_POINT ( 'NONE', #2809 ) ;
#10202=CARTESIAN_POINT ( 'NONE',  ( -1.889999999999999902, 7.299999999999999822, 0.6099999999999999867 ) ) ;
#10206=ADVANCED_FACE ( 'NONE', ( #11325 ), #5680, .T. ) ;
#10208=DIRECTION ( 'NONE',  ( -1.000000000000000000, 0.000000000000000000, 0.000000000000000000 ) ) ;
#10209=DIRECTION ( 'NONE',  ( -1.142385477618690234E-14, 1.110223024625159992E-16, -1.000000000000000000 ) ) ;
#10215=CIRCLE ( 'NONE', #757, 1.000000000000000000 ) ;
#10225=DIRECTION ( 'NONE',  ( 0.000000000000000000, 0.000000000000000000, -1.000000000000000000 ) ) ;
#10226=VECTOR ( 'NONE', #13370, 1000.000000000000000 ) ;
#10231=CARTESIAN_POINT ( 'NONE',  ( 2.500000000000000000, 2.000000000000000000, 1.600000000000000089 ) ) ;
#10235=ORIENTED_EDGE ( 'NONE', *, *, #14124, .F. ) ;
#10236=CARTESIAN_POINT ( 'NONE',  ( 2.500000000000000000, 2.000000000000000000, -1.522591576628789972E-15 ) ) ;
#10240=AXIS2_PLACEMENT_3D ( 'NONE', #17472, #17553, #10531 ) ;
#10247=CIRCLE ( 'NONE', #6158, 0.5999999999999998668 ) ;
#10249=AXIS2_PLACEMENT_3D ( 'NONE', #13391, #526, #12004 ) ;
#10254=VECTOR ( 'NONE', #9792, 1000.000000000000000 ) ;
#10255=LINE ( 'NONE', #17111, #4378 ) ;
#10257=DIRECTION ( 'NONE',  ( 1.000000000000000000, -1.224646799147339895E-16, 0.000000000000000000 ) ) ;
#10260=VERTEX_POINT ( 'NONE', #14545 ) ;
#10262=VECTOR ( 'NONE', #15761, 1000.000000000000000 ) ;
#10266=ADVANCED_FACE ( 'NONE', ( #388 ), #13246, .T. ) ;
#10267=ORIENTED_EDGE ( 'NONE', *, *, #16171, .F. ) ;
#10283=AXIS2_PLACEMENT_3D ( 'NONE', #9818, #5289, #5382 ) ;
#10287=CIRCLE ( 'NONE', #5858, 0.6999999999999992895 ) ;
#10288=EDGE_CURVE ( 'NONE', #8504, #15242, #9164, .T. ) ;
#10293=ORIENTED_EDGE ( 'NONE', *, *, #15938, .T. ) ;
#10295=ORIENTED_EDGE ( 'NONE', *, *, #11970, .F. ) ;
#10301=ADVANCED_FACE ( 'NONE', ( #13154 ), #3335, .F. ) ;
#10303=CARTESIAN_POINT ( 'NONE',  ( 1.889999999999999902, 8.500000000000000000, 0.6099999999999999867 ) ) ;
#10308=DIRECTION ( 'NONE',  ( 0.000000000000000000, 0.000000000000000000, -1.000000000000000000 ) ) ;
#10312=DIRECTION ( 'NONE',  ( 0.000000000000000000, 0.000000000000000000, 1.000000000000000000 ) ) ;
#10315=ADVANCED_FACE ( 'NONE', ( #3413 ), #10371, .T. ) ;
#10341=DIRECTION ( 'NONE',  ( 1.000000000000000000, -2.220446049250309876E-16, -6.049014748177260544E-16 ) ) ;
#10342=EDGE_LOOP ( 'NONE', ( #13722, #3323, #12262 ) ) ;
#10353=DIRECTION ( 'NONE',  ( -4.440892098500630106E-16, -1.000000000000000000, -1.332267629550190018E-15 ) ) ;
#10354=ORIENTED_EDGE ( 'NONE', *, *, #7501, .F. ) ;
#10360=DIRECTION ( 'NONE',  ( -4.318427418585891014E-15, 2.220446049250309876E-16, -1.000000000000000000 ) ) ;
#10370=DIRECTION ( 'NONE',  ( -2.114710523095539848E-16, -1.000000000000000000, 0.000000000000000000 ) ) ;
#10371=PLANE ( 'NONE',  #7387 ) ;
#10372=ORIENTED_EDGE ( 'NONE', *, *, #11854, .T. ) ;
#10376=ORIENTED_EDGE ( 'NONE', *, *, #13112, .F. ) ;
#10379=EDGE_CURVE ( 'NONE', #15324, #1696, #14824, .T. ) ;
#10380=CARTESIAN_POINT ( 'NONE',  ( 1.399999999999999911, 5.799999999999999822, 7.700000000000000178 ) ) ;
#10381=VERTEX_POINT ( 'NONE', #13429 ) ;
#10387=ORIENTED_EDGE ( 'NONE', *, *, #11938, .T. ) ;
#10388=LINE ( 'NONE', #7710, #17911 ) ;
#10393=ORIENTED_EDGE ( 'NONE', *, *, #7000, .T. ) ;
#10397=LINE ( 'NONE', #17071, #15411 ) ;
#10400=CARTESIAN_POINT ( 'NONE',  ( 2.500000000000000000, 0.4000000000000000222, 7.649999999999999467 ) ) ;
#10403=ORIENTED_EDGE ( 'NONE', *, *, #11147, .F. ) ;
#10412=EDGE_CURVE ( 'NONE', #13022, #13413, #6186, .T. ) ;
#10413=LINE ( 'NONE', #13117, #5285 ) ;
#10415=VECTOR ( 'NONE', #5337, 1000.000000000000000 ) ;
#10416=ORIENTED_EDGE ( 'NONE', *, *, #10722, .T. ) ;
#10421=ORIENTED_EDGE ( 'NONE', *, *, #8796, .T. ) ;
#10422=ORIENTED_EDGE ( 'NONE', *, *, #5696, .T. ) ;
#10425=FACE_OUTER_BOUND ( 'NONE', #15839, .T. ) ;
#10426=VERTEX_POINT ( 'NONE', #6377 ) ;
#10430=DIRECTION ( 'NONE',  ( 1.000000000000000000, 4.014365738757630620E-15, 5.017957173447030386E-16 ) ) ;
#10437=CARTESIAN_POINT ( 'NONE',  ( 1.000000000000000000, 6.799999999999999822, 8.300000000000000711 ) ) ;
#10442=EDGE_LOOP ( 'NONE', ( #4211, #5905, #6237, #11300, #6217, #10393, #11166, #17851 ) ) ;
#10456=DIRECTION ( 'NONE',  ( 3.700743415417190309E-15, -6.579099405186109509E-16, 1.000000000000000000 ) ) ;
#10461=ORIENTED_EDGE ( 'NONE', *, *, #5410, .T. ) ;
#10462=CARTESIAN_POINT ( 'NONE',  ( -0.5372984490435469551, 4.250000000000000000, 8.300000000000000711 ) ) ;
#10471=CARTESIAN_POINT ( 'NONE',  ( 1.800000000000000044, 11.29999999999999893, 7.649999999999999467 ) ) ;
#10475=ADVANCED_FACE ( 'NONE', ( #5005 ), #9629, .F. ) ;
#10483=DIRECTION ( 'NONE',  ( 1.000000000000000000, -1.059337802663170094E-14, 1.821459649775649668E-16 ) ) ;
#10486=ORIENTED_EDGE ( 'NONE', *, *, #9369, .F. ) ;
#10489=EDGE_CURVE ( 'NONE', #17764, #14464, #16672, .T. ) ;
#10493=CARTESIAN_POINT ( 'NONE',  ( -1.899999999999999911, 8.500000000000000000, 0.6099999999999999867 ) ) ;
#10494=LINE ( 'NONE', #17251, #15063 ) ;
#10502=CARTESIAN_POINT ( 'NONE',  ( -1.899999999999999911, 9.199999999999999289, 0.6099999999999999867 ) ) ;
#10507=CARTESIAN_POINT ( 'NONE',  ( -1.875000000000000000, 2.296212748401290437E-16, 7.700000000000000178 ) ) ;
#10514=DIRECTION ( 'NONE',  ( 0.000000000000000000, 0.000000000000000000, 1.000000000000000000 ) ) ;
#10515=DIRECTION ( 'NONE',  ( 6.083413833562510128E-16, -9.455524548882000146E-32, 1.000000000000000000 ) ) ;
#10528=EDGE_CURVE ( 'NONE', #12817, #13575, #2877, .T. ) ;
#10530=ORIENTED_EDGE ( 'NONE', *, *, #16850, .T. ) ;
#10531=DIRECTION ( 'NONE',  ( 0.000000000000000000, 1.000000000000000000, -2.168404344971008868E-15 ) ) ;
#10532=CARTESIAN_POINT ( 'NONE',  ( 1.899999999999999911, 10.00000000000000000, -5.075305255429290705E-16 ) ) ;
#10534=CIRCLE ( 'NONE', #4041, 1.000000000000000000 ) ;
#10543=CIRCLE ( 'NONE', #16770, 0.04999999999999991257 ) ;
#10548=AXIS2_PLACEMENT_3D ( 'NONE', #11220, #16680, #15406 ) ;
#10550=ORIENTED_EDGE ( 'NONE', *, *, #8237, .T. ) ;
#10556=LINE ( 'NONE', #10380, #17966 ) ;
#10563=DIRECTION ( 'NONE',  ( -7.109522442527898025E-16, 0.000000000000000000, -1.000000000000000000 ) ) ;
#10567=LINE ( 'NONE', #9179, #547 ) ;
#10572=AXIS2_PLACEMENT_3D ( 'NONE', #10902, #12003, #13390 ) ;
#10574=DIRECTION ( 'NONE',  ( 1.000000000000000000, 0.000000000000000000, 0.000000000000000000 ) ) ;
#10576=ORIENTED_EDGE ( 'NONE', *, *, #17183, .F. ) ;
#10578=ORIENTED_EDGE ( 'NONE', *, *, #5415, .F. ) ;
#10580=LINE ( 'NONE', #15400, #4675 ) ;
#10589=DIRECTION ( 'NONE',  ( 1.000000000000000000, 0.000000000000000000, -7.401486830834380223E-16 ) ) ;
#10590=FACE_OUTER_BOUND ( 'NONE', #12647, .T. ) ;
#10595=PLANE ( 'NONE',  #7081 ) ;
#10598=DIRECTION ( 'NONE',  ( -1.480297366166879989E-15, -2.476791224480699852E-30, -1.000000000000000000 ) ) ;
#10600=EDGE_CURVE ( 'NONE', #2787, #6171, #7226, .T. ) ;
#10609=ORIENTED_EDGE ( 'NONE', *, *, #13294, .T. ) ;
#10612=DIRECTION ( 'NONE',  ( -3.700743415417195042E-15, -3.289549702593060375E-15, 1.000000000000000000 ) ) ;
#10615=VECTOR ( 'NONE', #6160, 1000.000000000000000 ) ;
#10617=ORIENTED_EDGE ( 'NONE', *, *, #1720, .F. ) ;
#10643=CARTESIAN_POINT ( 'NONE',  ( -1.599999999999880185, 11.40000000000000036, 1.600000000000000089 ) ) ;
#10646=VERTEX_POINT ( 'NONE', #182 ) ;
#10648=ORIENTED_EDGE ( 'NONE', *, *, #17463, .T. ) ;
#10650=LINE ( 'NONE', #3601, #3190 ) ;
#10659=ORIENTED_EDGE ( 'NONE', *, *, #2642, .T. ) ;
#10660=ADVANCED_FACE ( 'NONE', ( #15747 ), #11210, .F. ) ;
#10664=ORIENTED_EDGE ( 'NONE', *, *, #1049, .T. ) ;
#10671=AXIS2_PLACEMENT_3D ( 'NONE', #12105, #17904, #15165 ) ;
#10672=FACE_OUTER_BOUND ( 'NONE', #7120, .T. ) ;
#10680=ORIENTED_EDGE ( 'NONE', *, *, #17162, .T. ) ;
#10699=CARTESIAN_POINT ( 'NONE',  ( -1.899999999999999911, 9.199999999999999289, 1.600000000000000089 ) ) ;
#10702=ORIENTED_EDGE ( 'NONE', *, *, #8688, .T. ) ;
#10703=CARTESIAN_POINT ( 'NONE',  ( 2.500000000000000000, 3.500000000000000000, 0.6099999999999999867 ) ) ;
#10707=ORIENTED_EDGE ( 'NONE', *, *, #6657, .F. ) ;
#10708=PLANE ( 'NONE',  #10671 ) ;
#10714=PLANE ( 'NONE',  #8524 ) ;
#10717=ADVANCED_FACE ( 'NONE', ( #16099 ), #14611, .T. ) ;
#10721=ORIENTED_EDGE ( 'NONE', *, *, #2803, .F. ) ;
#10722=EDGE_CURVE ( 'NONE', #2252, #2762, #7313, .T. ) ;
#10723=EDGE_CURVE ( 'NONE', #17164, #13357, #13049, .T. ) ;
#10724=CARTESIAN_POINT ( 'NONE',  ( -1.889999999999999902, 4.700000000000000178, -5.551115123125779744E-16 ) ) ;
#10725=DIRECTION ( 'NONE',  ( -1.000000000000000000, 0.000000000000000000, 0.000000000000000000 ) ) ;
#10727=CARTESIAN_POINT ( 'NONE',  ( 2.200000000000000178, 1.815095292823759964E-16, 4.000000000000000000 ) ) ;
#10731=CARTESIAN_POINT ( 'NONE',  ( -0.9999999999999978906, 9.099999999999999645, 7.700000000000000178 ) ) ;
#10740=LINE ( 'NONE', #12226, #6085 ) ;
#10743=FACE_OUTER_BOUND ( 'NONE', #15595, .T. ) ;
#10748=ORIENTED_EDGE ( 'NONE', *, *, #4296, .T. ) ;
#10752=ORIENTED_EDGE ( 'NONE', *, *, #14504, .F. ) ;
#10755=EDGE_LOOP ( 'NONE', ( #11309, #186 ) ) ;
#10760=ADVANCED_FACE ( 'NONE', ( #17549 ), #14340, .F. ) ;
#10761=DIRECTION ( 'NONE',  ( -0.000000000000000000, 1.000000000000000000, 0.000000000000000000 ) ) ;
#10765=PLANE ( 'NONE',  #10861 ) ;
#10769=CIRCLE ( 'NONE', #1893, 0.3999999999999999667 ) ;
#10781=CARTESIAN_POINT ( 'NONE',  ( -1.000000000000000000, 5.400000000000000355, 7.700000000000000178 ) ) ;
#10787=ORIENTED_EDGE ( 'NONE', *, *, #10379, .T. ) ;
#10789=CARTESIAN_POINT ( 'NONE',  ( 1.889999999999999902, 3.500000000000000000, 0.6099999999999999867 ) ) ;
#10799=FACE_OUTER_BOUND ( 'NONE', #18147, .T. ) ;
#10803=CARTESIAN_POINT ( 'NONE',  ( -0.7999999999998790301, 11.40000000000000036, -9.797174393178840942E-17 ) ) ;
#10805=CARTESIAN_POINT ( 'NONE',  ( -1.599999999999880185, 11.40000000000000036, 1.600000000000000089 ) ) ;
#10806=LINE ( 'NONE', #12011, #237 ) ;
#10812=LINE ( 'NONE', #11927, #15050 ) ;
#10816=CARTESIAN_POINT ( 'NONE',  ( -0.3367924244280810497, 2.254758922476410188, 7.700000000000000178 ) ) ;
#10817=VERTEX_POINT ( 'NONE', #630 ) ;
#10820=ORIENTED_EDGE ( 'NONE', *, *, #15715, .F. ) ;
#10822=PLANE ( 'NONE',  #766 ) ;
#10823=DIRECTION ( 'NONE',  ( 0.000000000000000000, 0.000000000000000000, 1.000000000000000000 ) ) ;
#10825=ADVANCED_FACE ( 'NONE', ( #11930 ), #14440, .T. ) ;
#10830=CARTESIAN_POINT ( 'NONE',  ( 2.500000000000000000, 8.500000000000000000, 0.6099999999999999867 ) ) ;
#10834=DIRECTION ( 'NONE',  ( 1.000000000000000000, -2.220446049250309876E-16, -7.401486830834380223E-16 ) ) ;
#10841=EDGE_CURVE ( 'NONE', #9046, #11652, #11845, .T. ) ;
#10848=EDGE_CURVE ( 'NONE', #17593, #14634, #11823, .T. ) ;
#10851=ADVANCED_FACE ( 'NONE', ( #14527 ), #6093, .F. ) ;
#10853=EDGE_CURVE ( 'NONE', #5435, #3235, #4702, .T. ) ;
#10856=AXIS2_PLACEMENT_3D ( 'NONE', #17527, #16160, #9113 ) ;
#10861=AXIS2_PLACEMENT_3D ( 'NONE', #7998, #9365, #13730 ) ;
#10865=VECTOR ( 'NONE', #9863, 1000.000000000000000 ) ;
#10871=VECTOR ( 'NONE', #297, 1000.000000000000000 ) ;
#10872=AXIS2_PLACEMENT_3D ( 'NONE', #10303, #2050, #10563 ) ;
#10873=VECTOR ( 'NONE', #16184, 1000.000000000000000 ) ;
#10886=CARTESIAN_POINT ( 'NONE',  ( -1.889999999999999902, 4.700000000000000178, 0.6099999999999999867 ) ) ;
#10888=VECTOR ( 'NONE', #4996, 1000.000000000000000 ) ;
#10891=AXIS2_PLACEMENT_3D ( 'NONE', #16936, #7148, #12957 ) ;
#10899=AXIS2_PLACEMENT_3D ( 'NONE', #1791, #9849, #7435 ) ;
#10902=CARTESIAN_POINT ( 'NONE',  ( 4.898587196589409994E-17, 0.1000000000000000056, 8.300000000000000711 ) ) ;
#10903=SPHERICAL_SURFACE ( 'NONE', #13818, 1.100000000000000089 ) ;
#10906=VECTOR ( 'NONE', #17955, 1000.000000000000000 ) ;
#10925=DIRECTION ( 'NONE',  ( 7.401486830834380223E-16, -8.540177112501229283E-17, 1.000000000000000000 ) ) ;
#10929=EDGE_LOOP ( 'NONE', ( #17278, #859, #9212, #8856 ) ) ;
#10932=VECTOR ( 'NONE', #4366, 1000.000000000000000 ) ;
#10933=DIRECTION ( 'NONE',  ( 0.000000000000000000, 0.000000000000000000, 1.000000000000000000 ) ) ;
#10942=VERTEX_POINT ( 'NONE', #10816 ) ;
#10943=CARTESIAN_POINT ( 'NONE',  ( -2.500000000000000000, 3.500000000000000000, 0.6099999999999999867 ) ) ;
#10945=ORIENTED_EDGE ( 'NONE', *, *, #7534, .F. ) ;
#10962=EDGE_CURVE ( 'NONE', #11846, #13146, #2493, .T. ) ;
#10963=ORIENTED_EDGE ( 'NONE', *, *, #3475, .T. ) ;
#10968=VECTOR ( 'NONE', #8505, 1000.000000000000000 ) ;
#10977=PLANE ( 'NONE',  #9135 ) ;
#10988=ORIENTED_EDGE ( 'NONE', *, *, #878, .T. ) ;
#10990=LINE ( 'NONE', #6824, #14432 ) ;
#10991=CARTESIAN_POINT ( 'NONE',  ( 2.500000000000000000, 11.29999999999999893, 1.600000000000000089 ) ) ;
#10996=CARTESIAN_POINT ( 'NONE',  ( 2.616666666666660035, -5.805074450128190455E-17, 4.000000000000000000 ) ) ;
#11007=EDGE_LOOP ( 'NONE', ( #5423, #7700, #142, #1854 ) ) ;
#11016=CARTESIAN_POINT ( 'NONE',  ( 2.500000000000000000, 2.000000000000000000, 1.600000000000000089 ) ) ;
#11022=DIRECTION ( 'NONE',  ( -1.000000000000000000, 0.000000000000000000, 0.000000000000000000 ) ) ;
#11023=ORIENTED_EDGE ( 'NONE', *, *, #7536, .T. ) ;
#11025=VECTOR ( 'NONE', #14994, 1000.000000000000000 ) ;
#11035=DIRECTION ( 'NONE',  ( 0.000000000000000000, 0.000000000000000000, 1.000000000000000000 ) ) ;
#11040=ORIENTED_EDGE ( 'NONE', *, *, #16251, .T. ) ;
#11044=LINE ( 'NONE', #17874, #13249 ) ;
#11050=CARTESIAN_POINT ( 'NONE',  ( 0.03000000000000110217, 11.40000000000000036, 1.600000000000000089 ) ) ;
#11051=EDGE_CURVE ( 'NONE', #7200, #2787, #13409, .T. ) ;
#11056=DIRECTION ( 'NONE',  ( 7.401486830834380223E-16, 1.000000000000000000, -1.110223024625159992E-16 ) ) ;
#11072=LINE ( 'NONE', #14126, #8534 ) ;
#11074=EDGE_CURVE ( 'NONE', #410, #11828, #6357, .T. ) ;
#11083=ORIENTED_EDGE ( 'NONE', *, *, #17084, .F. ) ;
#11110=DIRECTION ( 'NONE',  ( 1.000000000000000000, 0.000000000000000000, 0.000000000000000000 ) ) ;
#11111=VERTEX_POINT ( 'NONE', #9889 ) ;
#11122=PLANE ( 'NONE',  #9925 ) ;
#11123=AXIS2_PLACEMENT_3D ( 'NONE', #2200, #12291, #5254 ) ;
#11132=CYLINDRICAL_SURFACE ( 'NONE', #9095, 1.016666666666670160 ) ;
#11139=AXIS2_PLACEMENT_3D ( 'NONE', #13812, #952, #9556 ) ;
#11144=CARTESIAN_POINT ( 'NONE',  ( 4.898587196589409994E-17, 0.1000000000000000056, 8.300000000000000711 ) ) ;
#11147=EDGE_CURVE ( 'NONE', #13226, #16249, #13013, .T. ) ;
#11148=DIRECTION ( 'NONE',  ( 6.049014748177260544E-16, -2.493473113004680074E-16, 1.000000000000000000 ) ) ;
#11153=DIRECTION ( 'NONE',  ( 5.551115123125790591E-16, -9.251858538542978977E-17, 1.000000000000000000 ) ) ;
#11156=EDGE_CURVE ( 'NONE', #8261, #9511, #15398, .T. ) ;
#11164=CARTESIAN_POINT ( 'NONE',  ( 1.899999999999999911, 2.799999999999999822, 0.6099999999999999867 ) ) ;
#11166=ORIENTED_EDGE ( 'NONE', *, *, #2594, .T. ) ;
#11170=DIRECTION ( 'NONE',  ( -0.2800000000000001377, 0.9599999999999999645, 0.000000000000000000 ) ) ;
#11172=AXIS2_PLACEMENT_3D ( 'NONE', #7752, #16451, #13397 ) ;
#11173=CIRCLE ( 'NONE', #5566, 0.2000000000000005107 ) ;
#11174=CARTESIAN_POINT ( 'NONE',  ( 1.000000000000000000, 6.799999999999999822, 7.700000000000000178 ) ) ;
#11175=EDGE_CURVE ( 'NONE', #17218, #3339, #2852, .T. ) ;
#11176=EDGE_LOOP ( 'NONE', ( #15864, #8820, #2698, #2769 ) ) ;
#11179=AXIS2_PLACEMENT_3D ( 'NONE', #6909, #8482, #1453 ) ;
#11183=EDGE_CURVE ( 'NONE', #17929, #3526, #2955, .T. ) ;
#11185=DIRECTION ( 'NONE',  ( 1.445602896647339508E-15, 1.000000000000000000, 1.332267629550190412E-15 ) ) ;
#11191=CARTESIAN_POINT ( 'NONE',  ( 0.000000000000000000, 0.000000000000000000, 0.000000000000000000 ) ) ;
#11194=VECTOR ( 'NONE', #16025, 1000.000000000000000 ) ;
#11195=ORIENTED_EDGE ( 'NONE', *, *, #9930, .F. ) ;
#11198=CARTESIAN_POINT ( 'NONE',  ( -0.7999999999998730349, 12.00000000000000000, -9.797174393178840942E-17 ) ) ;
#11207=EDGE_CURVE ( 'NONE', #13279, #12720, #2767, .T. ) ;
#11210=CYLINDRICAL_SURFACE ( 'NONE', #879, 0.01000000000000002623 ) ;
#11214=VERTEX_POINT ( 'NONE', #7024 ) ;
#11217=CARTESIAN_POINT ( 'NONE',  ( 1.800000000000000044, 12.00000000000000000, 1.600000000000000089 ) ) ;
#11220=CARTESIAN_POINT ( 'NONE',  ( -1.889999999999999902, 3.500000000000000000, 0.6099999999999999867 ) ) ;
#11223=DIRECTION ( 'NONE',  ( 1.224646799147350002E-16, 1.000000000000000000, 0.000000000000000000 ) ) ;
#11224=AXIS2_PLACEMENT_3D ( 'NONE', #1064, #11056, #5332 ) ;
#11229=EDGE_CURVE ( 'NONE', #3622, #3076, #8412, .T. ) ;
#11231=CARTESIAN_POINT ( 'NONE',  ( -2.500000000000000000, 0.4000000000000000222, 7.649999999999999467 ) ) ;
#11232=AXIS2_PLACEMENT_3D ( 'NONE', #1662, #12959, #8787 ) ;
#11237=ORIENTED_EDGE ( 'NONE', *, *, #11988, .F. ) ;
#11239=VERTEX_POINT ( 'NONE', #1191 ) ;
#11241=( NAMED_UNIT ( * ) SI_UNIT ( $, .STERADIAN. ) SOLID_ANGLE_UNIT ( ) );
#11245=VECTOR ( 'NONE', #16464, 1000.000000000000000 ) ;
#11250=DIRECTION ( 'NONE',  ( 1.000000000000000000, 8.615382147616920419E-16, 0.000000000000000000 ) ) ;
#11253=EDGE_LOOP ( 'NONE', ( #17495, #5271, #18288, #16411 ) ) ;
#11258=ORIENTED_EDGE ( 'NONE', *, *, #12223, .T. ) ;
#11266=ORIENTED_EDGE ( 'NONE', *, *, #7770, .T. ) ;
#11269=CARTESIAN_POINT ( 'NONE',  ( 0.5291502622129179434, 0.1000000000000000056, 7.700000000000000178 ) ) ;
#11270=AXIS2_PLACEMENT_3D ( 'NONE', #3117, #15908, #16006 ) ;
#11279=DIRECTION ( 'NONE',  ( -3.861645303044020177E-16, -1.000000000000000000, 1.268826313857319964E-16 ) ) ;
#11281=ORIENTED_EDGE ( 'NONE', *, *, #15760, .T. ) ;
#11285=DIRECTION ( 'NONE',  ( 0.000000000000000000, 0.000000000000000000, -1.000000000000000000 ) ) ;
#11291=EDGE_CURVE ( 'NONE', #8865, #16897, #5636, .T. ) ;
#11294=EDGE_CURVE ( 'NONE', #2415, #6533, #12847, .T. ) ;
#11299=CARTESIAN_POINT ( 'NONE',  ( 1.889999999999999902, 4.700000000000000178, 0.6099999999999999867 ) ) ;
#11300=ORIENTED_EDGE ( 'NONE', *, *, #8590, .T. ) ;
#11309=ORIENTED_EDGE ( 'NONE', *, *, #15257, .F. ) ;
#11312=EDGE_CURVE ( 'NONE', #10145, #17164, #7691, .T. ) ;
#11317=DIRECTION ( 'NONE',  ( -1.000000000000000000, -1.331202777560457422E-30, -0.000000000000000000 ) ) ;
#11318=LINE ( 'NONE', #7162, #11757 ) ;
#11323=AXIS2_PLACEMENT_3D ( 'NONE', #4206, #16802, #2829 ) ;
#11325=FACE_OUTER_BOUND ( 'NONE', #10342, .T. ) ;
#11331=ORIENTED_EDGE ( 'NONE', *, *, #13042, .T. ) ;
#11335=EDGE_CURVE ( 'NONE', #1432, #2090, #13027, .T. ) ;
#11336=ORIENTED_EDGE ( 'NONE', *, *, #17684, .F. ) ;
#11339=ORIENTED_EDGE ( 'NONE', *, *, #1913, .F. ) ;
#11342=CARTESIAN_POINT ( 'NONE',  ( -1.899999999999999911, 4.700000000000000178, 0.5999999999999999778 ) ) ;
#11346=ORIENTED_EDGE ( 'NONE', *, *, #11312, .F. ) ;
#11347=DIRECTION ( 'NONE',  ( 0.7049180327868849183, -0.7092887755011130224, 0.000000000000000000 ) ) ;
#11349=VECTOR ( 'NONE', #432, 1000.000000000000000 ) ;
#11356=LINE ( 'NONE', #9785, #2570 ) ;
#11357=EDGE_CURVE ( 'NONE', #13417, #15242, #3253, .T. ) ;
#11363=PLANE ( 'NONE',  #9055 ) ;
#11364=VERTEX_POINT ( 'NONE', #9021 ) ;
#11373=CARTESIAN_POINT ( 'NONE',  ( 1.899999999999999911, 0.7500000000000000000, 7.649999999999999467 ) ) ;
#11374=LINE ( 'NONE', #6492, #2934 ) ;
#11381=ADVANCED_FACE ( 'NONE', ( #12936 ), #1740, .F. ) ;
#11386=DIRECTION ( 'NONE',  ( -2.537652627714639929E-16, -1.000000000000000000, 0.000000000000000000 ) ) ;
#11387=ORIENTED_EDGE ( 'NONE', *, *, #11357, .F. ) ;
#11393=FACE_OUTER_BOUND ( 'NONE', #4898, .T. ) ;
#11394=CARTESIAN_POINT ( 'NONE',  ( -0.5291502622129179434, 1.642400929185890127E-16, 7.700000000000000178 ) ) ;
#11399=CARTESIAN_POINT ( 'NONE',  ( -1.899999999999999911, 2.799999999999999822, 1.600000000000000089 ) ) ;
#11402=DIRECTION ( 'NONE',  ( -2.960594732333750117E-16, -1.000000000000000000, 0.000000000000000000 ) ) ;
#11409=LINE ( 'NONE', #17039, #16490 ) ;
#11411=CARTESIAN_POINT ( 'NONE',  ( -1.899999999999999911, 4.218847493575600080E-16, 1.163414459189990120E-16 ) ) ;
#11424=ORIENTED_EDGE ( 'NONE', *, *, #13793, .F. ) ;
#11425=CYLINDRICAL_SURFACE ( 'NONE', #13190, 0.6000000000000000888 ) ;
#11428=ORIENTED_EDGE ( 'NONE', *, *, #7167, .T. ) ;
#11429=CARTESIAN_POINT ( 'NONE',  ( -1.850000000000000089, 11.25000000000000000, 8.300000000000000711 ) ) ;
#11437=CARTESIAN_POINT ( 'NONE',  ( 1.983927814618709873E-15, 10.80000000000000071, 8.599999999999999645 ) ) ;
#11438=CIRCLE ( 'NONE', #14140, 0.3499999999999999778 ) ;
#11440=CARTESIAN_POINT ( 'NONE',  ( -1.899999999999999911, 10.00000000000000000, 1.600000000000000089 ) ) ;
#11443=ADVANCED_FACE ( 'NONE', ( #3211 ), #14509, .T. ) ;
#11450=CIRCLE ( 'NONE', #8494, 0.4000000000000000222 ) ;
#11459=VECTOR ( 'NONE', #427, 1000.000000000000000 ) ;
#11460=VERTEX_POINT ( 'NONE', #8765 ) ;
#11465=CARTESIAN_POINT ( 'NONE',  ( 1.899999999999999911, 0.8000000000000000444, -2.399999999999999911 ) ) ;
#11467=AXIS2_PLACEMENT_3D ( 'NONE', #2923, #1533, #134 ) ;
#11468=CARTESIAN_POINT ( 'NONE',  ( 2.500000000000000000, 4.700000000000000178, 0.5999999999999999778 ) ) ;
#11469=LINE ( 'NONE', #534, #14684 ) ;
#11472=CIRCLE ( 'NONE', #1130, 0.4000000000000001887 ) ;
#11474=EDGE_CURVE ( 'NONE', #8434, #10381, #14323, .T. ) ;
#11478=VECTOR ( 'NONE', #623, 1000.000000000000000 ) ;
#11479=DIRECTION ( 'NONE',  ( -1.000000000000000000, 0.000000000000000000, 0.000000000000000000 ) ) ;
#11483=ORIENTED_EDGE ( 'NONE', *, *, #14270, .T. ) ;
#11486=CIRCLE ( 'NONE', #6151, 0.3499999999999996447 ) ;
#11490=DIRECTION ( 'NONE',  ( 0.000000000000000000, 1.000000000000000000, 0.000000000000000000 ) ) ;
#11492=DIRECTION ( 'NONE',  ( -6.162975822039159109E-32, -1.000000000000000000, -1.110223024625159992E-16 ) ) ;
#11493=AXIS2_PLACEMENT_3D ( 'NONE', #3136, #8791, #17197 ) ;
#11496=DIRECTION ( 'NONE',  ( -1.000000000000000000, 0.000000000000000000, 0.000000000000000000 ) ) ;
#11502=DIRECTION ( 'NONE',  ( 0.000000000000000000, -1.000000000000000000, 0.000000000000000000 ) ) ;
#11512=ORIENTED_EDGE ( 'NONE', *, *, #2622, .T. ) ;
#11519=ADVANCED_FACE ( 'NONE', ( #3466 ), #13754, .T. ) ;
#11522=ORIENTED_EDGE ( 'NONE', *, *, #6088, .T. ) ;
#11530=CARTESIAN_POINT ( 'NONE',  ( -1.899999999999999911, 11.15000000000000036, 1.600000000000000089 ) ) ;
#11535=CARTESIAN_POINT ( 'NONE',  ( 2.500000000000000000, 11.29999999999999893, 7.649999999999999467 ) ) ;
#11538=ORIENTED_EDGE ( 'NONE', *, *, #13276, .F. ) ;
#11540=CARTESIAN_POINT ( 'NONE',  ( 2.500000000000000000, 7.299999999999999822, 1.600000000000000089 ) ) ;
#11546=VERTEX_POINT ( 'NONE', #15160 ) ;
#11547=EDGE_LOOP ( 'NONE', ( #4819, #8092, #17025, #5592 ) ) ;
#11550=ORIENTED_EDGE ( 'NONE', *, *, #13326, .F. ) ;
#11556=VECTOR ( 'NONE', #1292, 1000.000000000000000 ) ;
#11563=DIRECTION ( 'NONE',  ( 0.000000000000000000, -1.000000000000000000, -1.769136588914770194E-30 ) ) ;
#11566=EDGE_LOOP ( 'NONE', ( #4468, #7803, #14264, #5926, #441, #12701, #15221, #12250, #11023, #16939, #18213, #10422, #7932, #6794, #1818, #9112, #4079, #17244, #8758, #4677, #657, #10421, #11718, #17724 ) ) ;
#11567=CARTESIAN_POINT ( 'NONE',  ( 1.000000000000000000, 6.799999999999999822, 7.700000000000000178 ) ) ;
#11573=LINE ( 'NONE', #11665, #13494 ) ;
#11597=LINE ( 'NONE', #6128, #11759 ) ;
#11599=ORIENTED_EDGE ( 'NONE', *, *, #7896, .F. ) ;
#11605=PLANE ( 'NONE',  #8659 ) ;
#11609=DIRECTION ( 'NONE',  ( 0.000000000000000000, 1.000000000000000000, 0.000000000000000000 ) ) ;
#11611=DIRECTION ( 'NONE',  ( 0.000000000000000000, 0.000000000000000000, 1.000000000000000000 ) ) ;
#11612=EDGE_CURVE ( 'NONE', #10192, #9205, #5028, .T. ) ;
#11613=VECTOR ( 'NONE', #2072, 1000.000000000000000 ) ;
#11615=EDGE_CURVE ( 'NONE', #14464, #6674, #3542, .T. ) ;
#11628=CARTESIAN_POINT ( 'NONE',  ( 1.889999999999999902, 4.700000000000000178, -4.702461056355109900E-16 ) ) ;
#11629=DIRECTION ( 'NONE',  ( 0.000000000000000000, -1.000000000000000000, 0.000000000000000000 ) ) ;
#11632=ADVANCED_FACE ( 'NONE', ( #6334 ), #3852, .F. ) ;
#11634=DIRECTION ( 'NONE',  ( -1.000000000000000000, 1.224646799147350002E-16, 0.000000000000000000 ) ) ;
#11635=ADVANCED_FACE ( 'NONE', ( #9208 ), #12190, .T. ) ;
#11639=EDGE_LOOP ( 'NONE', ( #10098, #9118, #15675, #12282 ) ) ;
#11641=PLANE ( 'NONE',  #3785 ) ;
#11650=DIRECTION ( 'NONE',  ( 1.000000000000000000, 0.000000000000000000, 0.000000000000000000 ) ) ;
#11651=CARTESIAN_POINT ( 'NONE',  ( 0.3367924244280819934, 2.254758922476410188, 8.300000000000000711 ) ) ;
#11652=VERTEX_POINT ( 'NONE', #2748 ) ;
#11656=PLANE ( 'NONE',  #803 ) ;
#11658=CARTESIAN_POINT ( 'NONE',  ( -1.889999999999999902, 8.500000000000000000, 0.6099999999999999867 ) ) ;
#11663=DIRECTION ( 'NONE',  ( 1.000000000000000000, -2.220446049250309876E-16, -6.049014748177260544E-16 ) ) ;
#11665=CARTESIAN_POINT ( 'NONE',  ( -1.899999999999999911, -2.607830583485260225E-17, -8.881784197001250351E-16 ) ) ;
#11667=ADVANCED_FACE ( 'NONE', ( #9870 ), #6721, .T. ) ;
#11669=LINE ( 'NONE', #14791, #12691 ) ;
#11682=EDGE_LOOP ( 'NONE', ( #12655, #3340, #3630, #8346 ) ) ;
#11686=ORIENTED_EDGE ( 'NONE', *, *, #5628, .F. ) ;
#11687=CARTESIAN_POINT ( 'NONE',  ( 1.899999999999999911, 3.500000000000000000, 0.6099999999999999867 ) ) ;
#11690=CARTESIAN_POINT ( 'NONE',  ( -1.889999999999999902, 4.100000000000000533, 3.000000000000000000 ) ) ;
#11695=ORIENTED_EDGE ( 'NONE', *, *, #18282, .F. ) ;
#11697=CARTESIAN_POINT ( 'NONE',  ( -0.8740908734716290596, 4.154758922476410099, 7.700000000000000178 ) ) ;
#11698=VERTEX_POINT ( 'NONE', #1446 ) ;
#11705=EDGE_LOOP ( 'NONE', ( #9024, #10267, #9078, #7156 ) ) ;
#11707=CARTESIAN_POINT ( 'NONE',  ( 0.5372984490435490645, 4.599999999999999645, 8.300000000000000711 ) ) ;
#11710=DIRECTION ( 'NONE',  ( 0.000000000000000000, -1.000000000000000000, 0.000000000000000000 ) ) ;
#11711=DIRECTION ( 'NONE',  ( -4.318427418585891014E-15, 2.220446049250309876E-16, -1.000000000000000000 ) ) ;
#11714=EDGE_CURVE ( 'NONE', #12160, #3824, #8927, .T. ) ;
#11718=ORIENTED_EDGE ( 'NONE', *, *, #13830, .T. ) ;
#11720=LINE ( 'NONE', #4574, #13677 ) ;
#11723=ORIENTED_EDGE ( 'NONE', *, *, #10848, .F. ) ;
#11727=CARTESIAN_POINT ( 'NONE',  ( 2.500000000000000000, 0.4000000000000000222, -2.399999999999999911 ) ) ;
#11736=AXIS2_PLACEMENT_3D ( 'NONE', #9272, #10761, #3709 ) ;
#11740=EDGE_CURVE ( 'NONE', #6769, #435, #4557, .T. ) ;
#11746=EDGE_CURVE ( 'NONE', #11546, #2090, #7456, .T. ) ;
#11748=VECTOR ( 'NONE', #11710, 1000.000000000000000 ) ;
#11752=CARTESIAN_POINT ( 'NONE',  ( -1.899999999999999911, 2.799999999999999822, 0.6099999999999999867 ) ) ;
#11757=VECTOR ( 'NONE', #11402, 1000.000000000000000 ) ;
#11759=VECTOR ( 'NONE', #7521, 1000.000000000000000 ) ;
#11765=VECTOR ( 'NONE', #11153, 1000.000000000000000 ) ;
#11773=AXIS2_PLACEMENT_3D ( 'NONE', #3358, #11611, #11892 ) ;
#11775=AXIS2_PLACEMENT_3D ( 'NONE', #179, #5657, #8616 ) ;
#11778=CARTESIAN_POINT ( 'NONE',  ( -1.289999999999999813, 7.900000000000003908, 3.000000000000002220 ) ) ;
#11780=VECTOR ( 'NONE', #6884, 1000.000000000000000 ) ;
#11788=VECTOR ( 'NONE', #1902, 1000.000000000000000 ) ;
#11791=CIRCLE ( 'NONE', #8252, 0.3999999999999999667 ) ;
#11792=AXIS2_PLACEMENT_3D ( 'NONE', #12338, #7796, #6589 ) ;
#11796=EDGE_CURVE ( 'NONE', #2787, #13022, #10397, .T. ) ;
#11798=CYLINDRICAL_SURFACE ( 'NONE', #2882, 0.7000000000000000666 ) ;
#11801=ORIENTED_EDGE ( 'NONE', *, *, #1780, .T. ) ;
#11806=LINE ( 'NONE', #14943, #3207 ) ;
#11810=AXIS2_PLACEMENT_3D ( 'NONE', #8450, #15766, #11502 ) ;
#11813=DIRECTION ( 'NONE',  ( 0.2721173643531200059, 0.9622640697945191723, 0.000000000000000000 ) ) ;
#11816=CARTESIAN_POINT ( 'NONE',  ( 1.899999999999999911, 3.500000000000000000, 0.6099999999999999867 ) ) ;
#11823=CIRCLE ( 'NONE', #3837, 1.100000000000000311 ) ;
#11825=DIRECTION ( 'NONE',  ( 8.326672684688670109E-16, 0.000000000000000000, 1.000000000000000000 ) ) ;
#11826=CARTESIAN_POINT ( 'NONE',  ( 2.500000000000000000, 8.500000000000000000, 0.6099999999999999867 ) ) ;
#11828=VERTEX_POINT ( 'NONE', #4398 ) ;
#11842=PLANE ( 'NONE',  #3711 ) ;
#11845=LINE ( 'NONE', #11651, #1783 ) ;
#11846=VERTEX_POINT ( 'NONE', #14571 ) ;
#11848=ORIENTED_EDGE ( 'NONE', *, *, #6133, .F. ) ;
#11854=EDGE_CURVE ( 'NONE', #17047, #6319, #14391, .T. ) ;
#11855=EDGE_CURVE ( 'NONE', #7200, #16687, #1885, .T. ) ;
#11865=DIRECTION ( 'NONE',  ( -4.485749594445070317E-16, 0.000000000000000000, -1.000000000000000000 ) ) ;
#11867=ORIENTED_EDGE ( 'NONE', *, *, #6178, .F. ) ;
#11881=EDGE_LOOP ( 'NONE', ( #17954, #1904, #7112, #3808 ) ) ;
#11882=CARTESIAN_POINT ( 'NONE',  ( 0.03000000000000110217, 11.40000000000000036, 7.649999999999999467 ) ) ;
#11886=ORIENTED_EDGE ( 'NONE', *, *, #11051, .T. ) ;
#11892=DIRECTION ( 'NONE',  ( -0.9622640697945192834, -0.2721173643531198949, 0.000000000000000000 ) ) ;
#11901=LINE ( 'NONE', #7819, #5838 ) ;
#11913=ORIENTED_EDGE ( 'NONE', *, *, #4590, .T. ) ;
#11914=FACE_OUTER_BOUND ( 'NONE', #11705, .T. ) ;
#11915=CYLINDRICAL_SURFACE ( 'NONE', #10572, 0.2000000000000000111 ) ;
#11916=FACE_OUTER_BOUND ( 'NONE', #4790, .T. ) ;
#11918=DIRECTION ( 'NONE',  ( 0.000000000000000000, 0.000000000000000000, 1.000000000000000000 ) ) ;
#11921=DIRECTION ( 'NONE',  ( 1.073215590470990073E-14, 1.000000000000000000, 0.000000000000000000 ) ) ;
#11922=CIRCLE ( 'NONE', #677, 0.7211102550927980248 ) ;
#11927=CARTESIAN_POINT ( 'NONE',  ( 2.500000000000000000, 7.299999999999999822, 0.6099999999999999867 ) ) ;
#11928=AXIS2_PLACEMENT_3D ( 'NONE', #15205, #9349, #17948 ) ;
#11929=CARTESIAN_POINT ( 'NONE',  ( 1.399999999999999911, 6.400000000000000355, 7.700000000000000178 ) ) ;
#11930=FACE_OUTER_BOUND ( 'NONE', #1275, .T. ) ;
#11936=CARTESIAN_POINT ( 'NONE',  ( -1.875000000000000000, 12.00000000000000000, 7.700000000000000178 ) ) ;
#11938=EDGE_CURVE ( 'NONE', #15780, #15692, #286, .T. ) ;
#11946=DIRECTION ( 'NONE',  ( 2.220446049250309876E-16, 1.000000000000000000, -1.192513461937156062E-31 ) ) ;
#11949=DIRECTION ( 'NONE',  ( -3.700743415417195042E-15, -3.289549702593060375E-15, 1.000000000000000000 ) ) ;
#11950=EDGE_LOOP ( 'NONE', ( #13004, #18123, #9230, #756 ) ) ;
#11951=CARTESIAN_POINT ( 'NONE',  ( -1.399999999999999911, 6.400000000000000355, 8.300000000000000711 ) ) ;
#11957=ORIENTED_EDGE ( 'NONE', *, *, #7660, .F. ) ;
#11961=CARTESIAN_POINT ( 'NONE',  ( -11.62823001646930088, 1.318530427328540049E-14, 0.5999999999999559019 ) ) ;
#11966=EDGE_CURVE ( 'NONE', #5781, #9046, #4052, .T. ) ;
#11970=EDGE_CURVE ( 'NONE', #7523, #4252, #15734, .T. ) ;
#11971=EDGE_CURVE ( 'NONE', #12787, #17179, #15374, .T. ) ;
#11972=VECTOR ( 'NONE', #9098, 1000.000000000000000 ) ;
#11973=ORIENTED_EDGE ( 'NONE', *, *, #5115, .F. ) ;
#11975=EDGE_CURVE ( 'NONE', #1650, #3610, #4322, .T. ) ;
#11976=ORIENTED_EDGE ( 'NONE', *, *, #199, .F. ) ;
#11988=EDGE_CURVE ( 'NONE', #11460, #14967, #10081, .T. ) ;
#11991=VERTEX_POINT ( 'NONE', #7209 ) ;
#11993=VECTOR ( 'NONE', #12711, 1000.000000000000000 ) ;
#11995=EDGE_LOOP ( 'NONE', ( #3178, #6675, #1414, #15731, #13440, #1185, #5639, #8626, #4168, #7563, #14974, #485, #2446, #9819, #3804, #7476, #6165, #2528, #17022, #1554, #338, #14443, #5725, #5661, #7788, #3650 ) ) ;
#11998=DIRECTION ( 'NONE',  ( 0.000000000000000000, 2.960594732333760372E-15, -1.000000000000000000 ) ) ;
#12002=CARTESIAN_POINT ( 'NONE',  ( -1.889999999999999902, 4.700000000000000178, 0.5999999999999999778 ) ) ;
#12003=DIRECTION ( 'NONE',  ( -4.898587196589410857E-16, -1.000000000000000000, 0.000000000000000000 ) ) ;
#12004=DIRECTION ( 'NONE',  ( -1.000000000000000000, 2.220446049250309876E-16, 0.000000000000000000 ) ) ;
#12010=CARTESIAN_POINT ( 'NONE',  ( -1.899999999999999911, 11.15000000000000036, 1.600000000000000089 ) ) ;
#12011=CARTESIAN_POINT ( 'NONE',  ( -2.500000000000000000, 10.00000000000000000, 1.600000000000000089 ) ) ;
#12014=ADVANCED_FACE ( 'NONE', ( #6928 ), #5727, .T. ) ;
#12018=CARTESIAN_POINT ( 'NONE',  ( -1.000000000000000000, 6.799999999999999822, 8.300000000000000711 ) ) ;
#12026=CIRCLE ( 'NONE', #3723, 0.5999999999999998668 ) ;
#12032=AXIS2_PLACEMENT_3D ( 'NONE', #3103, #7006, #15717 ) ;
#12043=VECTOR ( 'NONE', #15037, 1000.000000000000000 ) ;
#12045=DIRECTION ( 'NONE',  ( 0.000000000000000000, 0.000000000000000000, -1.000000000000000000 ) ) ;
#12046=ORIENTED_EDGE ( 'NONE', *, *, #18056, .T. ) ;
#12054=VECTOR ( 'NONE', #9397, 1000.000000000000000 ) ;
#12061=CIRCLE ( 'NONE', #4073, 0.04999999999999969746 ) ;
#12069=ORIENTED_EDGE ( 'NONE', *, *, #11855, .T. ) ;
#12071=VECTOR ( 'NONE', #6315, 1000.000000000000000 ) ;
#12076=EDGE_CURVE ( 'NONE', #15692, #3882, #14809, .T. ) ;
#12081=EDGE_CURVE ( 'NONE', #5973, #11546, #5907, .T. ) ;
#12084=DIRECTION ( 'NONE',  ( -1.000000000000000000, 1.480297366166879989E-15, 0.000000000000000000 ) ) ;
#12085=LINE ( 'NONE', #3451, #15831 ) ;
#12090=LINE ( 'NONE', #17708, #12989 ) ;
#12092=ORIENTED_EDGE ( 'NONE', *, *, #4253, .T. ) ;
#12093=DIRECTION ( 'NONE',  ( 4.440892098500620245E-16, 1.000000000000000000, 1.110223024625159992E-16 ) ) ;
#12094=( GEOMETRIC_REPRESENTATION_CONTEXT ( 3 ) GLOBAL_UNCERTAINTY_ASSIGNED_CONTEXT ( ( #6585 ) ) GLOBAL_UNIT_ASSIGNED_CONTEXT ( ( #12259, #17877, #11241 ) ) REPRESENTATION_CONTEXT ( 'NONE', 'WORKASPACE' ) );
#12102=ORIENTED_EDGE ( 'NONE', *, *, #6311, .T. ) ;
#12105=CARTESIAN_POINT ( 'NONE',  ( -1.899999999999999911, 8.500000000000000000, 0.6099999999999999867 ) ) ;
#12110=EDGE_LOOP ( 'NONE', ( #18214, #17337, #7579, #17261 ) ) ;
#12113=CARTESIAN_POINT ( 'NONE',  ( 1.850000000000000089, 0.7500000000000000000, 7.649999999999999467 ) ) ;
#12118=CARTESIAN_POINT ( 'NONE',  ( -1.000000000000000000, 5.400000000000000355, 7.700000000000000178 ) ) ;
#12120=ADVANCED_FACE ( 'NONE', ( #11914 ), #5993, .F. ) ;
#12129=ORIENTED_EDGE ( 'NONE', *, *, #2700, .T. ) ;
#12144=CARTESIAN_POINT ( 'NONE',  ( -0.8740908734716290596, 4.154758922476410099, 7.700000000000000178 ) ) ;
#12145=ORIENTED_EDGE ( 'NONE', *, *, #15265, .F. ) ;
#12152=ADVANCED_FACE ( 'NONE', ( #17533 ), #4861, .T. ) ;
#12160=VERTEX_POINT ( 'NONE', #14777 ) ;
#12162=FACE_OUTER_BOUND ( 'NONE', #14512, .T. ) ;
#12182=LINE ( 'NONE', #365, #2457 ) ;
#12187=ADVANCED_FACE ( 'NONE', ( #14513 ), #12942, .T. ) ;
#12188=VERTEX_POINT ( 'NONE', #7477 ) ;
#12190=PLANE ( 'NONE',  #4149 ) ;
#12194=CARTESIAN_POINT ( 'NONE',  ( 1.899999999999999911, 11.29999999999999893, 7.649999999999999467 ) ) ;
#12195=LINE ( 'NONE', #9026, #523 ) ;
#12200=DIRECTION ( 'NONE',  ( 0.000000000000000000, -1.000000000000000000, 0.000000000000000000 ) ) ;
#12201=PLANE ( 'NONE',  #1717 ) ;
#12204=DIRECTION ( 'NONE',  ( -4.318427418585891014E-15, 2.220446049250309876E-16, -1.000000000000000000 ) ) ;
#12221=ORIENTED_EDGE ( 'NONE', *, *, #13436, .F. ) ;
#12223=EDGE_CURVE ( 'NONE', #4252, #4577, #13204, .T. ) ;
#12226=CARTESIAN_POINT ( 'NONE',  ( -2.500000000000000000, 7.299999999999999822, 1.600000000000000089 ) ) ;
#12230=EDGE_CURVE ( 'NONE', #9094, #14730, #9025, .T. ) ;
#12233=EDGE_LOOP ( 'NONE', ( #4709, #7451, #8551, #16887 ) ) ;
#12237=ORIENTED_EDGE ( 'NONE', *, *, #1694, .F. ) ;
#12250=ORIENTED_EDGE ( 'NONE', *, *, #7833, .T. ) ;
#12251=AXIS2_PLACEMENT_3D ( 'NONE', #8530, #14179, #1497 ) ;
#12259=( LENGTH_UNIT ( ) NAMED_UNIT ( * ) SI_UNIT ( .MILLI., .METRE. ) );
#12262=ORIENTED_EDGE ( 'NONE', *, *, #536, .F. ) ;
#12267=ADVANCED_FACE ( 'NONE', ( #13679 ), #17725, .T. ) ;
#12277=VERTEX_POINT ( 'NONE', #5345 ) ;
#12279=CARTESIAN_POINT ( 'NONE',  ( 4.265698758777729940E-16, 2.350000000000000089, 7.700000000000000178 ) ) ;
#12282=ORIENTED_EDGE ( 'NONE', *, *, #9492, .T. ) ;
#12291=DIRECTION ( 'NONE',  ( 0.000000000000000000, 0.000000000000000000, -1.000000000000000000 ) ) ;
#12297=ORIENTED_EDGE ( 'NONE', *, *, #4384, .F. ) ;
#12304=DIRECTION ( 'NONE',  ( 0.000000000000000000, 1.000000000000000000, -1.110223024625159745E-16 ) ) ;
#12309=CIRCLE ( 'NONE', #4310, 0.3999999999999999667 ) ;
#12310=EDGE_CURVE ( 'NONE', #6769, #14398, #16547, .T. ) ;
#12317=CARTESIAN_POINT ( 'NONE',  ( -1.899999999999999911, 2.799999999999999822, 0.6099999999999999867 ) ) ;
#12319=EDGE_CURVE ( 'NONE', #5474, #14839, #13481, .T. ) ;
#12323=VECTOR ( 'NONE', #12084, 1000.000000000000000 ) ;
#12324=LINE ( 'NONE', #12415, #9404 ) ;
#12326=VERTEX_POINT ( 'NONE', #12002 ) ;
#12327=FACE_OUTER_BOUND ( 'NONE', #4769, .T. ) ;
#12328=DIRECTION ( 'NONE',  ( 0.000000000000000000, 0.000000000000000000, -1.000000000000000000 ) ) ;
#12329=ORIENTED_EDGE ( 'NONE', *, *, #1729, .T. ) ;
#12330=ORIENTED_EDGE ( 'NONE', *, *, #7501, .T. ) ;
#12331=VECTOR ( 'NONE', #13048, 1000.000000000000000 ) ;
#12332=UNCERTAINTY_MEASURE_WITH_UNIT (LENGTH_MEASURE( 1.000000000000000082E-05 ), #9621, 'distance_accuracy_value', 'NONE');
#12336=ADVANCED_FACE ( 'NONE', ( #6438 ), #10708, .F. ) ;
#12338=CARTESIAN_POINT ( 'NONE',  ( -1.889999999999999902, 7.900000000000000355, 2.126957699879220439E-15 ) ) ;
#12345=ORIENTED_EDGE ( 'NONE', *, *, #8601, .T. ) ;
#12350=VECTOR ( 'NONE', #16452, 1000.000000000000000 ) ;
#12351=ORIENTED_EDGE ( 'NONE', *, *, #5085, .F. ) ;
#12352=DIRECTION ( 'NONE',  ( 0.000000000000000000, -1.000000000000000000, 2.775557561562890365E-16 ) ) ;
#12355=VECTOR ( 'NONE', #10370, 1000.000000000000000 ) ;
#12362=CIRCLE ( 'NONE', #1418, 0.5291502622129179434 ) ;
#12363=CARTESIAN_POINT ( 'NONE',  ( -2.500000000000000000, 11.29999999999999893, 7.649999999999999467 ) ) ;
#12365=DIRECTION ( 'NONE',  ( 1.059690869644410208E-14, 1.000000000000000000, -1.041146930477340028E-32 ) ) ;
#12372=CIRCLE ( 'NONE', #14717, 0.5999999999999998668 ) ;
#12378=CIRCLE ( 'NONE', #13855, 0.3500000000000001998 ) ;
#12379=DIRECTION ( 'NONE',  ( -1.000000000000000000, 0.000000000000000000, 7.401486830834370362E-16 ) ) ;
#12382=ORIENTED_EDGE ( 'NONE', *, *, #2565, .F. ) ;
#12385=CIRCLE ( 'NONE', #9711, 0.5999999999999998668 ) ;
#12388=FACE_OUTER_BOUND ( 'NONE', #16172, .T. ) ;
#12391=CARTESIAN_POINT ( 'NONE',  ( 1.600000000000000089, 1.928341960302230101E-16, 4.000000000000000000 ) ) ;
#12392=ORIENTED_EDGE ( 'NONE', *, *, #1913, .T. ) ;
#12397=FACE_OUTER_BOUND ( 'NONE', #7233, .T. ) ;
#12401=CARTESIAN_POINT ( 'NONE',  ( 2.500000000000000000, 4.700000000000000178, 1.600000000000000089 ) ) ;
#12404=DIRECTION ( 'NONE',  ( 0.000000000000000000, 1.000000000000000000, 0.000000000000000000 ) ) ;
#12407=DIRECTION ( 'NONE',  ( 1.850371707708589879E-16, 0.000000000000000000, -1.000000000000000000 ) ) ;
#12410=LINE ( 'NONE', #9623, #18079 ) ;
#12415=CARTESIAN_POINT ( 'NONE',  ( 1.800000000000000044, 11.40000000000000036, 7.649999999999999467 ) ) ;
#12417=EDGE_LOOP ( 'NONE', ( #14007, #14249, #4548, #11512 ) ) ;
#12418=EDGE_CURVE ( 'NONE', #12787, #12326, #4958, .T. ) ;
#12425=EDGE_CURVE ( 'NONE', #4252, #12680, #6724, .T. ) ;
#12442=EDGE_LOOP ( 'NONE', ( #16786, #7384, #10461, #1955 ) ) ;
#12443=EDGE_CURVE ( 'NONE', #9752, #16414, #703, .T. ) ;
#12459=CYLINDRICAL_SURFACE ( 'NONE', #11323, 0.6000000000000000888 ) ;
#12460=DIRECTION ( 'NONE',  ( 0.9622640697945186172, -0.2721173643531222264, 0.000000000000000000 ) ) ;
#12469=CARTESIAN_POINT ( 'NONE',  ( -1.899999999999999911, 0.7211102550927970256, 7.649999999999999467 ) ) ;
#12483=PLANE ( 'NONE',  #8365 ) ;
#12487=ORIENTED_EDGE ( 'NONE', *, *, #2702, .F. ) ;
#12490=DIRECTION ( 'NONE',  ( -1.000000000000000000, -4.336808689942016947E-15, 1.084202172485504276E-14 ) ) ;
#12493=ORIENTED_EDGE ( 'NONE', *, *, #8512, .T. ) ;
#12509=ORIENTED_EDGE ( 'NONE', *, *, #15046, .F. ) ;
#12513=DIRECTION ( 'NONE',  ( 0.000000000000000000, 0.000000000000000000, -1.000000000000000000 ) ) ;
#12517=PLANE ( 'NONE',  #14964 ) ;
#12518=DIRECTION ( 'NONE',  ( 0.000000000000000000, -1.387778780781449866E-16, -1.000000000000000000 ) ) ;
#12525=EDGE_LOOP ( 'NONE', ( #13203, #5522 ) ) ;
#12540=ADVANCED_FACE ( 'NONE', ( #14654 ), #8747, .T. ) ;
#12542=CARTESIAN_POINT ( 'NONE',  ( -2.500000000000000000, 11.15000000000000036, 1.600000000000000089 ) ) ;
#12547=CARTESIAN_POINT ( 'NONE',  ( 1.875000000000000000, 11.25000000000000000, 8.300000000000000711 ) ) ;
#12548=ORIENTED_EDGE ( 'NONE', *, *, #15036, .T. ) ;
#12550=CARTESIAN_POINT ( 'NONE',  ( 2.500000000000000000, 0.8000000000000000444, -1.674850734291659957E-15 ) ) ;
#12558=CARTESIAN_POINT ( 'NONE',  ( 2.241103642439659443E-15, 9.099999999999999645, 8.300000000000000711 ) ) ;
#12559=EDGE_LOOP ( 'NONE', ( #15334, #10235, #13756, #17824 ) ) ;
#12565=LINE ( 'NONE', #11174, #3434 ) ;
#12578=ORIENTED_EDGE ( 'NONE', *, *, #3574, .F. ) ;
#12581=LINE ( 'NONE', #11198, #13242 ) ;
#12583=DIRECTION ( 'NONE',  ( -0.2721173643531200059, 0.9622640697945191723, 0.000000000000000000 ) ) ;
#12584=DIRECTION ( 'NONE',  ( -1.000000000000000000, 0.000000000000000000, 0.000000000000000000 ) ) ;
#12593=ORIENTED_EDGE ( 'NONE', *, *, #8924, .T. ) ;
#12596=CARTESIAN_POINT ( 'NONE',  ( -1.899999999999999911, 11.29999999999999893, 7.649999999999999467 ) ) ;
#12597=ADVANCED_FACE ( 'NONE', ( #17334 ), #4664, .F. ) ;
#12601=AXIS2_PLACEMENT_3D ( 'NONE', #2798, #18225, #27 ) ;
#12605=DIRECTION ( 'NONE',  ( -1.000000000000000000, 1.224646799147350002E-16, 0.000000000000000000 ) ) ;
#12606=AXIS2_PLACEMENT_3D ( 'NONE', #3694, #16481, #16583 ) ;
#12612=CARTESIAN_POINT ( 'NONE',  ( 2.500000000000000000, 9.199999999999999289, 0.6099999999999999867 ) ) ;
#12624=VERTEX_POINT ( 'NONE', #10400 ) ;
#12631=CARTESIAN_POINT ( 'NONE',  ( -2.616666666666669805, -4.318079751576579732E-16, 4.000000000000000000 ) ) ;
#12637=FACE_OUTER_BOUND ( 'NONE', #13684, .T. ) ;
#12638=VECTOR ( 'NONE', #11490, 1000.000000000000000 ) ;
#12644=CIRCLE ( 'NONE', #1122, 0.4166666666666670737 ) ;
#12647=EDGE_LOOP ( 'NONE', ( #9067, #11686, #12237, #5623 ) ) ;
#12648=EDGE_CURVE ( 'NONE', #7773, #9755, #1968, .T. ) ;
#12651=ADVANCED_FACE ( 'NONE', ( #9091 ), #9478, .T. ) ;
#12653=LINE ( 'NONE', #5711, #5239 ) ;
#12655=ORIENTED_EDGE ( 'NONE', *, *, #1806, .F. ) ;
#12658=CIRCLE ( 'NONE', #15619, 0.4166666666666669072 ) ;
#12666=CIRCLE ( 'NONE', #7343, 0.3999999999999999667 ) ;
#12673=ORIENTED_EDGE ( 'NONE', *, *, #7007, .F. ) ;
#12678=CARTESIAN_POINT ( 'NONE',  ( 4.265698758777729940E-16, 2.350000000000000089, 8.300000000000000711 ) ) ;
#12680=VERTEX_POINT ( 'NONE', #4838 ) ;
#12685=DIRECTION ( 'NONE',  ( -1.708035422500239940E-16, -1.000000000000000000, -8.540177112501199701E-17 ) ) ;
#12689=VECTOR ( 'NONE', #16010, 1000.000000000000000 ) ;
#12691=VECTOR ( 'NONE', #11496, 1000.000000000000000 ) ;
#12694=CARTESIAN_POINT ( 'NONE',  ( 1.289999999999999813, 7.900000000000003908, 0.6000000000000025313 ) ) ;
#12700=CARTESIAN_POINT ( 'NONE',  ( 1.289999999999999813, 4.099999999999999645, 6.203059698991501599E-15 ) ) ;
#12701=ORIENTED_EDGE ( 'NONE', *, *, #7660, .T. ) ;
#12711=DIRECTION ( 'NONE',  ( 1.930822651522009842E-16, 1.000000000000000000, -1.268826313857319964E-16 ) ) ;
#12719=FACE_OUTER_BOUND ( 'NONE', #6051, .T. ) ;
#12720=VERTEX_POINT ( 'NONE', #16141 ) ;
#12731=VECTOR ( 'NONE', #11279, 1000.000000000000000 ) ;
#12734=FACE_OUTER_BOUND ( 'NONE', #16515, .T. ) ;
#12738=ORIENTED_EDGE ( 'NONE', *, *, #3686, .T. ) ;
#12741=CARTESIAN_POINT ( 'NONE',  ( -2.500000000000000000, 9.199999999999999289, 0.6099999999999999867 ) ) ;
#12744=VECTOR ( 'NONE', #14975, 1000.000000000000000 ) ;
#12747=VERTEX_POINT ( 'NONE', #16219 ) ;
#12749=DIRECTION ( 'NONE',  ( 1.000000000000000000, 0.000000000000000000, 0.000000000000000000 ) ) ;
#12750=DIRECTION ( 'NONE',  ( 1.000000000000000000, 0.000000000000000000, 0.000000000000000000 ) ) ;
#12752=DIRECTION ( 'NONE',  ( -1.000000000000000000, 0.000000000000000000, 0.000000000000000000 ) ) ;
#12757=ADVANCED_FACE ( 'NONE', ( #7884 ), #4814, .T. ) ;
#12758=CARTESIAN_POINT ( 'NONE',  ( -1.599999999999880185, 11.40000000000000036, -2.399999999999999911 ) ) ;
#12764=DIRECTION ( 'NONE',  ( 3.007035789127644200E-16, 1.000000000000000000, -1.202814315651057680E-15 ) ) ;
#12765=DIRECTION ( 'NONE',  ( 0.000000000000000000, 0.000000000000000000, 1.000000000000000000 ) ) ;
#12773=ADVANCED_FACE ( 'NONE', ( #576 ), #3527, .T. ) ;
#12776=LINE ( 'NONE', #11016, #1217 ) ;
#12783=PLANE ( 'NONE',  #15863 ) ;
#12786=CARTESIAN_POINT ( 'NONE',  ( 1.899999999999999911, 11.25000000000000000, 7.649999999999999467 ) ) ;
#12787=VERTEX_POINT ( 'NONE', #13347 ) ;
#12789=VERTEX_POINT ( 'NONE', #3422 ) ;
#12795=DIRECTION ( 'NONE',  ( 0.000000000000000000, -1.000000000000000000, 2.775557561562900226E-16 ) ) ;
#12796=DIRECTION ( 'NONE',  ( -5.551115123125780730E-16, 0.000000000000000000, -1.000000000000000000 ) ) ;
#12799=EDGE_CURVE ( 'NONE', #1178, #14262, #6494, .T. ) ;
#12800=DIRECTION ( 'NONE',  ( 0.000000000000000000, -1.000000000000000000, 1.807003620809174385E-16 ) ) ;
#12801=DIRECTION ( 'NONE',  ( -3.042833474898580443E-15, 3.289549702593060178E-16, 1.000000000000000000 ) ) ;
#12808=ORIENTED_EDGE ( 'NONE', *, *, #3469, .T. ) ;
#12811=ORIENTED_EDGE ( 'NONE', *, *, #17166, .F. ) ;
#12817=VERTEX_POINT ( 'NONE', #6587 ) ;
#12827=CARTESIAN_POINT ( 'NONE',  ( 0.5372984490435490645, 4.250000000000000000, 7.700000000000000178 ) ) ;
#12835=CARTESIAN_POINT ( 'NONE',  ( -1.899999999999999911, 0.7500000000000000000, 7.649999999999999467 ) ) ;
#12840=CARTESIAN_POINT ( 'NONE',  ( -2.616666666666669805, -2.774341069716839796E-16, 7.649999999999999467 ) ) ;
#12847=LINE ( 'NONE', #5807, #12731 ) ;
#12851=DIRECTION ( 'NONE',  ( 0.000000000000000000, 1.000000000000000000, 2.775557561562890365E-16 ) ) ;
#12854=ORIENTED_EDGE ( 'NONE', *, *, #379, .T. ) ;
#12860=AXIS2_PLACEMENT_3D ( 'NONE', #6468, #6650, #12304 ) ;
#12866=DIRECTION ( 'NONE',  ( -1.618168325422125073E-46, -1.000000000000000000, -1.110223024625159992E-16 ) ) ;
#12869=ORIENTED_EDGE ( 'NONE', *, *, #16718, .F. ) ;
#12873=LINE ( 'NONE', #9825, #2619 ) ;
#12875=ORIENTED_EDGE ( 'NONE', *, *, #4708, .F. ) ;
#12887=VECTOR ( 'NONE', #15312, 1000.000000000000000 ) ;
#12895=EDGE_LOOP ( 'NONE', ( #5358, #6506, #13966, #8067 ) ) ;
#12896=DIRECTION ( 'NONE',  ( 6.083413833562510128E-16, -1.647588903766459698E-16, 1.000000000000000000 ) ) ;
#12903=EDGE_LOOP ( 'NONE', ( #10752, #7546, #4640, #1245 ) ) ;
#12906=VERTEX_POINT ( 'NONE', #4080 ) ;
#12907=DIRECTION ( 'NONE',  ( 7.273661547324610053E-16, -6.123233995736789455E-17, 1.000000000000000000 ) ) ;
#12911=DIRECTION ( 'NONE',  ( 0.000000000000000000, 0.000000000000000000, -1.000000000000000000 ) ) ;
#12914=ORIENTED_EDGE ( 'NONE', *, *, #7770, .F. ) ;
#12923=LINE ( 'NONE', #13016, #15606 ) ;
#12926=DIRECTION ( 'NONE',  ( 6.123233995736769734E-17, 2.493473113004670213E-16, 1.000000000000000000 ) ) ;
#12931=CIRCLE ( 'NONE', #3746, 1.000000000000000000 ) ;
#12932=DIRECTION ( 'NONE',  ( 1.000000000000000000, 0.000000000000000000, 0.000000000000000000 ) ) ;
#12936=FACE_OUTER_BOUND ( 'NONE', #2750, .T. ) ;
#12940=AXIS2_PLACEMENT_3D ( 'NONE', #17339, #12926, #7380 ) ;
#12942=PLANE ( 'NONE',  #1210 ) ;
#12945=VECTOR ( 'NONE', #6180, 1000.000000000000000 ) ;
#12957=DIRECTION ( 'NONE',  ( 0.9622640697945186172, -0.2721173643531222264, 0.000000000000000000 ) ) ;
#12959=DIRECTION ( 'NONE',  ( 1.480297366166879989E-15, 1.000000000000000000, 0.000000000000000000 ) ) ;
#12962=DIRECTION ( 'NONE',  ( 0.000000000000000000, -1.000000000000000000, -8.540177112501209562E-17 ) ) ;
#12967=ORIENTED_EDGE ( 'NONE', *, *, #14756, .F. ) ;
#12970=FACE_OUTER_BOUND ( 'NONE', #15754, .T. ) ;
#12974=VECTOR ( 'NONE', #298, 1000.000000000000000 ) ;
#12975=CARTESIAN_POINT ( 'NONE',  ( -1.899999999999999911, 9.199999999999999289, 0.6099999999999999867 ) ) ;
#12981=CARTESIAN_POINT ( 'NONE',  ( 2.500000000000000000, 10.00000000000000000, 1.600000000000000089 ) ) ;
#12982=ADVANCED_FACE ( 'NONE', ( #8354 ), #15212, .T. ) ;
#12989=VECTOR ( 'NONE', #5039, 1000.000000000000000 ) ;
#12994=ORIENTED_EDGE ( 'NONE', *, *, #15426, .T. ) ;
#12998=EDGE_CURVE ( 'NONE', #2042, #11364, #1132, .T. ) ;
#13000=AXIS2_PLACEMENT_3D ( 'NONE', #12144, #6768, #17763 ) ;
#13002=LINE ( 'NONE', #14381, #1116 ) ;
#13003=EDGE_CURVE ( 'NONE', #13806, #6568, #3899, .T. ) ;
#13004=ORIENTED_EDGE ( 'NONE', *, *, #17183, .T. ) ;
#13005=FACE_OUTER_BOUND ( 'NONE', #5708, .T. ) ;
#13013=CIRCLE ( 'NONE', #5019, 1.000000000000000000 ) ;
#13016=CARTESIAN_POINT ( 'NONE',  ( -1.899999999999999911, 2.000000000000000000, -2.537652627714639929E-16 ) ) ;
#13021=EDGE_CURVE ( 'NONE', #37, #4379, #8264, .T. ) ;
#13022=VERTEX_POINT ( 'NONE', #12596 ) ;
#13023=VECTOR ( 'NONE', #8743, 1000.000000000000000 ) ;
#13024=LINE ( 'NONE', #15898, #6155 ) ;
#13027=LINE ( 'NONE', #7290, #3270 ) ;
#13029=ORIENTED_EDGE ( 'NONE', *, *, #17323, .F. ) ;
#13032=CARTESIAN_POINT ( 'NONE',  ( -1.889999999999999902, 4.100000000000000533, 0.5999999999999999778 ) ) ;
#13035=VECTOR ( 'NONE', #13964, 1000.000000000000000 ) ;
#13042=EDGE_CURVE ( 'NONE', #8865, #5991, #1220, .T. ) ;
#13048=DIRECTION ( 'NONE',  ( -3.700743415417190309E-15, 0.000000000000000000, -1.000000000000000000 ) ) ;
#13049=LINE ( 'NONE', #13313, #18012 ) ;
#13053=CARTESIAN_POINT ( 'NONE',  ( 1.000000000000000000, 5.400000000000000355, 7.700000000000000178 ) ) ;
#13068=DIRECTION ( 'NONE',  ( 1.000000000000000000, 0.000000000000000000, 0.000000000000000000 ) ) ;
#13071=EDGE_LOOP ( 'NONE', ( #80, #1391, #8749, #2530 ) ) ;
#13085=ADVANCED_FACE ( 'NONE', ( #6643 ), #13501, .T. ) ;
#13092=ORIENTED_EDGE ( 'NONE', *, *, #16940, .F. ) ;
#13093=CARTESIAN_POINT ( 'NONE',  ( -1.850000000000000089, 0.7500000000000000000, 7.649999999999999467 ) ) ;
#13095=ADVANCED_FACE ( 'NONE', ( #9138 ), #17919, .T. ) ;
#13097=CARTESIAN_POINT ( 'NONE',  ( 2.500000000000000000, 2.000000000000000000, -1.695950706916410117E-15 ) ) ;
#13101=VECTOR ( 'NONE', #4228, 1000.000000000000000 ) ;
#13104=ADVANCED_FACE ( 'NONE', ( #1006 ), #14797, .F. ) ;
#13110=CARTESIAN_POINT ( 'NONE',  ( -1.899999999999999911, 11.29999999999999893, 1.600000000000000089 ) ) ;
#13112=EDGE_CURVE ( 'NONE', #15044, #2252, #9433, .T. ) ;
#13117=CARTESIAN_POINT ( 'NONE',  ( -0.03000000000000000236, 11.40000000000000036, 6.759657321199410264E-76 ) ) ;
#13123=ORIENTED_EDGE ( 'NONE', *, *, #4253, .F. ) ;
#13140=EDGE_LOOP ( 'NONE', ( #4186, #5136, #10721 ) ) ;
#13143=CARTESIAN_POINT ( 'NONE',  ( -1.399999999999999911, 5.799999999999999822, 8.300000000000000711 ) ) ;
#13146=VERTEX_POINT ( 'NONE', #6556 ) ;
#13148=CARTESIAN_POINT ( 'NONE',  ( 1.899999999999999911, 0.7211102550927980248, 4.000000000000000000 ) ) ;
#13153=CARTESIAN_POINT ( 'NONE',  ( -2.500000000000000000, 4.700000000000000178, 1.600000000000000089 ) ) ;
#13154=FACE_OUTER_BOUND ( 'NONE', #17837, .T. ) ;
#13155=ORIENTED_EDGE ( 'NONE', *, *, #6580, .F. ) ;
#13158=EDGE_LOOP ( 'NONE', ( #12129, #11522, #9029 ) ) ;
#13159=ORIENTED_EDGE ( 'NONE', *, *, #7896, .T. ) ;
#13166=VECTOR ( 'NONE', #13719, 1000.000000000000000 ) ;
#13169=VERTEX_POINT ( 'NONE', #16280 ) ;
#13170=FACE_OUTER_BOUND ( 'NONE', #18186, .T. ) ;
#13186=DIRECTION ( 'NONE',  ( -1.000000000000000000, 0.000000000000000000, 0.000000000000000000 ) ) ;
#13190=AXIS2_PLACEMENT_3D ( 'NONE', #11690, #8651, #8914 ) ;
#13193=EDGE_CURVE ( 'NONE', #13368, #11846, #10812, .T. ) ;
#13203=ORIENTED_EDGE ( 'NONE', *, *, #7009, .T. ) ;
#13204=LINE ( 'NONE', #525, #1813 ) ;
#13218=LINE ( 'NONE', #13666, #17312 ) ;
#13221=AXIS2_PLACEMENT_3D ( 'NONE', #13843, #1337, #17988 ) ;
#13223=VECTOR ( 'NONE', #14189, 1000.000000000000000 ) ;
#13225=DIRECTION ( 'NONE',  ( 0.000000000000000000, 0.000000000000000000, 1.000000000000000000 ) ) ;
#13226=VERTEX_POINT ( 'NONE', #4043 ) ;
#13234=EDGE_LOOP ( 'NONE', ( #8231, #1523, #3397, #6327 ) ) ;
#13242=VECTOR ( 'NONE', #12407, 1000.000000000000000 ) ;
#13246=PLANE ( 'NONE',  #5010 ) ;
#13249=VECTOR ( 'NONE', #12352, 1000.000000000000000 ) ;
#13252=EDGE_LOOP ( 'NONE', ( #17716, #10530, #4606, #17903 ) ) ;
#13256=DIRECTION ( 'NONE',  ( 1.000000000000000000, -8.673617379884035472E-15, 0.000000000000000000 ) ) ;
#13268=ORIENTED_EDGE ( 'NONE', *, *, #7900, .F. ) ;
#13271=VERTEX_POINT ( 'NONE', #18180 ) ;
#13274=DIRECTION ( 'NONE',  ( 1.000000000000000000, 0.000000000000000000, 0.000000000000000000 ) ) ;
#13276=EDGE_CURVE ( 'NONE', #16395, #1884, #5719, .T. ) ;
#13279=VERTEX_POINT ( 'NONE', #8225 ) ;
#13280=AXIS2_PLACEMENT_3D ( 'NONE', #16961, #4271, #14362 ) ;
#13282=DIRECTION ( 'NONE',  ( 4.265713465516724418E-16, 1.000000000000000000, -8.531426931033448836E-16 ) ) ;
#13287=ORIENTED_EDGE ( 'NONE', *, *, #3008, .F. ) ;
#13289=EDGE_LOOP ( 'NONE', ( #11266, #4050, #8431, #8327 ) ) ;
#13292=DIRECTION ( 'NONE',  ( 0.000000000000000000, -1.000000000000000000, 0.000000000000000000 ) ) ;
#13294=EDGE_CURVE ( 'NONE', #2455, #10006, #13957, .T. ) ;
#13297=VERTEX_POINT ( 'NONE', #2668 ) ;
#13305=DIRECTION ( 'NONE',  ( 0.000000000000000000, -5.224578939412490694E-16, 1.000000000000000000 ) ) ;
#13312=DIRECTION ( 'NONE',  ( -1.000000000000000000, 0.000000000000000000, 0.000000000000000000 ) ) ;
#13313=CARTESIAN_POINT ( 'NONE',  ( 1.899999999999999911, 0.7500000000000000000, 7.649999999999999467 ) ) ;
#13319=LINE ( 'NONE', #635, #9378 ) ;
#13326=EDGE_CURVE ( 'NONE', #1947, #16854, #15455, .T. ) ;
#13327=CARTESIAN_POINT ( 'NONE',  ( 1.899999999999999911, 6.661338147750959950E-17, 9.955530934770520091 ) ) ;
#13328=LINE ( 'NONE', #10179, #14403 ) ;
#13336=LINE ( 'NONE', #13427, #2621 ) ;
#13339=VERTEX_POINT ( 'NONE', #5983 ) ;
#13343=ORIENTED_EDGE ( 'NONE', *, *, #8924, .F. ) ;
#13347=CARTESIAN_POINT ( 'NONE',  ( -1.889999999999999902, 3.500000000000000000, 0.5999999999999999778 ) ) ;
#13353=EDGE_LOOP ( 'NONE', ( #17515, #55, #15852, #14997 ) ) ;
#13357=VERTEX_POINT ( 'NONE', #17087 ) ;
#13361=ORIENTED_EDGE ( 'NONE', *, *, #5518, .F. ) ;
#13362=CARTESIAN_POINT ( 'NONE',  ( -1.800000000000000044, 12.00000000000000000, 7.649999999999999467 ) ) ;
#13368=VERTEX_POINT ( 'NONE', #7386 ) ;
#13370=DIRECTION ( 'NONE',  ( 1.850371707708589879E-16, 1.000000000000000000, -9.251858538542959255E-17 ) ) ;
#13371=CARTESIAN_POINT ( 'NONE',  ( 1.889999999999999902, 8.500000000000000000, 4.204760881734880211E-16 ) ) ;
#13373=DIRECTION ( 'NONE',  ( 1.000000000000000000, 0.000000000000000000, 0.000000000000000000 ) ) ;
#13376=ORIENTED_EDGE ( 'NONE', *, *, #13452, .F. ) ;
#13377=DIRECTION ( 'NONE',  ( 2.775557561562900226E-16, 1.000000000000000000, -2.775557561562900226E-16 ) ) ;
#13380=VECTOR ( 'NONE', #9325, 1000.000000000000000 ) ;
#13386=ORIENTED_EDGE ( 'NONE', *, *, #1332, .F. ) ;
#13389=CARTESIAN_POINT ( 'NONE',  ( 2.500000000000000000, 2.799999999999999822, 1.600000000000000089 ) ) ;
#13390=DIRECTION ( 'NONE',  ( -1.000000000000000000, 4.743384504624081899E-16, 0.000000000000000000 ) ) ;
#13391=CARTESIAN_POINT ( 'NONE',  ( 1.899999999999999911, 2.481229107598850043E-16, 7.649999999999999467 ) ) ;
#13395=DIRECTION ( 'NONE',  ( 1.000000000000000000, -1.054711873393900133E-14, 1.850371707708589879E-16 ) ) ;
#13397=DIRECTION ( 'NONE',  ( 0.000000000000000000, -1.000000000000000000, -1.332267629550190018E-15 ) ) ;
#13400=CARTESIAN_POINT ( 'NONE',  ( 1.889999999999999902, 7.900000000000000355, 0.5999999999999999778 ) ) ;
#13404=CARTESIAN_POINT ( 'NONE',  ( 0.2000000000000000111, -2.449293598294700066E-17, 8.300000000000000711 ) ) ;
#13409=LINE ( 'NONE', #9438, #4429 ) ;
#13413=VERTEX_POINT ( 'NONE', #14505 ) ;
#13414=LINE ( 'NONE', #727, #7013 ) ;
#13417=VERTEX_POINT ( 'NONE', #7548 ) ;
#13427=CARTESIAN_POINT ( 'NONE',  ( 1.899999999999999911, 9.199999999999999289, 1.600000000000000089 ) ) ;
#13429=CARTESIAN_POINT ( 'NONE',  ( 1.875000000000000000, 0.7500000000000000000, 8.300000000000000711 ) ) ;
#13430=ORIENTED_EDGE ( 'NONE', *, *, #14397, .F. ) ;
#13436=EDGE_CURVE ( 'NONE', #3824, #2153, #7286, .T. ) ;
#13437=ORIENTED_EDGE ( 'NONE', *, *, #320, .F. ) ;
#13438=ADVANCED_FACE ( 'NONE', ( #17254 ), #8670, .F. ) ;
#13440=ORIENTED_EDGE ( 'NONE', *, *, #8682, .T. ) ;
#13445=ORIENTED_EDGE ( 'NONE', *, *, #6228, .F. ) ;
#13452=EDGE_CURVE ( 'NONE', #10145, #4379, #13024, .T. ) ;
#13459=LINE ( 'NONE', #776, #3699 ) ;
#13462=DIRECTION ( 'NONE',  ( 5.872254014546280719E-16, -5.872254014546280719E-16, 1.000000000000000000 ) ) ;
#13463=CARTESIAN_POINT ( 'NONE',  ( -11.62823001646920140, -8.079925217494299891E-16, -2.930988785010409480E-14 ) ) ;
#13474=ORIENTED_EDGE ( 'NONE', *, *, #14335, .T. ) ;
#13477=DIRECTION ( 'NONE',  ( 0.000000000000000000, 0.000000000000000000, 1.000000000000000000 ) ) ;
#13479=ORIENTED_EDGE ( 'NONE', *, *, #4617, .F. ) ;
#13481=LINE ( 'NONE', #9508, #8008 ) ;
#13485=AXIS2_PLACEMENT_3D ( 'NONE', #4053, #9708, #8233 ) ;
#13488=CARTESIAN_POINT ( 'NONE',  ( 1.271629043573289915E-13, 12.00000000000000000, -5.003920418925160367E-17 ) ) ;
#13491=AXIS2_PLACEMENT_3D ( 'NONE', #10996, #5440, #11170 ) ;
#13492=DIRECTION ( 'NONE',  ( 0.000000000000000000, 0.000000000000000000, 1.000000000000000000 ) ) ;
#13494=VECTOR ( 'NONE', #7586, 1000.000000000000000 ) ;
#13501=PLANE ( 'NONE',  #4673 ) ;
#13511=DIRECTION ( 'NONE',  ( 7.006492321624090022E-46, 1.000000000000000000, 1.332267629550190018E-15 ) ) ;
#13512=VECTOR ( 'NONE', #6012, 1000.000000000000000 ) ;
#13513=ORIENTED_EDGE ( 'NONE', *, *, #2746, .T. ) ;
#13514=VECTOR ( 'NONE', #6355, 1000.000000000000000 ) ;
#13516=ORIENTED_EDGE ( 'NONE', *, *, #12799, .F. ) ;
#13526=CARTESIAN_POINT ( 'NONE',  ( -1.800000000000000044, 11.29999999999999893, 7.649999999999999467 ) ) ;
#13528=LINE ( 'NONE', #2039, #5277 ) ;
#13530=DIRECTION ( 'NONE',  ( -1.000000000000000000, 0.000000000000000000, 0.000000000000000000 ) ) ;
#13536=VECTOR ( 'NONE', #1820, 1000.000000000000000 ) ;
#13541=ORIENTED_EDGE ( 'NONE', *, *, #5918, .F. ) ;
#13543=EDGE_CURVE ( 'NONE', #6171, #10426, #8940, .T. ) ;
#13544=AXIS2_PLACEMENT_3D ( 'NONE', #6858, #5188, #18118 ) ;
#13548=AXIS2_PLACEMENT_3D ( 'NONE', #7187, #8571, #2650 ) ;
#13552=ORIENTED_EDGE ( 'NONE', *, *, #14944, .F. ) ;
#13562=EDGE_CURVE ( 'NONE', #12680, #8572, #3208, .T. ) ;
#13567=CARTESIAN_POINT ( 'NONE',  ( 4.898587196589409994E-17, 0.1000000000000000056, 8.300000000000000711 ) ) ;
#13568=EDGE_CURVE ( 'NONE', #9192, #396, #10413, .T. ) ;
#13575=VERTEX_POINT ( 'NONE', #1556 ) ;
#13576=LINE ( 'NONE', #9401, #5509 ) ;
#13577=DIRECTION ( 'NONE',  ( 1.000000000000000000, -8.673617379884035472E-15, 0.000000000000000000 ) ) ;
#13580=ORIENTED_EDGE ( 'NONE', *, *, #13897, .F. ) ;
#13583=DIRECTION ( 'NONE',  ( -7.401486830834380223E-16, -1.769136588914775099E-30, 1.000000000000000000 ) ) ;
#13586=ORIENTED_EDGE ( 'NONE', *, *, #2746, .F. ) ;
#13588=DIRECTION ( 'NONE',  ( 0.000000000000000000, -2.118639217574429265E-16, -1.000000000000000000 ) ) ;
#13590=DIRECTION ( 'NONE',  ( -1.000000000000000000, 1.224646799147341128E-16, 0.000000000000000000 ) ) ;
#13594=CARTESIAN_POINT ( 'NONE',  ( -2.616666666666669805, -4.318079751576579732E-16, 4.000000000000000000 ) ) ;
#13596=DIRECTION ( 'NONE',  ( 1.000000000000000000, 0.000000000000000000, 0.000000000000000000 ) ) ;
#13599=CARTESIAN_POINT ( 'NONE',  ( -0.03000000000000000236, 11.40000000000000036, -2.869354249208270301E-17 ) ) ;
#13608=DIRECTION ( 'NONE',  ( -5.734623061080349568E-18, 0.000000000000000000, 1.000000000000000000 ) ) ;
#13611=EDGE_CURVE ( 'NONE', #10381, #17781, #892, .T. ) ;
#13616=ORIENTED_EDGE ( 'NONE', *, *, #8796, .F. ) ;
#13623=DIRECTION ( 'NONE',  ( -2.220446049250309876E-16, -1.000000000000000000, 0.000000000000000000 ) ) ;
#13627=DIRECTION ( 'NONE',  ( -4.898587196589410857E-16, -1.000000000000000000, -4.276423536147510117E-47 ) ) ;
#13634=EDGE_LOOP ( 'NONE', ( #319, #11195, #15509, #573 ) ) ;
#13635=ORIENTED_EDGE ( 'NONE', *, *, #13611, .F. ) ;
#13641=VECTOR ( 'NONE', #2856, 1000.000000000000000 ) ;
#13659=PLANE ( 'NONE',  #7298 ) ;
#13662=FACE_OUTER_BOUND ( 'NONE', #12903, .T. ) ;
#13663=CARTESIAN_POINT ( 'NONE',  ( 0.03000000000000110217, 11.40000000000000036, 1.600000000000000089 ) ) ;
#13666=CARTESIAN_POINT ( 'NONE',  ( -0.02999999999999520064, 12.00000000000000000, 7.649999999999999467 ) ) ;
#13668=EDGE_CURVE ( 'NONE', #2762, #2627, #7366, .T. ) ;
#13677=VECTOR ( 'NONE', #5988, 1000.000000000000000 ) ;
#13679=FACE_OUTER_BOUND ( 'NONE', #12110, .T. ) ;
#13684=EDGE_LOOP ( 'NONE', ( #5348, #17474, #4705, #2733 ) ) ;
#13693=CIRCLE ( 'NONE', #7191, 0.01000000000000002623 ) ;
#13703=ADVANCED_FACE ( 'NONE', ( #8923 ), #10050, .F. ) ;
#13706=CARTESIAN_POINT ( 'NONE',  ( -1.800000000000000044, 11.29999999999999893, 1.600000000000000089 ) ) ;
#13707=DIRECTION ( 'NONE',  ( 3.652293603810800245E-15, 1.332267629550185876E-15, -1.000000000000000000 ) ) ;
#13719=DIRECTION ( 'NONE',  ( -1.216682766712499758E-16, 6.416248801027068947E-32, -1.000000000000000000 ) ) ;
#13722=ORIENTED_EDGE ( 'NONE', *, *, #12076, .F. ) ;
#13728=APPLICATION_CONTEXT ( 'automotive_design' ) ;
#13730=DIRECTION ( 'NONE',  ( 1.000000000000000000, 0.000000000000000000, 0.000000000000000000 ) ) ;
#13735=EDGE_LOOP ( 'NONE', ( #9841, #5664, #977, #16077 ) ) ;
#13742=DIRECTION ( 'NONE',  ( -1.000000000000000000, 0.000000000000000000, 0.000000000000000000 ) ) ;
#13749=DIRECTION ( 'NONE',  ( -1.000000000000000000, 0.000000000000000000, 0.000000000000000000 ) ) ;
#13754=PLANE ( 'NONE',  #15983 ) ;
#13756=ORIENTED_EDGE ( 'NONE', *, *, #8581, .F. ) ;
#13771=EDGE_CURVE ( 'NONE', #14262, #2153, #3280, .T. ) ;
#13781=CYLINDRICAL_SURFACE ( 'NONE', #5504, 0.3499999999999996447 ) ;
#13791=DIRECTION ( 'NONE',  ( 0.000000000000000000, -1.000000000000000000, -6.049014748177290126E-16 ) ) ;
#13793=EDGE_CURVE ( 'NONE', #16687, #2627, #8198, .T. ) ;
#13797=AXIS2_PLACEMENT_3D ( 'NONE', #17984, #9664, #5330 ) ;
#13806=VERTEX_POINT ( 'NONE', #11697 ) ;
#13807=DIRECTION ( 'NONE',  ( -4.440892098500620245E-16, 3.700743415417219694E-16, -1.000000000000000000 ) ) ;
#13811=VECTOR ( 'NONE', #17152, 1000.000000000000000 ) ;
#13812=CARTESIAN_POINT ( 'NONE',  ( 1.890000000000029878, 4.100000000000000533, 3.000000000000000000 ) ) ;
#13815=EDGE_CURVE ( 'NONE', #17593, #14776, #2890, .T. ) ;
#13818=AXIS2_PLACEMENT_3D ( 'NONE', #17906, #13590, #9682 ) ;
#13827=VECTOR ( 'NONE', #14136, 1000.000000000000000 ) ;
#13828=ORIENTED_EDGE ( 'NONE', *, *, #13021, .T. ) ;
#13829=DIRECTION ( 'NONE',  ( -2.220446049250309876E-16, -1.000000000000000000, 1.850371707708589879E-16 ) ) ;
#13830=EDGE_CURVE ( 'NONE', #16687, #6171, #15308, .T. ) ;
#13833=CIRCLE ( 'NONE', #3179, 0.7000000000000000666 ) ;
#13835=ORIENTED_EDGE ( 'NONE', *, *, #6467, .F. ) ;
#13839=EDGE_CURVE ( 'NONE', #13271, #8528, #4083, .T. ) ;
#13843=CARTESIAN_POINT ( 'NONE',  ( -1.889999999999999902, 3.500000000000000000, 0.6099999999999999867 ) ) ;
#13846=FACE_OUTER_BOUND ( 'NONE', #12559, .T. ) ;
#13854=ORIENTED_EDGE ( 'NONE', *, *, #2963, .F. ) ;
#13855=AXIS2_PLACEMENT_3D ( 'NONE', #9170, #17570, #7603 ) ;
#13857=CARTESIAN_POINT ( 'NONE',  ( 1.850000000000000089, 11.25000000000000000, 7.649999999999999467 ) ) ;
#13859=ORIENTED_EDGE ( 'NONE', *, *, #15047, .T. ) ;
#13861=VECTOR ( 'NONE', #15366, 1000.000000000000000 ) ;
#13878=ORIENTED_EDGE ( 'NONE', *, *, #4833, .F. ) ;
#13884=EDGE_CURVE ( 'NONE', #8433, #9237, #2711, .T. ) ;
#13888=VECTOR ( 'NONE', #11918, 1000.000000000000000 ) ;
#13894=CARTESIAN_POINT ( 'NONE',  ( 2.500000000000000000, 0.8000000000000000444, -1.769429514865259726E-15 ) ) ;
#13897=EDGE_CURVE ( 'NONE', #15169, #5684, #16866, .T. ) ;
#13899=ORIENTED_EDGE ( 'NONE', *, *, #8639, .T. ) ;
#13900=VECTOR ( 'NONE', #13225, 1000.000000000000000 ) ;
#13903=ADVANCED_FACE ( 'NONE', ( #15577 ), #7067, .F. ) ;
#13906=EDGE_CURVE ( 'NONE', #12624, #11239, #17122, .T. ) ;
#13914=DIRECTION ( 'NONE',  ( 1.000000000000000000, 0.000000000000000000, -5.332141831895923026E-16 ) ) ;
#13919=EDGE_LOOP ( 'NONE', ( #9186, #12221, #9990, #10354 ) ) ;
#13923=LINE ( 'NONE', #1241, #11780 ) ;
#13957=LINE ( 'NONE', #5534, #13861 ) ;
#13964=DIRECTION ( 'NONE',  ( 1.000000000000000000, 0.000000000000000000, 0.000000000000000000 ) ) ;
#13966=ORIENTED_EDGE ( 'NONE', *, *, #14444, .T. ) ;
#13977=CARTESIAN_POINT ( 'NONE',  ( 1.850000000000000089, 11.25000000000000000, 7.700000000000000178 ) ) ;
#13980=ORIENTED_EDGE ( 'NONE', *, *, #10528, .T. ) ;
#13983=ORIENTED_EDGE ( 'NONE', *, *, #15317, .F. ) ;
#13992=CARTESIAN_POINT ( 'NONE',  ( 2.500000000000000000, 2.799999999999999822, 1.600000000000000089 ) ) ;
#14002=DIRECTION ( 'NONE',  ( 6.123233995736759873E-17, -6.123233995736769734E-17, 1.000000000000000000 ) ) ;
#14007=ORIENTED_EDGE ( 'NONE', *, *, #1890, .F. ) ;
#14009=EDGE_LOOP ( 'NONE', ( #5540, #11867, #2062, #5198 ) ) ;
#14017=PLANE ( 'NONE',  #13797 ) ;
#14018=LINE ( 'NONE', #1334, #16777 ) ;
#14023=ORIENTED_EDGE ( 'NONE', *, *, #4267, .T. ) ;
#14025=CYLINDRICAL_SURFACE ( 'NONE', #9393, 1.000000000000000000 ) ;
#14029=CARTESIAN_POINT ( 'NONE',  ( 1.899999999999999911, 8.500000000000000000, 0.6099999999999999867 ) ) ;
#14032=ORIENTED_EDGE ( 'NONE', *, *, #8711, .T. ) ;
#14035=CARTESIAN_POINT ( 'NONE',  ( 1.850000000000000089, 11.25000000000000000, 7.649999999999999467 ) ) ;
#14036=ORIENTED_EDGE ( 'NONE', *, *, #5628, .T. ) ;
#14051=DIRECTION ( 'NONE',  ( 0.000000000000000000, 0.000000000000000000, 1.000000000000000000 ) ) ;
#14055=ORIENTED_EDGE ( 'NONE', *, *, #15760, .F. ) ;
#14067=ORIENTED_EDGE ( 'NONE', *, *, #16421, .T. ) ;
#14069=ORIENTED_EDGE ( 'NONE', *, *, #7274, .F. ) ;
#14070=EDGE_LOOP ( 'NONE', ( #15592, #2023, #5768, #12738 ) ) ;
#14077=DIRECTION ( 'NONE',  ( 1.400676323190716506E-30, -1.000000000000000000, 0.000000000000000000 ) ) ;
#14086=ORIENTED_EDGE ( 'NONE', *, *, #8132, .F. ) ;
#14089=ORIENTED_EDGE ( 'NONE', *, *, #4296, .F. ) ;
#14090=VECTOR ( 'NONE', #4176, 1000.000000000000000 ) ;
#14102=AXIS2_PLACEMENT_3D ( 'NONE', #487, #406, #17319 ) ;
#14104=AXIS2_PLACEMENT_3D ( 'NONE', #11437, #5520, #8398 ) ;
#14110=PLANE ( 'NONE',  #2888 ) ;
#14114=LINE ( 'NONE', #7100, #4212 ) ;
#14116=CARTESIAN_POINT ( 'NONE',  ( -1.800000000000000044, 11.40000000000000036, 1.600000000000000089 ) ) ;
#14124=EDGE_CURVE ( 'NONE', #14130, #16733, #13328, .T. ) ;
#14126=CARTESIAN_POINT ( 'NONE',  ( 1.899999999999999911, 7.299999999999999822, 0.6099999999999999867 ) ) ;
#14127=CARTESIAN_POINT ( 'NONE',  ( -2.200000000000000178, 4.053507564265650114E-17, 7.649999999999999467 ) ) ;
#14130=VERTEX_POINT ( 'NONE', #12317 ) ;
#14131=CIRCLE ( 'NONE', #2906, 0.3500000000000001998 ) ;
#14136=DIRECTION ( 'NONE',  ( 0.000000000000000000, -1.000000000000000000, 0.000000000000000000 ) ) ;
#14138=( GEOMETRIC_REPRESENTATION_CONTEXT ( 3 ) GLOBAL_UNCERTAINTY_ASSIGNED_CONTEXT ( ( #12332 ) ) GLOBAL_UNIT_ASSIGNED_CONTEXT ( ( #9621, #8243, #1202 ) ) REPRESENTATION_CONTEXT ( 'NONE', 'WORKASPACE' ) );
#14140=AXIS2_PLACEMENT_3D ( 'NONE', #12678, #11285, #14422 ) ;
#14144=AXIS2_PLACEMENT_3D ( 'NONE', #574, #6035, #4728 ) ;
#14149=DIRECTION ( 'NONE',  ( 0.2800000000000002487, -6.217248937900882148E-17, -0.9599999999999998535 ) ) ;
#14153=CARTESIAN_POINT ( 'NONE',  ( 0.5372984490435490645, 4.599999999999999645, 8.300000000000000711 ) ) ;
#14158=CIRCLE ( 'NONE', #14102, 0.5999999999999998668 ) ;
#14169=AXIS2_PLACEMENT_3D ( 'NONE', #13594, #6344, #4866 ) ;
#14174=LINE ( 'NONE', #14437, #3193 ) ;
#14179=DIRECTION ( 'NONE',  ( 0.000000000000000000, 0.000000000000000000, 1.000000000000000000 ) ) ;
#14181=ORIENTED_EDGE ( 'NONE', *, *, #16621, .T. ) ;
#14182=CARTESIAN_POINT ( 'NONE',  ( -1.800000000000000044, 11.40000000000000036, 7.649999999999999467 ) ) ;
#14188=CARTESIAN_POINT ( 'NONE',  ( -1.899999999999999911, 0.7211102550927970256, 4.000000000000000000 ) ) ;
#14189=DIRECTION ( 'NONE',  ( 2.537652627714639929E-16, 1.000000000000000000, -8.458842092382139670E-17 ) ) ;
#14211=ORIENTED_EDGE ( 'NONE', *, *, #11988, .T. ) ;
#14219=DIRECTION ( 'NONE',  ( -1.000000000000000000, 6.659085919832825627E-16, 0.000000000000000000 ) ) ;
#14221=ORIENTED_EDGE ( 'NONE', *, *, #15584, .F. ) ;
#14227=DIRECTION ( 'NONE',  ( -1.000000000000000000, 0.000000000000000000, 0.000000000000000000 ) ) ;
#14235=ORIENTED_EDGE ( 'NONE', *, *, #8407, .F. ) ;
#14237=CARTESIAN_POINT ( 'NONE',  ( -2.500000000000000000, 11.25000000000000000, 7.649999999999999467 ) ) ;
#14243=CARTESIAN_POINT ( 'NONE',  ( -2.616666666666669805, 1.330536610280860259E-16, 4.000000000000000000 ) ) ;
#14249=ORIENTED_EDGE ( 'NONE', *, *, #8601, .F. ) ;
#14255=FACE_OUTER_BOUND ( 'NONE', #8654, .T. ) ;
#14259=EDGE_CURVE ( 'NONE', #11828, #9567, #15914, .T. ) ;
#14262=VERTEX_POINT ( 'NONE', #7567 ) ;
#14264=ORIENTED_EDGE ( 'NONE', *, *, #5312, .T. ) ;
#14265=CARTESIAN_POINT ( 'NONE',  ( 1.000000000000002220, 9.099999999999999645, 7.700000000000000178 ) ) ;
#14270=EDGE_CURVE ( 'NONE', #9094, #7523, #11469, .T. ) ;
#14271=DIRECTION ( 'NONE',  ( 1.000000000000000000, 0.000000000000000000, 0.000000000000000000 ) ) ;
#14272=CARTESIAN_POINT ( 'NONE',  ( 1.899999999999999911, 11.15000000000000036, 1.600000000000000089 ) ) ;
#14273=DIRECTION ( 'NONE',  ( 0.000000000000000000, -1.000000000000000000, 0.000000000000000000 ) ) ;
#14275=CARTESIAN_POINT ( 'NONE',  ( 2.500000000000000000, 11.15000000000000036, 1.600000000000000089 ) ) ;
#14282=VECTOR ( 'NONE', #4393, 1000.000000000000000 ) ;
#14283=CARTESIAN_POINT ( 'NONE',  ( 1.800000000000000044, 11.29999999999999893, 1.600000000000000089 ) ) ;
#14286=ORIENTED_EDGE ( 'NONE', *, *, #18165, .F. ) ;
#14301=CARTESIAN_POINT ( 'NONE',  ( 1.600000000000000089, -1.127398508120030014E-17, 7.649999999999999467 ) ) ;
#14302=AXIS2_PLACEMENT_3D ( 'NONE', #15671, #7057, #4074 ) ;
#14305=VECTOR ( 'NONE', #9020, 1000.000000000000000 ) ;
#14310=CARTESIAN_POINT ( 'NONE',  ( 1.875000000000000000, -2.296212748401290437E-16, 7.700000000000000178 ) ) ;
#14317=CARTESIAN_POINT ( 'NONE',  ( 11.62823001646920140, -1.904792371696999770E-14, 0.5999999999999559019 ) ) ;
#14318=VERTEX_POINT ( 'NONE', #4428 ) ;
#14319=CARTESIAN_POINT ( 'NONE',  ( 1.899999999999999911, 10.00000000000000000, 1.600000000000000089 ) ) ;
#14323=LINE ( 'NONE', #14415, #1799 ) ;
#14325=VERTEX_POINT ( 'NONE', #16092 ) ;
#14333=CARTESIAN_POINT ( 'NONE',  ( -1.600000000000000089, 1.602906964449920292E-16, 7.649999999999999467 ) ) ;
#14335=EDGE_CURVE ( 'NONE', #2390, #11460, #9033, .T. ) ;
#14340=PLANE ( 'NONE',  #11232 ) ;
#14344=CARTESIAN_POINT ( 'NONE',  ( -1.899999999999999911, 2.799999999999999822, 1.600000000000000089 ) ) ;
#14346=ORIENTED_EDGE ( 'NONE', *, *, #14472, .F. ) ;
#14362=DIRECTION ( 'NONE',  ( -1.000000000000000000, 0.000000000000000000, 4.318427418585891014E-15 ) ) ;
#14368=VERTEX_POINT ( 'NONE', #14333 ) ;
#14376=DIRECTION ( 'NONE',  ( 1.000000000000000000, 1.480297366166879989E-15, -7.401486830834380223E-16 ) ) ;
#14377=AXIS2_PLACEMENT_3D ( 'NONE', #4890, #15197, #6572 ) ;
#14381=CARTESIAN_POINT ( 'NONE',  ( -2.500000000000000000, 2.799999999999999822, 0.6099999999999999867 ) ) ;
#14383=CARTESIAN_POINT ( 'NONE',  ( 1.875000000000000000, 12.00000000000000000, 8.300000000000000711 ) ) ;
#14388=EDGE_CURVE ( 'NONE', #7262, #11698, #12658, .T. ) ;
#14391=LINE ( 'NONE', #14490, #8882 ) ;
#14397=EDGE_CURVE ( 'NONE', #16040, #13368, #7662, .T. ) ;
#14398=VERTEX_POINT ( 'NONE', #9129 ) ;
#14399=CARTESIAN_POINT ( 'NONE',  ( 2.500000000000000000, 1.148961478048660025E-16, 3.600000000000000089 ) ) ;
#14402=CARTESIAN_POINT ( 'NONE',  ( 2.500000000000000000, 0.8000000000000000444, -2.399999999999999911 ) ) ;
#14403=VECTOR ( 'NONE', #1773, 1000.000000000000000 ) ;
#14406=CARTESIAN_POINT ( 'NONE',  ( -1.899999999999999911, 4.700000000000000178, 1.600000000000000089 ) ) ;
#14409=AXIS2_PLACEMENT_3D ( 'NONE', #13327, #11663, #7419 ) ;
#14410=DIRECTION ( 'NONE',  ( -4.485749594445070317E-16, 0.000000000000000000, -1.000000000000000000 ) ) ;
#14415=CARTESIAN_POINT ( 'NONE',  ( 1.875000000000000000, -2.296212748401290437E-16, 8.300000000000000711 ) ) ;
#14417=ORIENTED_EDGE ( 'NONE', *, *, #205, .F. ) ;
#14420=ORIENTED_EDGE ( 'NONE', *, *, #9373, .F. ) ;
#14421=DIRECTION ( 'NONE',  ( -0.000000000000000000, 1.000000000000000000, 0.000000000000000000 ) ) ;
#14422=DIRECTION ( 'NONE',  ( -0.9622640697945192834, -0.2721173643531198949, 0.000000000000000000 ) ) ;
#14423=VERTEX_POINT ( 'NONE', #14786 ) ;
#14424=CIRCLE ( 'NONE', #17959, 0.6100000000000000977 ) ;
#14432=VECTOR ( 'NONE', #18167, 1000.000000000000000 ) ;
#14437=CARTESIAN_POINT ( 'NONE',  ( 1.899999999999999911, 11.29999999999999893, 1.600000000000000089 ) ) ;
#14438=VECTOR ( 'NONE', #16916, 1000.000000000000000 ) ;
#14440=PLANE ( 'NONE',  #16561 ) ;
#14443=ORIENTED_EDGE ( 'NONE', *, *, #1576, .F. ) ;
#14444=EDGE_CURVE ( 'NONE', #9205, #1235, #2296, .T. ) ;
#14445=CARTESIAN_POINT ( 'NONE',  ( -1.875000000000000000, 0.7500000000000000000, 8.300000000000000711 ) ) ;
#14449=CARTESIAN_POINT ( 'NONE',  ( -1.875000000000000000, 12.00000000000000000, 7.700000000000000178 ) ) ;
#14451=DIRECTION ( 'NONE',  ( -1.000000000000000000, 0.000000000000000000, 0.000000000000000000 ) ) ;
#14461=CARTESIAN_POINT ( 'NONE',  ( -2.616666666666669805, -2.774341069716839796E-16, 7.649999999999999467 ) ) ;
#14464=VERTEX_POINT ( 'NONE', #997 ) ;
#14470=AXIS2_PLACEMENT_3D ( 'NONE', #12113, #5252, #9219 ) ;
#14472=EDGE_CURVE ( 'NONE', #14776, #17593, #16743, .T. ) ;
#14473=PLANE ( 'NONE',  #10899 ) ;
#14478=ORIENTED_EDGE ( 'NONE', *, *, #15257, .T. ) ;
#14479=DIRECTION ( 'NONE',  ( 3.652293603810800245E-15, 1.332267629550190018E-15, -1.000000000000000000 ) ) ;
#14485=DIRECTION ( 'NONE',  ( -6.344131569286609929E-16, -1.000000000000000000, 1.586032892321649771E-16 ) ) ;
#14486=ORIENTED_EDGE ( 'NONE', *, *, #2827, .F. ) ;
#14490=CARTESIAN_POINT ( 'NONE',  ( -1.399999999999999911, 6.400000000000000355, 7.700000000000000178 ) ) ;
#14494=VECTOR ( 'NONE', #161, 1000.000000000000000 ) ;
#14498=LINE ( 'NONE', #13110, #15322 ) ;
#14501=LINE ( 'NONE', #11816, #10615 ) ;
#14504=EDGE_CURVE ( 'NONE', #6533, #10817, #10806, .T. ) ;
#14505=CARTESIAN_POINT ( 'NONE',  ( -1.800000000000000044, 11.40000000000000036, 7.649999999999999467 ) ) ;
#14508=CARTESIAN_POINT ( 'NONE',  ( -1.875000000000000000, 12.00000000000000000, 8.300000000000000711 ) ) ;
#14509=PLANE ( 'NONE',  #7411 ) ;
#14512=EDGE_LOOP ( 'NONE', ( #14924, #17490, #11331, #3264 ) ) ;
#14513=FACE_OUTER_BOUND ( 'NONE', #16551, .T. ) ;
#14514=DIRECTION ( 'NONE',  ( 0.000000000000000000, -1.000000000000000000, 0.000000000000000000 ) ) ;
#14516=VECTOR ( 'NONE', #2091, 1000.000000000000000 ) ;
#14525=LINE ( 'NONE', #4784, #10873 ) ;
#14527=FACE_OUTER_BOUND ( 'NONE', #5336, .T. ) ;
#14529=PLANE ( 'NONE',  #5445 ) ;
#14532=LINE ( 'NONE', #10532, #16518 ) ;
#14534=ORIENTED_EDGE ( 'NONE', *, *, #9998, .F. ) ;
#14538=DIRECTION ( 'NONE',  ( 6.437450399132682577E-16, 1.000000000000000000, 0.000000000000000000 ) ) ;
#14545=CARTESIAN_POINT ( 'NONE',  ( 1.899999999999999911, 2.481229107598859903E-16, -2.399999999999999911 ) ) ;
#14551=VERTEX_POINT ( 'NONE', #3668 ) ;
#14563=FACE_OUTER_BOUND ( 'NONE', #14769, .T. ) ;
#14564=EDGE_CURVE ( 'NONE', #3610, #5685, #808, .T. ) ;
#14566=EDGE_CURVE ( 'NONE', #18124, #5409, #17735, .T. ) ;
#14571=CARTESIAN_POINT ( 'NONE',  ( 2.500000000000000000, 8.500000000000000000, 0.6099999999999999867 ) ) ;
#14581=DIRECTION ( 'NONE',  ( 5.421010862427519212E-16, 1.000000000000000000, 0.000000000000000000 ) ) ;
#14582=CARTESIAN_POINT ( 'NONE',  ( 0.3367924244280819934, 2.254758922476410188, 7.700000000000000178 ) ) ;
#14584=VECTOR ( 'NONE', #519, 1000.000000000000000 ) ;
#14586=DIRECTION ( 'NONE',  ( 1.000000000000000000, -1.480297366166869931E-15, 0.000000000000000000 ) ) ;
#14593=VERTEX_POINT ( 'NONE', #9601 ) ;
#14595=DIRECTION ( 'NONE',  ( 3.700743415417190112E-16, 1.000000000000000000, 1.268826313857319964E-16 ) ) ;
#14611=PLANE ( 'NONE',  #3532 ) ;
#14612=ORIENTED_EDGE ( 'NONE', *, *, #6072, .F. ) ;
#14634=VERTEX_POINT ( 'NONE', #15175 ) ;
#14636=VECTOR ( 'NONE', #11813, 1000.000000000000114 ) ;
#14640=DIRECTION ( 'NONE',  ( 2.220446049250309876E-16, 1.000000000000000000, -2.385026923874314915E-32 ) ) ;
#14648=ORIENTED_EDGE ( 'NONE', *, *, #14564, .F. ) ;
#14654=FACE_OUTER_BOUND ( 'NONE', #15144, .T. ) ;
#14655=EDGE_CURVE ( 'NONE', #8501, #16536, #4035, .T. ) ;
#14657=ORIENTED_EDGE ( 'NONE', *, *, #6663, .T. ) ;
#14659=LINE ( 'NONE', #600, #4908 ) ;
#14668=ORIENTED_EDGE ( 'NONE', *, *, #8922, .F. ) ;
#14670=LINE ( 'NONE', #1989, #6302 ) ;
#14674=ORIENTED_EDGE ( 'NONE', *, *, #1088, .F. ) ;
#14678=ADVANCED_FACE ( 'NONE', ( #12388 ), #5527, .F. ) ;
#14684=VECTOR ( 'NONE', #10161, 1000.000000000000000 ) ;
#14685=VECTOR ( 'NONE', #14968, 1000.000000000000000 ) ;
#14689=VECTOR ( 'NONE', #3426, 1000.000000000000000 ) ;
#14694=AXIS2_PLACEMENT_3D ( 'NONE', #10069, #15722, #4410 ) ;
#14696=LINE ( 'NONE', #3492, #2781 ) ;
#14699=ORIENTED_EDGE ( 'NONE', *, *, #12223, .F. ) ;
#14705=VECTOR ( 'NONE', #9555, 1000.000000000000000 ) ;
#14707=ORIENTED_EDGE ( 'NONE', *, *, #3751, .F. ) ;
#14711=DIRECTION ( 'NONE',  ( 3.172065784643310388E-16, 1.000000000000000000, -1.586032892321649771E-16 ) ) ;
#14717=AXIS2_PLACEMENT_3D ( 'NONE', #4505, #8418, #5812 ) ;
#14720=AXIS2_PLACEMENT_3D ( 'NONE', #3407, #11492, #15844 ) ;
#14730=VERTEX_POINT ( 'NONE', #16722 ) ;
#14735=VECTOR ( 'NONE', #12404, 1000.000000000000000 ) ;
#14755=ORIENTED_EDGE ( 'NONE', *, *, #14655, .T. ) ;
#14756=EDGE_CURVE ( 'NONE', #13339, #18164, #5626, .T. ) ;
#14759=CARTESIAN_POINT ( 'NONE',  ( 1.899999999999999911, 0.4000000000000000222, -2.399999999999999911 ) ) ;
#14760=PLANE ( 'NONE',  #17007 ) ;
#14763=DIRECTION ( 'NONE',  ( -4.379659758543260954E-15, 1.000000000000000000, 0.000000000000000000 ) ) ;
#14765=ORIENTED_EDGE ( 'NONE', *, *, #11938, .F. ) ;
#14766=DIRECTION ( 'NONE',  ( 2.986159789035700404E-15, -1.110223024625159992E-16, -1.000000000000000000 ) ) ;
#14769=EDGE_LOOP ( 'NONE', ( #13878, #10680, #5451, #5751 ) ) ;
#14771=DIRECTION ( 'NONE',  ( 2.035408878479449976E-15, -1.000000000000000000, -9.251858538542959255E-17 ) ) ;
#14772=CARTESIAN_POINT ( 'NONE',  ( 2.500000000000000000, 0.8000000000000000444, -2.399999999999999911 ) ) ;
#14775=VERTEX_POINT ( 'NONE', #9880 ) ;
#14776=VERTEX_POINT ( 'NONE', #2840 ) ;
#14777=CARTESIAN_POINT ( 'NONE',  ( 2.500000000000000000, 4.700000000000000178, 1.600000000000000089 ) ) ;
#14778=LINE ( 'NONE', #7941, #9999 ) ;
#14779=CARTESIAN_POINT ( 'NONE',  ( -2.500000000000000000, 11.29999999999999893, 1.600000000000000089 ) ) ;
#14782=FACE_OUTER_BOUND ( 'NONE', #9967, .T. ) ;
#14784=ADVANCED_FACE ( 'NONE', ( #69 ), #5715, .F. ) ;
#14785=DIRECTION ( 'NONE',  ( 0.000000000000000000, -1.000000000000000000, -5.224578939412490694E-16 ) ) ;
#14786=CARTESIAN_POINT ( 'NONE',  ( 0.3367924244280819934, 2.254758922476410188, 7.700000000000000178 ) ) ;
#14791=CARTESIAN_POINT ( 'NONE',  ( 1.875000000000000000, 11.25000000000000000, 7.700000000000000178 ) ) ;
#14796=ADVANCED_FACE ( 'NONE', ( #1730 ), #8933, .T. ) ;
#14797=CYLINDRICAL_SURFACE ( 'NONE', #18263, 0.3999999999999999667 ) ;
#14800=CARTESIAN_POINT ( 'NONE',  ( -1.850000000000000089, 0.7500000000000000000, 8.300000000000000711 ) ) ;
#14807=VERTEX_POINT ( 'NONE', #4408 ) ;
#14809=CIRCLE ( 'NONE', #11270, 0.5999999999999998668 ) ;
#14816=DIRECTION ( 'NONE',  ( -1.000000000000000000, 0.000000000000000000, 0.000000000000000000 ) ) ;
#14824=LINE ( 'NONE', #2137, #2658 ) ;
#14827=LINE ( 'NONE', #2140, #13166 ) ;
#14832=VERTEX_POINT ( 'NONE', #11535 ) ;
#14837=CARTESIAN_POINT ( 'NONE',  ( 2.500000000000000000, 9.199999999999999289, 1.600000000000000089 ) ) ;
#14839=VERTEX_POINT ( 'NONE', #17079 ) ;
#14845=VERTEX_POINT ( 'NONE', #14402 ) ;
#14856=CIRCLE ( 'NONE', #667, 0.01000000000000002623 ) ;
#14858=EDGE_CURVE ( 'NONE', #14730, #13146, #15797, .T. ) ;
#14859=LINE ( 'NONE', #8018, #10226 ) ;
#14860=CARTESIAN_POINT ( 'NONE',  ( -2.616666666666669805, -4.318079751576579732E-16, 4.000000000000000000 ) ) ;
#14862=FACE_BOUND ( 'NONE', #1700, .T. ) ;
#14865=ORIENTED_EDGE ( 'NONE', *, *, #18093, .T. ) ;
#14869=CIRCLE ( 'NONE', #4223, 0.5999999999999998668 ) ;
#14873=CARTESIAN_POINT ( 'NONE',  ( -1.875000000000000000, 0.7500000000000000000, 7.700000000000000178 ) ) ;
#14885=PLANE ( 'NONE',  #9691 ) ;
#14906=EDGE_CURVE ( 'NONE', #12720, #13022, #14498, .T. ) ;
#14907=ORIENTED_EDGE ( 'NONE', *, *, #14270, .F. ) ;
#14908=EDGE_CURVE ( 'NONE', #6669, #16962, #17640, .T. ) ;
#14909=EDGE_LOOP ( 'NONE', ( #16041, #944, #12145, #16810 ) ) ;
#14912=DIRECTION ( 'NONE',  ( 0.000000000000000000, 0.000000000000000000, -1.000000000000000000 ) ) ;
#14916=DIRECTION ( 'NONE',  ( -0.7049180327868858065, 1.565232460946939801E-16, -0.7092887755011121342 ) ) ;
#14921=CARTESIAN_POINT ( 'NONE',  ( -0.5372984490435469551, 4.599999999999999645, 7.700000000000000178 ) ) ;
#14924=ORIENTED_EDGE ( 'NONE', *, *, #17391, .F. ) ;
#14925=EDGE_LOOP ( 'NONE', ( #5743, #3138, #15691, #3982 ) ) ;
#14926=CARTESIAN_POINT ( 'NONE',  ( 0.5291502622129179434, -1.642400929185890127E-16, 7.700000000000000178 ) ) ;
#14943=CARTESIAN_POINT ( 'NONE',  ( -0.7999999999998790301, 11.40000000000000036, -9.797174393178840942E-17 ) ) ;
#14944=EDGE_CURVE ( 'NONE', #9567, #16962, #5892, .T. ) ;
#14950=DIRECTION ( 'NONE',  ( 2.775557561562890365E-16, 1.000000000000000000, -2.775557561562890365E-16 ) ) ;
#14953=CARTESIAN_POINT ( 'NONE',  ( -1.850000000000000089, 0.7500000000000000000, 7.700000000000000178 ) ) ;
#14957=PLANE ( 'NONE',  #6122 ) ;
#14964=AXIS2_PLACEMENT_3D ( 'NONE', #113, #18131, #4357 ) ;
#14967=VERTEX_POINT ( 'NONE', #11707 ) ;
#14968=DIRECTION ( 'NONE',  ( 6.344131569286609929E-16, 1.000000000000000000, 1.586032892321649771E-16 ) ) ;
#14969=CARTESIAN_POINT ( 'NONE',  ( 1.850000000000000089, 0.7500000000000000000, 7.649999999999999467 ) ) ;
#14972=VERTEX_POINT ( 'NONE', #4671 ) ;
#14973=ADVANCED_FACE ( 'NONE', ( #17517 ), #2263, .T. ) ;
#14974=ORIENTED_EDGE ( 'NONE', *, *, #4647, .T. ) ;
#14975=DIRECTION ( 'NONE',  ( 0.000000000000000000, 1.000000000000000000, -1.850371707708589879E-16 ) ) ;
#14976=FACE_OUTER_BOUND ( 'NONE', #12233, .T. ) ;
#14982=CARTESIAN_POINT ( 'NONE',  ( -0.7999999999998730349, 12.00000000000000000, -9.797174393178840942E-17 ) ) ;
#14983=AXIS2_PLACEMENT_3D ( 'NONE', #2507, #8154, #18035 ) ;
#14984=VECTOR ( 'NONE', #8382, 1000.000000000000000 ) ;
#14985=FACE_OUTER_BOUND ( 'NONE', #13140, .T. ) ;
#14991=ORIENTED_EDGE ( 'NONE', *, *, #12425, .T. ) ;
#14994=DIRECTION ( 'NONE',  ( -1.850371707708589879E-16, -1.000000000000000000, -1.268826313857319964E-16 ) ) ;
#14997=ORIENTED_EDGE ( 'NONE', *, *, #1806, .T. ) ;
#15008=CARTESIAN_POINT ( 'NONE',  ( 2.500000000000000000, 10.00000000000000000, -1.206091987257470116E-15 ) ) ;
#15014=EDGE_CURVE ( 'NONE', #18253, #14972, #14659, .T. ) ;
#15019=AXIS2_PLACEMENT_3D ( 'NONE', #14461, #15685, #4623 ) ;
#15022=ORIENTED_EDGE ( 'NONE', *, *, #5312, .F. ) ;
#15023=VERTEX_POINT ( 'NONE', #10781 ) ;
#15024=DIRECTION ( 'NONE',  ( -1.643460219210440021E-31, -1.000000000000000000, -2.220446049250309876E-16 ) ) ;
#15032=VECTOR ( 'NONE', #7273, 1000.000000000000000 ) ;
#15033=VERTEX_POINT ( 'NONE', #5035 ) ;
#15036=EDGE_CURVE ( 'NONE', #4096, #4195, #16149, .T. ) ;
#15037=DIRECTION ( 'NONE',  ( -1.000000000000000000, 0.000000000000000000, 8.326672684688679970E-16 ) ) ;
#15039=PRODUCT_DEFINITION ( 'UNKNOWN', '', #7103, #15123 ) ;
#15044=VERTEX_POINT ( 'NONE', #14953 ) ;
#15045=AXIS2_PLACEMENT_3D ( 'NONE', #8116, #9504, #16346 ) ;
#15046=EDGE_CURVE ( 'NONE', #9755, #10260, #7888, .T. ) ;
#15047=EDGE_CURVE ( 'NONE', #10006, #4096, #14859, .T. ) ;
#15050=VECTOR ( 'NONE', #3870, 1000.000000000000000 ) ;
#15051=AXIS2_PLACEMENT_3D ( 'NONE', #14182, #10174, #9914 ) ;
#15052=DIRECTION ( 'NONE',  ( 0.000000000000000000, -1.000000000000000000, 0.000000000000000000 ) ) ;
#15056=ORIENTED_EDGE ( 'NONE', *, *, #9930, .T. ) ;
#15061=DIRECTION ( 'NONE',  ( -1.000000000000000000, 2.220446049250309876E-16, 6.049014748177260544E-16 ) ) ;
#15063=VECTOR ( 'NONE', #10225, 1000.000000000000000 ) ;
#15066=CARTESIAN_POINT ( 'NONE',  ( -1.850000000000000089, 11.25000000000000000, 7.649999999999999467 ) ) ;
#15069=FACE_OUTER_BOUND ( 'NONE', #4994, .T. ) ;
#15078=ORIENTED_EDGE ( 'NONE', *, *, #4710, .T. ) ;
#15082=AXIS2_PLACEMENT_3D ( 'NONE', #7428, #470, #1942 ) ;
#15084=ORIENTED_EDGE ( 'NONE', *, *, #2225, .F. ) ;
#15088=EDGE_CURVE ( 'NONE', #8344, #14551, #11374, .T. ) ;
#15091=CARTESIAN_POINT ( 'NONE',  ( -1.899999999999999911, 9.199999999999999289, 0.6099999999999999867 ) ) ;
#15092=ADVANCED_FACE ( 'NONE', ( #2071 ), #16243, .T. ) ;
#15095=ORIENTED_EDGE ( 'NONE', *, *, #9585, .T. ) ;
#15098=DIRECTION ( 'NONE',  ( 0.000000000000000000, 0.000000000000000000, 1.000000000000000000 ) ) ;
#15104=FACE_OUTER_BOUND ( 'NONE', #16600, .T. ) ;
#15117=AXIS2_PLACEMENT_3D ( 'NONE', #3215, #14421, #1834 ) ;
#15119=ORIENTED_EDGE ( 'NONE', *, *, #10853, .F. ) ;
#15123=PRODUCT_DEFINITION_CONTEXT ( 'detailed design', #15980, 'design' ) ;
#15124=ORIENTED_EDGE ( 'NONE', *, *, #18149, .T. ) ;
#15128=CYLINDRICAL_SURFACE ( 'NONE', #11139, 0.6000000000000000888 ) ;
#15144=EDGE_LOOP ( 'NONE', ( #929, #14069, #4109, #10070 ) ) ;
#15148=ADVANCED_FACE ( 'NONE', ( #4937 ), #13659, .F. ) ;
#15150=LINE ( 'NONE', #12542, #8525 ) ;
#15152=PLANE ( 'NONE',  #4653 ) ;
#15160=CARTESIAN_POINT ( 'NONE',  ( 2.500000000000000000, 2.000000000000000000, -1.695950706916410117E-15 ) ) ;
#15162=EDGE_LOOP ( 'NONE', ( #894, #14674, #5126, #16103 ) ) ;
#15164=EDGE_CURVE ( 'NONE', #12277, #16854, #12026, .T. ) ;
#15165=DIRECTION ( 'NONE',  ( 1.000000000000000000, 0.000000000000000000, 0.000000000000000000 ) ) ;
#15168=EDGE_CURVE ( 'NONE', #6864, #14832, #16334, .T. ) ;
#15169=VERTEX_POINT ( 'NONE', #971 ) ;
#15175=CARTESIAN_POINT ( 'NONE',  ( 1.983927814618709873E-15, 10.80000000000000071, 7.500000000000000000 ) ) ;
#15177=DIRECTION ( 'NONE',  ( 1.387778780781449866E-16, 1.110223024625160090E-15, 1.000000000000000000 ) ) ;
#15181=CARTESIAN_POINT ( 'NONE',  ( -1.850000000000000089, 0.7500000000000000000, 7.649999999999999467 ) ) ;
#15188=PLANE ( 'NONE',  #1621 ) ;
#15195=CARTESIAN_POINT ( 'NONE',  ( -2.500000000000000000, 8.500000000000000000, 0.6099999999999999867 ) ) ;
#15197=DIRECTION ( 'NONE',  ( -1.000000000000000000, 2.220446049250309876E-16, 6.123233995736769734E-17 ) ) ;
#15204=ORIENTED_EDGE ( 'NONE', *, *, #16035, .T. ) ;
#15205=CARTESIAN_POINT ( 'NONE',  ( 1.399999999999999911, 5.799999999999999822, 7.700000000000000178 ) ) ;
#15212=PLANE ( 'NONE',  #4100 ) ;
#15214=DIRECTION ( 'NONE',  ( -1.142385477618690076E-14, 1.110223024625153952E-16, -1.000000000000000000 ) ) ;
#15217=EDGE_CURVE ( 'NONE', #18244, #6584, #15336, .T. ) ;
#15221=ORIENTED_EDGE ( 'NONE', *, *, #17323, .T. ) ;
#15234=EDGE_CURVE ( 'NONE', #8501, #12906, #4199, .T. ) ;
#15242=VERTEX_POINT ( 'NONE', #9490 ) ;
#15244=DIRECTION ( 'NONE',  ( 0.000000000000000000, 0.000000000000000000, 1.000000000000000000 ) ) ;
#15257=EDGE_CURVE ( 'NONE', #3526, #17345, #16450, .T. ) ;
#15260=CARTESIAN_POINT ( 'NONE',  ( -1.000000000000000000, 6.799999999999999822, 7.700000000000000178 ) ) ;
#15262=LINE ( 'NONE', #8222, #4688 ) ;
#15263=EDGE_LOOP ( 'NONE', ( #7409, #10707, #889 ) ) ;
#15265=EDGE_CURVE ( 'NONE', #10426, #6674, #6806, .T. ) ;
#15268=ADVANCED_FACE ( 'NONE', ( #18152 ), #14017, .F. ) ;
#15275=DIRECTION ( 'NONE',  ( 1.000000000000000000, 0.000000000000000000, -7.401486830834380223E-16 ) ) ;
#15277=CARTESIAN_POINT ( 'NONE',  ( 1.899999999999999911, 11.29999999999999893, 7.649999999999999467 ) ) ;
#15283=LINE ( 'NONE', #15660, #15748 ) ;
#15286=LINE ( 'NONE', #2600, #7565 ) ;
#15287=VECTOR ( 'NONE', #16623, 1000.000000000000000 ) ;
#15291=AXIS2_PLACEMENT_3D ( 'NONE', #883, #4755, #13282 ) ;
#15292=CARTESIAN_POINT ( 'NONE',  ( -1.899999999999999911, -5.909399420205969064E-16, 4.000000000000000000 ) ) ;
#15297=ORIENTED_EDGE ( 'NONE', *, *, #11207, .T. ) ;
#15298=ORIENTED_EDGE ( 'NONE', *, *, #8512, .F. ) ;
#15299=AXIS2_PLACEMENT_3D ( 'NONE', #15354, #16907, #2938 ) ;
#15302=CARTESIAN_POINT ( 'NONE',  ( -0.8740908734716290596, 4.154758922476410099, 7.700000000000000178 ) ) ;
#15306=CARTESIAN_POINT ( 'NONE',  ( -1.289999999999999813, 4.099999999999998757, 1.106527474781921491E-15 ) ) ;
#15308=LINE ( 'NONE', #5577, #13223 ) ;
#15309=CARTESIAN_POINT ( 'NONE',  ( -1.850000000000000089, 11.25000000000000000, 8.300000000000000711 ) ) ;
#15311=VECTOR ( 'NONE', #17281, 1000.000000000000000 ) ;
#15312=DIRECTION ( 'NONE',  ( 0.000000000000000000, 1.000000000000000000, 2.775557561562890365E-16 ) ) ;
#15317=EDGE_CURVE ( 'NONE', #7434, #9192, #5416, .T. ) ;
#15322=VECTOR ( 'NONE', #17169, 1000.000000000000000 ) ;
#15323=LINE ( 'NONE', #16692, #2444 ) ;
#15324=VERTEX_POINT ( 'NONE', #4011 ) ;
#15327=SHAPE_REPRESENTATION_RELATIONSHIP ( 'NONE' , 'NONE' ,  #8322, #4434 ) ;
#15334=ORIENTED_EDGE ( 'NONE', *, *, #1042, .F. ) ;
#15336=LINE ( 'NONE', #17885, #1679 ) ;
#15342=DIRECTION ( 'NONE',  ( -1.000000000000000000, 7.401486830834380223E-16, 0.000000000000000000 ) ) ;
#15354=CARTESIAN_POINT ( 'NONE',  ( -1.875000000000000000, 12.00000000000000000, 7.700000000000000178 ) ) ;
#15366=DIRECTION ( 'NONE',  ( 1.000000000000000000, 0.000000000000000000, 0.000000000000000000 ) ) ;
#15373=ORIENTED_EDGE ( 'NONE', *, *, #556, .F. ) ;
#15374=LINE ( 'NONE', #1564, #13641 ) ;
#15376=CARTESIAN_POINT ( 'NONE',  ( -1.889999999999999902, 7.900000000000000355, 0.5999999999999999778 ) ) ;
#15382=PRESENTATION_STYLE_ASSIGNMENT (( #1481 ) ) ;
#15387=ADVANCED_FACE ( 'NONE', ( #405 ), #4469, .F. ) ;
#15390=CARTESIAN_POINT ( 'NONE',  ( -1.899999999999999911, -2.607830583485250056E-17, -4.440892098500630106E-16 ) ) ;
#15392=DIRECTION ( 'NONE',  ( -6.123233995736774664E-17, 0.000000000000000000, -1.000000000000000000 ) ) ;
#15394=DIRECTION ( 'NONE',  ( 0.000000000000000000, 0.000000000000000000, 1.000000000000000000 ) ) ;
#15395=ORIENTED_EDGE ( 'NONE', *, *, #11175, .T. ) ;
#15398=CIRCLE ( 'NONE', #15972, 0.4166666666666669072 ) ;
#15400=CARTESIAN_POINT ( 'NONE',  ( -1.875000000000000000, 0.7500000000000000000, 7.700000000000000178 ) ) ;
#15405=ADVANCED_FACE ( 'NONE', ( #321 ), #11425, .T. ) ;
#15406=DIRECTION ( 'NONE',  ( -1.000000000000000000, 0.000000000000000000, 0.000000000000000000 ) ) ;
#15408=DIRECTION ( 'NONE',  ( 1.000000000000000000, 9.697257589008697037E-16, 0.000000000000000000 ) ) ;
#15409=CARTESIAN_POINT ( 'NONE',  ( -2.500000000000000000, 7.299999999999999822, 0.6099999999999999867 ) ) ;
#15411=VECTOR ( 'NONE', #11609, 1000.000000000000000 ) ;
#15426=EDGE_CURVE ( 'NONE', #6584, #17750, #1952, .T. ) ;
#15427=ORIENTED_EDGE ( 'NONE', *, *, #8297, .T. ) ;
#15435=LINE ( 'NONE', #8386, #8212 ) ;
#15437=CARTESIAN_POINT ( 'NONE',  ( -1.289999999999999813, 4.099999999999998757, 0.6000000000000017542 ) ) ;
#15438=CARTESIAN_POINT ( 'NONE',  ( -1.899999999999999911, 2.799999999999999822, 1.600000000000000089 ) ) ;
#15445=DIRECTION ( 'NONE',  ( -3.700743415417190112E-16, -1.000000000000000000, -9.251858538542959255E-17 ) ) ;
#15448=EDGE_LOOP ( 'NONE', ( #3295, #1131, #6305, #10403 ) ) ;
#15453=FACE_OUTER_BOUND ( 'NONE', #1099, .T. ) ;
#15455=LINE ( 'NONE', #2763, #14438 ) ;
#15465=EDGE_LOOP ( 'NONE', ( #17902, #3655, #7475, #18084 ) ) ;
#15470=LINE ( 'NONE', #3972, #11556 ) ;
#15473=CARTESIAN_POINT ( 'NONE',  ( -1.875000000000000000, 0.7500000000000000000, 7.700000000000000178 ) ) ;
#15475=ORIENTED_EDGE ( 'NONE', *, *, #9718, .F. ) ;
#15485=ORIENTED_EDGE ( 'NONE', *, *, #16197, .F. ) ;
#15486=DIRECTION ( 'NONE',  ( -1.000000000000000000, 0.000000000000000000, 4.440892098500620245E-16 ) ) ;
#15509=ORIENTED_EDGE ( 'NONE', *, *, #17305, .F. ) ;
#15516=ORIENTED_EDGE ( 'NONE', *, *, #16592, .T. ) ;
#15529=DIRECTION ( 'NONE',  ( 0.000000000000000000, 0.000000000000000000, 1.000000000000000000 ) ) ;
#15530=CARTESIAN_POINT ( 'NONE',  ( -1.889999999999999902, 4.100000000000000533, 3.000000000000000000 ) ) ;
#15535=FACE_OUTER_BOUND ( 'NONE', #3020, .T. ) ;
#15537=DIRECTION ( 'NONE',  ( 1.387778780781449866E-16, 0.000000000000000000, 1.000000000000000000 ) ) ;
#15539=ADVANCED_FACE ( 'NONE', ( #13170 ), #17845, .T. ) ;
#15562=DIRECTION ( 'NONE',  ( 0.000000000000000000, 0.000000000000000000, 1.000000000000000000 ) ) ;
#15571=LINE ( 'NONE', #7318, #4921 ) ;
#15576=DIRECTION ( 'NONE',  ( -0.2800000000000001377, 0.9599999999999999645, 0.000000000000000000 ) ) ;
#15577=FACE_OUTER_BOUND ( 'NONE', #3462, .T. ) ;
#15584=EDGE_CURVE ( 'NONE', #1696, #9534, #10388, .T. ) ;
#15592=ORIENTED_EDGE ( 'NONE', *, *, #7921, .F. ) ;
#15593=CIRCLE ( 'NONE', #5792, 0.2000000000000000111 ) ;
#15594=CIRCLE ( 'NONE', #16467, 0.6099999999999999867 ) ;
#15595=EDGE_LOOP ( 'NONE', ( #2190, #7651, #8352, #10175 ) ) ;
#15596=VECTOR ( 'NONE', #10430, 1000.000000000000000 ) ;
#15606=VECTOR ( 'NONE', #15537, 1000.000000000000000 ) ;
#15607=EDGE_LOOP ( 'NONE', ( #15022, #12673, #2144, #1790 ) ) ;
#15618=DIRECTION ( 'NONE',  ( 1.216682766712499758E-16, 4.229421046191059358E-17, 1.000000000000000000 ) ) ;
#15619=AXIS2_PLACEMENT_3D ( 'NONE', #3314, #4694, #1917 ) ;
#15620=DIRECTION ( 'NONE',  ( 0.000000000000000000, 0.000000000000000000, -1.000000000000000000 ) ) ;
#15622=VECTOR ( 'NONE', #12518, 1000.000000000000000 ) ;
#15630=PLANE ( 'NONE',  #15299 ) ;
#15631=ORIENTED_EDGE ( 'NONE', *, *, #7303, .F. ) ;
#15641=CARTESIAN_POINT ( 'NONE',  ( 2.500000000000000000, 2.799999999999999822, 0.6099999999999999867 ) ) ;
#15642=EDGE_LOOP ( 'NONE', ( #18104, #6401, #11848, #11040 ) ) ;
#15648=CARTESIAN_POINT ( 'NONE',  ( 1.875000000000000000, 11.25000000000000000, 8.300000000000000711 ) ) ;
#15653=VECTOR ( 'NONE', #9553, 1000.000000000000000 ) ;
#15657=ADVANCED_FACE ( 'NONE', ( #6661 ), #7524, .F. ) ;
#15660=CARTESIAN_POINT ( 'NONE',  ( 1.899999999999999911, 7.299999999999999822, 1.600000000000000089 ) ) ;
#15671=CARTESIAN_POINT ( 'NONE',  ( 1.800000000000000044, 11.29999999999999893, 1.600000000000000089 ) ) ;
#15672=PLANE ( 'NONE',  #1022 ) ;
#15675=ORIENTED_EDGE ( 'NONE', *, *, #13668, .F. ) ;
#15677=CYLINDRICAL_SURFACE ( 'NONE', #10548, 0.6100000000000000977 ) ;
#15685=DIRECTION ( 'NONE',  ( -6.123233995736779594E-17, -2.493473113004670213E-16, -1.000000000000000000 ) ) ;
#15691=ORIENTED_EDGE ( 'NONE', *, *, #4829, .F. ) ;
#15692=VERTEX_POINT ( 'NONE', #5651 ) ;
#15705=LINE ( 'NONE', #14383, #6279 ) ;
#15715=EDGE_CURVE ( 'NONE', #1696, #14262, #15594, .T. ) ;
#15717=DIRECTION ( 'NONE',  ( 5.421010862427519212E-16, 1.000000000000000000, 0.000000000000000000 ) ) ;
#15722=DIRECTION ( 'NONE',  ( -2.220446049250309876E-16, -1.000000000000000000, 0.000000000000000000 ) ) ;
#15723=ORIENTED_EDGE ( 'NONE', *, *, #6311, .F. ) ;
#15729=DIRECTION ( 'NONE',  ( -5.551115123125780730E-16, 0.000000000000000000, -1.000000000000000000 ) ) ;
#15731=ORIENTED_EDGE ( 'NONE', *, *, #6169, .T. ) ;
#15733=EDGE_LOOP ( 'NONE', ( #7207, #13479, #16008, #17455 ) ) ;
#15734=LINE ( 'NONE', #82, #16009 ) ;
#15744=DIRECTION ( 'NONE',  ( 6.098637220230962441E-16, 1.000000000000000000, 0.000000000000000000 ) ) ;
#15747=FACE_OUTER_BOUND ( 'NONE', #15162, .T. ) ;
#15748=VECTOR ( 'NONE', #12685, 1000.000000000000000 ) ;
#15753=PLANE ( 'NONE',  #11493 ) ;
#15754=EDGE_LOOP ( 'NONE', ( #3173, #14055 ) ) ;
#15760=EDGE_CURVE ( 'NONE', #9237, #13339, #7308, .T. ) ;
#15761=DIRECTION ( 'NONE',  ( -4.498716214366520783E-15, 1.000000000000000000, 7.401486830834380223E-16 ) ) ;
#15766=DIRECTION ( 'NONE',  ( 0.000000000000000000, 0.000000000000000000, -1.000000000000000000 ) ) ;
#15772=VERTEX_POINT ( 'NONE', #10090 ) ;
#15774=ORIENTED_EDGE ( 'NONE', *, *, #6663, .F. ) ;
#15780=VERTEX_POINT ( 'NONE', #174 ) ;
#15781=DIRECTION ( 'NONE',  ( 0.000000000000000000, 1.421904488505579605E-15, -1.000000000000000000 ) ) ;
#15786=ORIENTED_EDGE ( 'NONE', *, *, #4708, .T. ) ;
#15787=VECTOR ( 'NONE', #1585, 1000.000000000000000 ) ;
#15788=DIRECTION ( 'NONE',  ( -2.537652627714639929E-16, -1.000000000000000000, 0.000000000000000000 ) ) ;
#15797=LINE ( 'NONE', #502, #3774 ) ;
#15811=DIRECTION ( 'NONE',  ( -2.220446049250309876E-16, -1.000000000000000000, -4.930380657631319405E-32 ) ) ;
#15813=CARTESIAN_POINT ( 'NONE',  ( -0.8740908734716290596, 4.154758922476410099, 8.300000000000000711 ) ) ;
#15814=ORIENTED_EDGE ( 'NONE', *, *, #15317, .T. ) ;
#15825=ADVANCED_FACE ( 'NONE', ( #14255 ), #9, .F. ) ;
#15831=VECTOR ( 'NONE', #3549, 1000.000000000000000 ) ;
#15839=EDGE_LOOP ( 'NONE', ( #8967, #14067, #7414, #3909, #17611, #4190, #4519, #14657, #1851, #509, #2259, #16788, #9400, #2910, #6080, #12330, #2362, #8951, #4811, #5489, #11483, #17747, #11258, #6578, #13513, #15786 ) ) ;
#15841=CARTESIAN_POINT ( 'NONE',  ( -1.889999999999999902, 4.700000000000000178, 0.5999999999999999778 ) ) ;
#15844=DIRECTION ( 'NONE',  ( 0.000000000000000000, 0.000000000000000000, -1.000000000000000000 ) ) ;
#15845=EDGE_CURVE ( 'NONE', #396, #9909, #5917, .T. ) ;
#15850=DIRECTION ( 'NONE',  ( 4.440892098500620245E-16, -3.700743415417219694E-16, 1.000000000000000000 ) ) ;
#15852=ORIENTED_EDGE ( 'NONE', *, *, #1271, .F. ) ;
#15863=AXIS2_PLACEMENT_3D ( 'NONE', #15473, #17110, #18201 ) ;
#15864=ORIENTED_EDGE ( 'NONE', *, *, #17826, .F. ) ;
#15876=AXIS2_PLACEMENT_3D ( 'NONE', #11882, #3887, #13791 ) ;
#15894=ORIENTED_EDGE ( 'NONE', *, *, #17723, .F. ) ;
#15895=CIRCLE ( 'NONE', #7908, 0.5999999999999998668 ) ;
#15896=AXIS2_PLACEMENT_3D ( 'NONE', #11961, #14479, #402 ) ;
#15897=CIRCLE ( 'NONE', #15019, 0.4166666666666671848 ) ;
#15898=CARTESIAN_POINT ( 'NONE',  ( 1.850000000000000089, 0.7500000000000000000, 7.700000000000000178 ) ) ;
#15904=ORIENTED_EDGE ( 'NONE', *, *, #12230, .F. ) ;
#15908=DIRECTION ( 'NONE',  ( 4.318427418585891014E-15, -2.220446049250315053E-16, 1.000000000000000000 ) ) ;
#15914=LINE ( 'NONE', #7215, #15596 ) ;
#15922=CYLINDRICAL_SURFACE ( 'NONE', #17041, 0.6100000000000000977 ) ;
#15927=EDGE_LOOP ( 'NONE', ( #2981, #876, #4070, #11913 ) ) ;
#15928=LINE ( 'NONE', #3236, #8121 ) ;
#15931=LINE ( 'NONE', #7860, #5287 ) ;
#15938=EDGE_CURVE ( 'NONE', #16796, #13279, #17634, .T. ) ;
#15939=CARTESIAN_POINT ( 'NONE',  ( 0.5372984490435490645, 4.599999999999999645, 7.700000000000000178 ) ) ;
#15951=AXIS2_PLACEMENT_3D ( 'NONE', #8417, #15024, #9894 ) ;
#15953=CARTESIAN_POINT ( 'NONE',  ( 1.850000000000000089, 11.25000000000000000, 8.300000000000000711 ) ) ;
#15959=AXIS2_PLACEMENT_3D ( 'NONE', #10803, #13395, #3861 ) ;
#15960=ORIENTED_EDGE ( 'NONE', *, *, #4045, .T. ) ;
#15972=AXIS2_PLACEMENT_3D ( 'NONE', #14243, #18102, #14149 ) ;
#15976=DIRECTION ( 'NONE',  ( -1.000000000000000000, 0.000000000000000000, 1.142385477618690234E-14 ) ) ;
#15980=APPLICATION_CONTEXT ( 'automotive_design' ) ;
#15981=EDGE_CURVE ( 'NONE', #4246, #6244, #492, .T. ) ;
#15983=AXIS2_PLACEMENT_3D ( 'NONE', #14873, #3562, #6431 ) ;
#15985=EDGE_LOOP ( 'NONE', ( #1417, #14765, #47, #984 ) ) ;
#15990=CARTESIAN_POINT ( 'NONE',  ( -0.7999999999998790301, 11.40000000000000036, -9.797174393178840942E-17 ) ) ;
#15995=EDGE_CURVE ( 'NONE', #475, #8344, #7846, .T. ) ;
#16006=DIRECTION ( 'NONE',  ( -2.168404344971009262E-15, -1.000000000000000000, -2.220446049250220143E-16 ) ) ;
#16007=PLANE ( 'NONE',  #10249 ) ;
#16008=ORIENTED_EDGE ( 'NONE', *, *, #9405, .T. ) ;
#16009=VECTOR ( 'NONE', #12851, 1000.000000000000000 ) ;
#16010=DIRECTION ( 'NONE',  ( 2.960594732333750117E-16, 1.000000000000000000, 0.000000000000000000 ) ) ;
#16017=CYLINDRICAL_SURFACE ( 'NONE', #2752, 0.01000000000000002623 ) ;
#16020=CARTESIAN_POINT ( 'NONE',  ( -1.899999999999999911, 11.25000000000000000, 7.649999999999999467 ) ) ;
#16025=DIRECTION ( 'NONE',  ( 1.000000000000000000, 0.000000000000000000, 0.000000000000000000 ) ) ;
#16035=EDGE_CURVE ( 'NONE', #15023, #3622, #2104, .T. ) ;
#16040=VERTEX_POINT ( 'NONE', #9131 ) ;
#16041=ORIENTED_EDGE ( 'NONE', *, *, #8297, .F. ) ;
#16043=ORIENTED_EDGE ( 'NONE', *, *, #17430, .F. ) ;
#16058=ADVANCED_FACE ( 'NONE', ( #16275 ), #16557, .F. ) ;
#16077=ORIENTED_EDGE ( 'NONE', *, *, #11746, .T. ) ;
#16082=ORIENTED_EDGE ( 'NONE', *, *, #3579, .T. ) ;
#16085=CARTESIAN_POINT ( 'NONE',  ( -0.7999999999998720357, 12.00000000000000000, -2.399999999999999911 ) ) ;
#16092=CARTESIAN_POINT ( 'NONE',  ( -0.9999999999999978906, 9.099999999999999645, 7.700000000000000178 ) ) ;
#16095=EDGE_CURVE ( 'NONE', #9192, #16395, #7952, .T. ) ;
#16098=CARTESIAN_POINT ( 'NONE',  ( -1.000000000000000000, 5.799999999999999822, 8.300000000000000711 ) ) ;
#16099=FACE_OUTER_BOUND ( 'NONE', #13289, .T. ) ;
#16103=ORIENTED_EDGE ( 'NONE', *, *, #8760, .F. ) ;
#16110=CARTESIAN_POINT ( 'NONE',  ( -1.899999999999999911, 2.799999999999999822, 0.6099999999999999867 ) ) ;
#16129=CARTESIAN_POINT ( 'NONE',  ( -1.889999999999999902, 3.500000000000000000, -6.185550171619869534E-16 ) ) ;
#16140=ADVANCED_FACE ( 'NONE', ( #15453 ), #11363, .T. ) ;
#16141=CARTESIAN_POINT ( 'NONE',  ( -1.899999999999999911, 11.29999999999999893, 1.600000000000000089 ) ) ;
#16149=LINE ( 'NONE', #9394, #12323 ) ;
#16150=DIRECTION ( 'NONE',  ( 2.986159789035700404E-15, -1.110223024625159992E-16, -1.000000000000000000 ) ) ;
#16152=CARTESIAN_POINT ( 'NONE',  ( 0.000000000000000000, 0.000000000000000000, 7.700000000000000178 ) ) ;
#16160=DIRECTION ( 'NONE',  ( -1.480297366166879989E-15, -2.476791224480685138E-30, -1.000000000000000000 ) ) ;
#16161=LINE ( 'NONE', #349, #14584 ) ;
#16162=CIRCLE ( 'NONE', #6114, 0.5999999999999998668 ) ;
#16163=DIRECTION ( 'NONE',  ( -2.168404344971011235E-15, 1.000000000000000000, 0.000000000000000000 ) ) ;
#16168=DIRECTION ( 'NONE',  ( -1.224646799147350002E-16, -1.000000000000000000, 0.000000000000000000 ) ) ;
#16170=FACE_OUTER_BOUND ( 'NONE', #3816, .T. ) ;
#16171=EDGE_CURVE ( 'NONE', #435, #11991, #2947, .T. ) ;
#16172=EDGE_LOOP ( 'NONE', ( #7758, #16227, #4198, #8381 ) ) ;
#16184=DIRECTION ( 'NONE',  ( 1.110223024625160090E-15, 1.000000000000000000, 0.000000000000000000 ) ) ;
#16191=ORIENTED_EDGE ( 'NONE', *, *, #18093, .F. ) ;
#16197=EDGE_CURVE ( 'NONE', #9483, #1501, #12565, .T. ) ;
#16213=VECTOR ( 'NONE', #3525, 1000.000000000000000 ) ;
#16217=LINE ( 'NONE', #17494, #16213 ) ;
#16218=EDGE_LOOP ( 'NONE', ( #6863, #13159, #16997, #15894 ) ) ;
#16219=CARTESIAN_POINT ( 'NONE',  ( -1.800000000000000044, 11.40000000000000036, 1.600000000000000089 ) ) ;
#16227=ORIENTED_EDGE ( 'NONE', *, *, #1354, .F. ) ;
#16230=AXIS2_PLACEMENT_3D ( 'NONE', #4973, #5357, #5260 ) ;
#16231=EDGE_LOOP ( 'NONE', ( #12854, #6791 ) ) ;
#16243=SPHERICAL_SURFACE ( 'NONE', #15291, 1.016666666666670160 ) ;
#16244=CYLINDRICAL_SURFACE ( 'NONE', #1961, 0.4166666666666670737 ) ;
#16249=VERTEX_POINT ( 'NONE', #4134 ) ;
#16250=DIRECTION ( 'NONE',  ( 1.000000000000000000, 0.000000000000000000, 0.000000000000000000 ) ) ;
#16251=EDGE_CURVE ( 'NONE', #1501, #5435, #8587, .T. ) ;
#16258=DIRECTION ( 'NONE',  ( -3.700743415417199972E-16, 1.000000000000000000, 3.581736239852565328E-31 ) ) ;
#16259=DIRECTION ( 'NONE',  ( -0.7049180327868849183, 0.7092887755011130224, 8.531426931033447850E-16 ) ) ;
#16262=EDGE_LOOP ( 'NONE', ( #1716, #13854, #14699, #14991 ) ) ;
#16273=VECTOR ( 'NONE', #1560, 1000.000000000000000 ) ;
#16275=FACE_OUTER_BOUND ( 'NONE', #4703, .T. ) ;
#16280=CARTESIAN_POINT ( 'NONE',  ( 1.899999999999999911, 7.299999999999999822, 1.600000000000000089 ) ) ;
#16285=CARTESIAN_POINT ( 'NONE',  ( 0.03000000000000110217, 11.40000000000000036, 1.600000000000000089 ) ) ;
#16296=DIRECTION ( 'NONE',  ( 7.401486830834380223E-16, -4.695600626315540288E-31, 1.000000000000000000 ) ) ;
#16298=PLANE ( 'NONE',  #14377 ) ;
#16302=EDGE_CURVE ( 'NONE', #6821, #14368, #1384, .T. ) ;
#16305=LINE ( 'NONE', #329, #7929 ) ;
#16317=CARTESIAN_POINT ( 'NONE',  ( -1.899999999999999911, 11.25000000000000000, 7.649999999999999467 ) ) ;
#16325=ORIENTED_EDGE ( 'NONE', *, *, #11474, .T. ) ;
#16334=LINE ( 'NONE', #7816, #2255 ) ;
#16338=FACE_OUTER_BOUND ( 'NONE', #2078, .T. ) ;
#16341=DIRECTION ( 'NONE',  ( 4.440892098500620245E-16, 1.000000000000000000, 2.220446049250309876E-16 ) ) ;
#16346=DIRECTION ( 'NONE',  ( 1.000000000000000000, 0.000000000000000000, -4.265713465516738421E-15 ) ) ;
#16356=ORIENTED_EDGE ( 'NONE', *, *, #155, .T. ) ;
#16363=DIRECTION ( 'NONE',  ( -8.971499188890150495E-16, 0.000000000000000000, -1.000000000000000000 ) ) ;
#16364=EDGE_CURVE ( 'NONE', #17345, #7849, #8666, .T. ) ;
#16377=DIRECTION ( 'NONE',  ( 0.000000000000000000, 0.000000000000000000, 1.000000000000000000 ) ) ;
#16379=CARTESIAN_POINT ( 'NONE',  ( 1.889999999999999902, 7.299999999999999822, -1.002722375122780079E-16 ) ) ;
#16380=CARTESIAN_POINT ( 'NONE',  ( 1.850000000000000089, 11.25000000000000000, 8.300000000000000711 ) ) ;
#16384=ADVANCED_FACE ( 'NONE', ( #17249 ), #154, .T. ) ;
#16395=VERTEX_POINT ( 'NONE', #15990 ) ;
#16399=VECTOR ( 'NONE', #16377, 1000.000000000000000 ) ;
#16400=ORIENTED_EDGE ( 'NONE', *, *, #8590, .F. ) ;
#16411=ORIENTED_EDGE ( 'NONE', *, *, #4482, .F. ) ;
#16414=VERTEX_POINT ( 'NONE', #17083 ) ;
#16416=CARTESIAN_POINT ( 'NONE',  ( -2.500000000000000000, 7.299999999999999822, 0.6099999999999999867 ) ) ;
#16419=VECTOR ( 'NONE', #14950, 1000.000000000000000 ) ;
#16421=EDGE_CURVE ( 'NONE', #14832, #18253, #4490, .T. ) ;
#16423=CARTESIAN_POINT ( 'NONE',  ( -2.500000000000000000, 9.199999999999999289, 0.6099999999999999867 ) ) ;
#16427=DIRECTION ( 'NONE',  ( -2.220446049250309876E-16, -1.000000000000000000, 1.268826313857319964E-16 ) ) ;
#16436=DIRECTION ( 'NONE',  ( -1.000000000000000000, 0.000000000000000000, 0.000000000000000000 ) ) ;
#16445=CARTESIAN_POINT ( 'NONE',  ( 0.3367924244280819934, 2.254758922476410188, 7.700000000000000178 ) ) ;
#16450=CIRCLE ( 'NONE', #4604, 0.2000000000000000111 ) ;
#16451=DIRECTION ( 'NONE',  ( 3.652293603810800245E-15, 1.332267629550190018E-15, -1.000000000000000000 ) ) ;
#16452=DIRECTION ( 'NONE',  ( 1.000000000000000000, 4.014365738757630620E-15, 5.017957173447030386E-16 ) ) ;
#16455=DIRECTION ( 'NONE',  ( 1.000000000000000000, 0.000000000000000000, 0.000000000000000000 ) ) ;
#16464=DIRECTION ( 'NONE',  ( -1.000000000000000000, 0.000000000000000000, 7.401486830834390084E-16 ) ) ;
#16466=ORIENTED_EDGE ( 'NONE', *, *, #15164, .F. ) ;
#16467=AXIS2_PLACEMENT_3D ( 'NONE', #5555, #16931, #18199 ) ;
#16480=AXIS2_PLACEMENT_3D ( 'NONE', #3014, #10209, #15976 ) ;
#16481=DIRECTION ( 'NONE',  ( -3.700743415417195042E-15, -3.289549702593060375E-15, 1.000000000000000000 ) ) ;
#16483=CARTESIAN_POINT ( 'NONE',  ( 2.500000000000000000, 1.148961478048669885E-16, -2.399999999999999911 ) ) ;
#16484=CIRCLE ( 'NONE', #8508, 1.016666666666670160 ) ;
#16485=CIRCLE ( 'NONE', #10872, 0.6099999999999999867 ) ;
#16487=ORIENTED_EDGE ( 'NONE', *, *, #1464, .T. ) ;
#16490=VECTOR ( 'NONE', #4365, 1000.000000000000000 ) ;
#16491=CARTESIAN_POINT ( 'NONE',  ( -1.850000000000000089, 11.25000000000000000, 7.700000000000000178 ) ) ;
#16501=CARTESIAN_POINT ( 'NONE',  ( 2.500000000000000000, 11.15000000000000036, 1.600000000000000089 ) ) ;
#16503=EDGE_LOOP ( 'NONE', ( #8094, #18210, #6258, #3058 ) ) ;
#16515=EDGE_LOOP ( 'NONE', ( #7314, #1429, #14707 ) ) ;
#16518=VECTOR ( 'NONE', #3240, 1000.000000000000000 ) ;
#16526=AXIS2_PLACEMENT_3D ( 'NONE', #18190, #852, #17858 ) ;
#16527=CARTESIAN_POINT ( 'NONE',  ( -1.899999999999999911, 2.000000000000000000, 1.600000000000000089 ) ) ;
#16530=DIRECTION ( 'NONE',  ( 0.000000000000000000, -1.000000000000000000, 0.000000000000000000 ) ) ;
#16534=CARTESIAN_POINT ( 'NONE',  ( -1.899999999999999911, 10.00000000000000000, 1.600000000000000089 ) ) ;
#16536=VERTEX_POINT ( 'NONE', #4847 ) ;
#16537=CARTESIAN_POINT ( 'NONE',  ( -1.399999999999999911, 6.400000000000000355, 7.700000000000000178 ) ) ;
#16538=CARTESIAN_POINT ( 'NONE',  ( 1.800000000000000044, 11.29999999999999893, 7.649999999999999467 ) ) ;
#16547=LINE ( 'NONE', #13389, #14516 ) ;
#16549=AXIS2_PLACEMENT_3D ( 'NONE', #13526, #12045, #11022 ) ;
#16551=EDGE_LOOP ( 'NONE', ( #11801, #2046, #4324, #15373, #14032, #1288, #9767, #4726 ) ) ;
#16554=FACE_OUTER_BOUND ( 'NONE', #16218, .T. ) ;
#16557=PLANE ( 'NONE',  #2268 ) ;
#16561=AXIS2_PLACEMENT_3D ( 'NONE', #3132, #3320, #11563 ) ;
#16573=FACE_OUTER_BOUND ( 'NONE', #6422, .T. ) ;
#16576=ORIENTED_EDGE ( 'NONE', *, *, #2944, .F. ) ;
#16577=AXIS2_PLACEMENT_3D ( 'NONE', #5903, #11629, #8946 ) ;
#16583=DIRECTION ( 'NONE',  ( 1.000000000000000000, 5.782411586589356455E-15, 3.614007241618347587E-15 ) ) ;
#16588=LINE ( 'NONE', #848, #3971 ) ;
#16592=EDGE_CURVE ( 'NONE', #5474, #1639, #3641, .T. ) ;
#16599=VECTOR ( 'NONE', #2148, 1000.000000000000000 ) ;
#16600=EDGE_LOOP ( 'NONE', ( #2675, #5629, #17571, #7863 ) ) ;
#16604=EDGE_CURVE ( 'NONE', #15023, #4272, #6242, .T. ) ;
#16617=ADVANCED_FACE ( 'NONE', ( #13662 ), #14957, .F. ) ;
#16621=EDGE_CURVE ( 'NONE', #10145, #17781, #11901, .T. ) ;
#16623=DIRECTION ( 'NONE',  ( -1.000000000000000000, 1.480297366166869931E-15, 7.401486830834370362E-16 ) ) ;
#16625=ADVANCED_FACE ( 'NONE', ( #3453, #7729, #9495, #14862, #5038 ), #15152, .F. ) ;
#16633=DIRECTION ( 'NONE',  ( 3.097720492815730124E-16, 1.000000000000000000, 0.000000000000000000 ) ) ;
#16636=ORIENTED_EDGE ( 'NONE', *, *, #1673, .F. ) ;
#16665=LINE ( 'NONE', #5554, #6835 ) ;
#16669=CARTESIAN_POINT ( 'NONE',  ( 2.500000000000000000, 1.148961478048669885E-16, -2.399999999999999911 ) ) ;
#16672=LINE ( 'NONE', #6668, #10046 ) ;
#16680=DIRECTION ( 'NONE',  ( -2.114651788903909713E-47, 1.000000000000000000, -1.110223024625159992E-16 ) ) ;
#16687=VERTEX_POINT ( 'NONE', #4204 ) ;
#16692=CARTESIAN_POINT ( 'NONE',  ( 2.500000000000000000, 7.299999999999999822, 1.600000000000000089 ) ) ;
#16701=DIRECTION ( 'NONE',  ( 1.823160359065819982E-16, 0.000000000000000000, -1.000000000000000000 ) ) ;
#16706=LINE ( 'NONE', #12741, #1994 ) ;
#16716=LINE ( 'NONE', #11164, #4385 ) ;
#16718=EDGE_CURVE ( 'NONE', #16897, #3896, #6810, .T. ) ;
#16722=CARTESIAN_POINT ( 'NONE',  ( 1.899999999999999911, 9.199999999999999289, 0.6099999999999999867 ) ) ;
#16731=CARTESIAN_POINT ( 'NONE',  ( -1.899999999999999911, 10.00000000000000000, 1.600000000000000089 ) ) ;
#16733=VERTEX_POINT ( 'NONE', #6710 ) ;
#16736=CIRCLE ( 'NONE', #13485, 0.01000000000000002623 ) ;
#16737=ORIENTED_EDGE ( 'NONE', *, *, #15047, .F. ) ;
#16743=CIRCLE ( 'NONE', #11123, 0.6324555320336745501 ) ;
#16753=DIRECTION ( 'NONE',  ( 0.000000000000000000, -3.152456273542039042E-16, -1.000000000000000000 ) ) ;
#16756=EDGE_CURVE ( 'NONE', #17179, #2455, #7604, .T. ) ;
#16757=CYLINDRICAL_SURFACE ( 'NONE', #14302, 0.1000000000000000472 ) ;
#16760=AXIS2_PLACEMENT_3D ( 'NONE', #14310, #12750, #4215 ) ;
#16769=DIRECTION ( 'NONE',  ( 0.000000000000000000, 0.000000000000000000, -1.000000000000000000 ) ) ;
#16770=AXIS2_PLACEMENT_3D ( 'NONE', #1075, #6719, #18269 ) ;
#16777=VECTOR ( 'NONE', #5873, 1000.000000000000000 ) ;
#16786=ORIENTED_EDGE ( 'NONE', *, *, #9492, .F. ) ;
#16788=ORIENTED_EDGE ( 'NONE', *, *, #216, .T. ) ;
#16796=VERTEX_POINT ( 'NONE', #8473 ) ;
#16798=DIRECTION ( 'NONE',  ( -1.000000000000000000, 6.098637220230962441E-16, 0.000000000000000000 ) ) ;
#16801=FACE_OUTER_BOUND ( 'NONE', #17699, .T. ) ;
#16802=DIRECTION ( 'NONE',  ( 3.700743415417190309E-15, -6.579099405186109509E-16, 1.000000000000000000 ) ) ;
#16810=ORIENTED_EDGE ( 'NONE', *, *, #17253, .T. ) ;
#16815=ORIENTED_EDGE ( 'NONE', *, *, #13452, .T. ) ;
#16816=LINE ( 'NONE', #4130, #7895 ) ;
#16822=ADVANCED_FACE ( 'NONE', ( #16801 ), #14110, .T. ) ;
#16823=DIRECTION ( 'NONE',  ( -1.000000000000000000, 0.000000000000000000, 0.000000000000000000 ) ) ;
#16828=AXIS2_PLACEMENT_3D ( 'NONE', #2294, #12200, #17816 ) ;
#16836=DIRECTION ( 'NONE',  ( 0.000000000000000000, 0.000000000000000000, 1.000000000000000000 ) ) ;
#16843=VECTOR ( 'NONE', #11949, 1000.000000000000000 ) ;
#16844=LINE ( 'NONE', #18032, #4489 ) ;
#16850=EDGE_CURVE ( 'NONE', #7434, #4810, #15435, .T. ) ;
#16854=VERTEX_POINT ( 'NONE', #16979 ) ;
#16857=LINE ( 'NONE', #9823, #3956 ) ;
#16859=VECTOR ( 'NONE', #8595, 1000.000000000000000 ) ;
#16860=VERTEX_POINT ( 'NONE', #7266 ) ;
#16866=LINE ( 'NONE', #14272, #1101 ) ;
#16882=EDGE_LOOP ( 'NONE', ( #9547, #3537, #2813, #3564 ) ) ;
#16887=ORIENTED_EDGE ( 'NONE', *, *, #11183, .F. ) ;
#16890=ORIENTED_EDGE ( 'NONE', *, *, #7000, .F. ) ;
#16892=CARTESIAN_POINT ( 'NONE',  ( -0.03000000000000159830, 11.40000000000000036, 7.649999999999999467 ) ) ;
#16897=VERTEX_POINT ( 'NONE', #4741 ) ;
#16898=DIRECTION ( 'NONE',  ( -1.000000000000000000, 0.000000000000000000, 0.000000000000000000 ) ) ;
#16904=EDGE_LOOP ( 'NONE', ( #370, #8638, #15084 ) ) ;
#16907=DIRECTION ( 'NONE',  ( -1.000000000000000000, 2.960594732333750117E-16, 0.000000000000000000 ) ) ;
#16916=DIRECTION ( 'NONE',  ( 1.060879779086260081E-14, -8.223874256482640091E-16, 1.000000000000000000 ) ) ;
#16921=ORIENTED_EDGE ( 'NONE', *, *, #8331, .T. ) ;
#16924=CARTESIAN_POINT ( 'NONE',  ( 2.500000000000000000, 11.25000000000000000, 7.649999999999999467 ) ) ;
#16931=DIRECTION ( 'NONE',  ( -6.162975822039159109E-32, -1.000000000000000000, -1.110223024625159992E-16 ) ) ;
#16936=CARTESIAN_POINT ( 'NONE',  ( 0.5372984490435490645, 4.250000000000000000, 7.700000000000000178 ) ) ;
#16937=ORIENTED_EDGE ( 'NONE', *, *, #13815, .F. ) ;
#16939=ORIENTED_EDGE ( 'NONE', *, *, #4482, .T. ) ;
#16940=EDGE_CURVE ( 'NONE', #2455, #16733, #13002, .T. ) ;
#16946=EDGE_CURVE ( 'NONE', #16796, #2415, #3296, .T. ) ;
#16952=CARTESIAN_POINT ( 'NONE',  ( 1.875000000000000000, -2.296212748401290437E-16, 7.700000000000000178 ) ) ;
#16961=CARTESIAN_POINT ( 'NONE',  ( 11.62823001646920140, -1.891469695401499911E-14, -4.352074256530609852E-14 ) ) ;
#16962=VERTEX_POINT ( 'NONE', #512 ) ;
#16976=LINE ( 'NONE', #17060, #514 ) ;
#16977=DIRECTION ( 'NONE',  ( -1.480297366166869931E-15, -1.000000000000000000, 0.000000000000000000 ) ) ;
#16979=CARTESIAN_POINT ( 'NONE',  ( 1.289999999999999813, 4.099999999999999645, 0.6000000000000067502 ) ) ;
#16991=ORIENTED_EDGE ( 'NONE', *, *, #11183, .T. ) ;
#16997=ORIENTED_EDGE ( 'NONE', *, *, #8015, .F. ) ;
#17002=DIRECTION ( 'NONE',  ( -1.000000000000000000, 0.000000000000000000, 0.000000000000000000 ) ) ;
#17004=ORIENTED_EDGE ( 'NONE', *, *, #4833, .T. ) ;
#17007=AXIS2_PLACEMENT_3D ( 'NONE', #7636, #6416, #17599 ) ;
#17022=ORIENTED_EDGE ( 'NONE', *, *, #12648, .T. ) ;
#17025=ORIENTED_EDGE ( 'NONE', *, *, #6657, .T. ) ;
#17039=CARTESIAN_POINT ( 'NONE',  ( -2.500000000000000000, 4.700000000000000178, 0.6099999999999999867 ) ) ;
#17041=AXIS2_PLACEMENT_3D ( 'NONE', #11299, #12866, #4436 ) ;
#17043=CARTESIAN_POINT ( 'NONE',  ( 1.850000000000000089, 0.7500000000000000000, 7.700000000000000178 ) ) ;
#17047=VERTEX_POINT ( 'NONE', #6616 ) ;
#17051=AXIS2_PLACEMENT_3D ( 'NONE', #13093, #411, #6050 ) ;
#17057=ORIENTED_EDGE ( 'NONE', *, *, #11207, .F. ) ;
#17060=CARTESIAN_POINT ( 'NONE',  ( -2.500000000000000000, 11.15000000000000036, 2.137972338849589826E-15 ) ) ;
#17065=LINE ( 'NONE', #3096, #14282 ) ;
#17067=ADVANCED_FACE ( 'NONE', ( #787 ), #9106, .F. ) ;
#17071=CARTESIAN_POINT ( 'NONE',  ( -1.899999999999999911, 11.25000000000000000, 7.649999999999999467 ) ) ;
#17075=DIRECTION ( 'NONE',  ( -1.000000000000000000, 0.000000000000000000, 0.000000000000000000 ) ) ;
#17079=CARTESIAN_POINT ( 'NONE',  ( -2.500000000000000000, 8.500000000000000000, 0.6099999999999999867 ) ) ;
#17081=VECTOR ( 'NONE', #4888, 1000.000000000000000 ) ;
#17083=CARTESIAN_POINT ( 'NONE',  ( 1.899999999999999911, 11.25000000000000000, 7.649999999999999467 ) ) ;
#17084=EDGE_CURVE ( 'NONE', #14807, #17218, #3456, .T. ) ;
#17087=CARTESIAN_POINT ( 'NONE',  ( 1.899999999999999911, 0.7211102550927970256, 7.649999999999999467 ) ) ;
#17096=VECTOR ( 'NONE', #15788, 1000.000000000000000 ) ;
#17106=DIRECTION ( 'NONE',  ( 0.000000000000000000, -1.000000000000000000, 0.000000000000000000 ) ) ;
#17109=AXIS2_PLACEMENT_3D ( 'NONE', #15066, #6325, #9199 ) ;
#17110=DIRECTION ( 'NONE',  ( 0.000000000000000000, -1.000000000000000000, 0.000000000000000000 ) ) ;
#17111=CARTESIAN_POINT ( 'NONE',  ( -2.500000000000000000, 4.700000000000000178, 0.6099999999999999867 ) ) ;
#17114=PLANE ( 'NONE',  #1608 ) ;
#17116=CARTESIAN_POINT ( 'NONE',  ( 1.000000000000000000, 6.799999999999999822, 7.700000000000000178 ) ) ;
#17117=CARTESIAN_POINT ( 'NONE',  ( 1.875000000000000000, -2.296212748401290437E-16, 8.300000000000000711 ) ) ;
#17122=LINE ( 'NONE', #2617, #4636 ) ;
#17126=LINE ( 'NONE', #8712, #10262 ) ;
#17131=VECTOR ( 'NONE', #13608, 1000.000000000000000 ) ;
#17139=ORIENTED_EDGE ( 'NONE', *, *, #12418, .T. ) ;
#17142=ORIENTED_EDGE ( 'NONE', *, *, #2594, .F. ) ;
#17146=ORIENTED_EDGE ( 'NONE', *, *, #13021, .F. ) ;
#17152=DIRECTION ( 'NONE',  ( -1.000000000000000000, 1.480297366166879989E-15, 0.000000000000000000 ) ) ;
#17155=AXIS2_PLACEMENT_3D ( 'NONE', #335, #10137, #8847 ) ;
#17161=DIRECTION ( 'NONE',  ( -1.000000000000000000, 0.000000000000000000, 0.000000000000000000 ) ) ;
#17162=EDGE_CURVE ( 'NONE', #5409, #14832, #10287, .T. ) ;
#17163=ADVANCED_FACE ( 'NONE', ( #6423 ), #5138, .F. ) ;
#17164=VERTEX_POINT ( 'NONE', #5044 ) ;
#17166=EDGE_CURVE ( 'NONE', #1884, #15033, #12666, .T. ) ;
#17169=DIRECTION ( 'NONE',  ( 3.670158759091429763E-17, 0.000000000000000000, 1.000000000000000000 ) ) ;
#17179=VERTEX_POINT ( 'NONE', #9584 ) ;
#17183=EDGE_CURVE ( 'NONE', #12747, #13413, #139, .T. ) ;
#17193=CARTESIAN_POINT ( 'NONE',  ( 1.889999999999999902, 3.500000000000000000, 0.5999999999999999778 ) ) ;
#17197=DIRECTION ( 'NONE',  ( -1.000000000000000000, 0.000000000000000000, 1.142385477618690234E-14 ) ) ;
#17199=ORIENTED_EDGE ( 'NONE', *, *, #7338, .F. ) ;
#17200=AXIS2_PLACEMENT_3D ( 'NONE', #17234, #9953, #7452 ) ;
#17203=FACE_OUTER_BOUND ( 'NONE', #11995, .T. ) ;
#17207=LINE ( 'NONE', #3149, #17679 ) ;
#17212=CARTESIAN_POINT ( 'NONE',  ( 1.899999999999999911, 11.15000000000000036, -6.992551034670250827E-16 ) ) ;
#17218=VERTEX_POINT ( 'NONE', #2929 ) ;
#17219=ORIENTED_EDGE ( 'NONE', *, *, #14906, .T. ) ;
#17228=ORIENTED_EDGE ( 'NONE', *, *, #11975, .F. ) ;
#17234=CARTESIAN_POINT ( 'NONE',  ( 1.800000000000000044, 11.40000000000000036, 1.600000000000000089 ) ) ;
#17238=ORIENTED_EDGE ( 'NONE', *, *, #7167, .F. ) ;
#17244=ORIENTED_EDGE ( 'NONE', *, *, #5000, .T. ) ;
#17249=FACE_OUTER_BOUND ( 'NONE', #13353, .T. ) ;
#17251=CARTESIAN_POINT ( 'NONE',  ( -1.850000000000000089, 0.7500000000000000000, 8.300000000000000711 ) ) ;
#17253=EDGE_CURVE ( 'NONE', #10426, #17808, #4668, .T. ) ;
#17254=FACE_OUTER_BOUND ( 'NONE', #4955, .T. ) ;
#17258=LINE ( 'NONE', #10231, #9569 ) ;
#17259=ADVANCED_FACE ( 'NONE', ( #9956 ), #14025, .F. ) ;
#17261=ORIENTED_EDGE ( 'NONE', *, *, #11357, .T. ) ;
#17273=DIRECTION ( 'NONE',  ( 1.000000000000000000, -1.480297366166879989E-15, -1.850371707708599740E-16 ) ) ;
#17275=EDGE_CURVE ( 'NONE', #9237, #13339, #12362, .T. ) ;
#17277=CARTESIAN_POINT ( 'NONE',  ( 1.983927814618709873E-15, 10.80000000000000071, 8.599999999999999645 ) ) ;
#17278=ORIENTED_EDGE ( 'NONE', *, *, #12998, .T. ) ;
#17280=ORIENTED_EDGE ( 'NONE', *, *, #4038, .F. ) ;
#17281=DIRECTION ( 'NONE',  ( -3.700743415417190309E-15, 0.000000000000000000, -1.000000000000000000 ) ) ;
#17283=ORIENTED_EDGE ( 'NONE', *, *, #8391, .F. ) ;
#17285=LINE ( 'NONE', #15939, #3813 ) ;
#17290=LINE ( 'NONE', #16110, #2871 ) ;
#17291=CARTESIAN_POINT ( 'NONE',  ( -1.899999999999999911, 10.00000000000000000, 7.286648454926749993E-16 ) ) ;
#17296=ADVANCED_FACE ( 'NONE', ( #13846 ), #1167, .F. ) ;
#17299=EDGE_LOOP ( 'NONE', ( #3545, #124, #3163, #11599 ) ) ;
#17303=ORIENTED_EDGE ( 'NONE', *, *, #17581, .T. ) ;
#17305=EDGE_CURVE ( 'NONE', #5781, #12188, #14131, .T. ) ;
#17312=VECTOR ( 'NONE', #5231, 1000.000000000000000 ) ;
#17319=DIRECTION ( 'NONE',  ( 1.554023113895890109E-14, -1.000000000000000000, -1.110223024626929998E-16 ) ) ;
#17323=EDGE_CURVE ( 'NONE', #14318, #240, #16706, .T. ) ;
#17331=CARTESIAN_POINT ( 'NONE',  ( 2.500000000000000000, 2.799999999999999822, 0.6099999999999999867 ) ) ;
#17333=CARTESIAN_POINT ( 'NONE',  ( -1.899999999999999911, 2.000000000000000000, 2.388061258337340122E-16 ) ) ;
#17334=FACE_OUTER_BOUND ( 'NONE', #2339, .T. ) ;
#17335=VECTOR ( 'NONE', #12752, 1000.000000000000000 ) ;
#17337=ORIENTED_EDGE ( 'NONE', *, *, #2803, .T. ) ;
#17339=CARTESIAN_POINT ( 'NONE',  ( -1.899999999999999911, -2.607830583485260225E-17, 7.649999999999999467 ) ) ;
#17341=CARTESIAN_POINT ( 'NONE',  ( 0.5291502622129179434, -6.480221748870319920E-17, 7.700000000000000178 ) ) ;
#17344=CARTESIAN_POINT ( 'NONE',  ( 1.000000000000000000, 6.799999999999999822, 7.700000000000000178 ) ) ;
#17345=VERTEX_POINT ( 'NONE', #4018 ) ;
#17348=VECTOR ( 'NONE', #5586, 1000.000000000000000 ) ;
#17354=DIRECTION ( 'NONE',  ( 3.652293603810800245E-15, 1.332267629550185876E-15, -1.000000000000000000 ) ) ;
#17367=EDGE_CURVE ( 'NONE', #14845, #5973, #6900, .T. ) ;
#17375=AXIS2_PLACEMENT_3D ( 'NONE', #10789, #12093, #16250 ) ;
#17381=CIRCLE ( 'NONE', #9421, 0.5999999999999998668 ) ;
#17387=CARTESIAN_POINT ( 'NONE',  ( 1.889999999999999902, 7.900000000000000355, 0.5999999999999999778 ) ) ;
#17388=VECTOR ( 'NONE', #5710, 1000.000000000000000 ) ;
#17391=EDGE_CURVE ( 'NONE', #16897, #7970, #14778, .T. ) ;
#17403=ORIENTED_EDGE ( 'NONE', *, *, #10723, .T. ) ;
#17406=ORIENTED_EDGE ( 'NONE', *, *, #16421, .F. ) ;
#17409=DIRECTION ( 'NONE',  ( 1.000000000000000000, 0.000000000000000000, 0.000000000000000000 ) ) ;
#17413=ADVANCED_FACE ( 'NONE', ( #3567 ), #5148, .F. ) ;
#17423=ORIENTED_EDGE ( 'NONE', *, *, #9028, .T. ) ;
#17426=ADVANCED_FACE ( 'NONE', ( #14976 ), #11915, .F. ) ;
#17429=DIRECTION ( 'NONE',  ( 1.054711873393900133E-14, 1.000000000000000000, 0.000000000000000000 ) ) ;
#17430=EDGE_CURVE ( 'NONE', #9511, #7811, #11472, .T. ) ;
#17431=DIRECTION ( 'NONE',  ( -4.157615153618229646E-15, 1.000000000000000000, 1.972152263052530214E-30 ) ) ;
#17453=DIRECTION ( 'NONE',  ( -1.000000000000000000, 0.000000000000000000, 7.401486830834370362E-16 ) ) ;
#17455=ORIENTED_EDGE ( 'NONE', *, *, #8639, .F. ) ;
#17457=CARTESIAN_POINT ( 'NONE',  ( 1.875000000000000000, 11.25000000000000000, 7.700000000000000178 ) ) ;
#17463=EDGE_CURVE ( 'NONE', #10646, #5474, #12195, .T. ) ;
#17465=CARTESIAN_POINT ( 'NONE',  ( -1.850000000000000089, 11.25000000000000000, 7.649999999999999467 ) ) ;
#17472=CARTESIAN_POINT ( 'NONE',  ( 2.500000000000000000, -3.214554059336160952E-17, 4.000000000000000000 ) ) ;
#17474=ORIENTED_EDGE ( 'NONE', *, *, #16302, .T. ) ;
#17490=ORIENTED_EDGE ( 'NONE', *, *, #11291, .F. ) ;
#17494=CARTESIAN_POINT ( 'NONE',  ( 1.800000000000000044, 12.00000000000000000, 1.600000000000000089 ) ) ;
#17495=ORIENTED_EDGE ( 'NONE', *, *, #8391, .T. ) ;
#17506=ORIENTED_EDGE ( 'NONE', *, *, #11229, .F. ) ;
#17511=ORIENTED_EDGE ( 'NONE', *, *, #7007, .T. ) ;
#17515=ORIENTED_EDGE ( 'NONE', *, *, #15014, .F. ) ;
#17517=FACE_OUTER_BOUND ( 'NONE', #6309, .T. ) ;
#17520=LINE ( 'NONE', #14406, #8555 ) ;
#17525=CARTESIAN_POINT ( 'NONE',  ( 1.850000000000000089, 0.7500000000000000000, 8.300000000000000711 ) ) ;
#17527=CARTESIAN_POINT ( 'NONE',  ( 1.800000000000000044, 11.29999999999999893, 7.649999999999999467 ) ) ;
#17531=ORIENTED_EDGE ( 'NONE', *, *, #17253, .F. ) ;
#17533=FACE_OUTER_BOUND ( 'NONE', #17667, .T. ) ;
#17537=LINE ( 'NONE', #709, #559 ) ;
#17539=LINE ( 'NONE', #6346, #2000 ) ;
#17540=CARTESIAN_POINT ( 'NONE',  ( 2.500000000000000000, 7.299999999999999822, 0.6099999999999999867 ) ) ;
#17544=ORIENTED_EDGE ( 'NONE', *, *, #1088, .T. ) ;
#17546=DIRECTION ( 'NONE',  ( 0.000000000000000000, 0.000000000000000000, 1.000000000000000000 ) ) ;
#17549=FACE_OUTER_BOUND ( 'NONE', #11253, .T. ) ;
#17553=DIRECTION ( 'NONE',  ( -1.000000000000000000, 2.220446049250315053E-16, 6.049014748177260544E-16 ) ) ;
#17564=DIRECTION ( 'NONE',  ( 1.000000000000000000, -2.220446049250309876E-16, 0.000000000000000000 ) ) ;
#17569=ORIENTED_EDGE ( 'NONE', *, *, #3094, .T. ) ;
#17570=DIRECTION ( 'NONE',  ( 0.000000000000000000, 0.000000000000000000, -1.000000000000000000 ) ) ;
#17571=ORIENTED_EDGE ( 'NONE', *, *, #1843, .F. ) ;
#17581=EDGE_CURVE ( 'NONE', #17808, #4810, #10990, .T. ) ;
#17593=VERTEX_POINT ( 'NONE', #7002 ) ;
#17597=ADVANCED_FACE ( 'NONE', ( #5433 ), #8310, .T. ) ;
#17599=DIRECTION ( 'NONE',  ( 0.000000000000000000, -1.000000000000000000, 6.123233995736769734E-17 ) ) ;
#17611=ORIENTED_EDGE ( 'NONE', *, *, #13906, .T. ) ;
#17612=CARTESIAN_POINT ( 'NONE',  ( 1.889999999999999902, 4.700000000000000178, 0.5999999999999999778 ) ) ;
#17614=VECTOR ( 'NONE', #1748, 1000.000000000000000 ) ;
#17621=DIRECTION ( 'NONE',  ( 0.000000000000000000, -1.000000000000000000, 0.000000000000000000 ) ) ;
#17623=AXIS2_PLACEMENT_3D ( 'NONE', #9719, #7220, #12584 ) ;
#17628=EDGE_CURVE ( 'NONE', #2153, #8790, #9509, .T. ) ;
#17633=VECTOR ( 'NONE', #1772, 1000.000000000000000 ) ;
#17634=LINE ( 'NONE', #3580, #9971 ) ;
#17637=ORIENTED_EDGE ( 'NONE', *, *, #4267, .F. ) ;
#17639=DIRECTION ( 'NONE',  ( 0.000000000000000000, 0.000000000000000000, 1.000000000000000000 ) ) ;
#17640=CIRCLE ( 'NONE', #4064, 0.1000000000000000472 ) ;
#17646=EDGE_CURVE ( 'NONE', #4096, #11111, #8209, .T. ) ;
#17649=DIRECTION ( 'NONE',  ( -1.000000000000000000, 0.000000000000000000, 0.000000000000000000 ) ) ;
#17653=EDGE_CURVE ( 'NONE', #389, #13169, #11072, .T. ) ;
#17656=EDGE_CURVE ( 'NONE', #11991, #14398, #16716, .T. ) ;
#17658=DIRECTION ( 'NONE',  ( 1.000000000000000000, 0.000000000000000000, -7.401486830834380223E-16 ) ) ;
#17663=VECTOR ( 'NONE', #289, 1000.000000000000000 ) ;
#17667=EDGE_LOOP ( 'NONE', ( #16356, #2659, #16191, #3489, #3189, #632, #4321, #5615 ) ) ;
#17673=DIRECTION ( 'NONE',  ( 1.110223024625160090E-15, 1.000000000000000000, 0.000000000000000000 ) ) ;
#17679=VECTOR ( 'NONE', #12801, 1000.000000000000000 ) ;
#17681=AXIS2_PLACEMENT_3D ( 'NONE', #11191, #16836, #4146 ) ;
#17684=EDGE_CURVE ( 'NONE', #16414, #5991, #6758, .T. ) ;
#17696=EDGE_CURVE ( 'NONE', #17047, #2205, #1175, .T. ) ;
#17699=EDGE_LOOP ( 'NONE', ( #2637, #2554, #3705, #17406 ) ) ;
#17708=CARTESIAN_POINT ( 'NONE',  ( 0.03000000000000110217, 11.40000000000000036, 7.649999999999999467 ) ) ;
#17716=ORIENTED_EDGE ( 'NONE', *, *, #1720, .T. ) ;
#17723=EDGE_CURVE ( 'NONE', #16395, #9909, #11806, .T. ) ;
#17724=ORIENTED_EDGE ( 'NONE', *, *, #13543, .T. ) ;
#17725=CYLINDRICAL_SURFACE ( 'NONE', #8892, 0.6000000000000000888 ) ;
#17731=ADVANCED_FACE ( 'NONE', ( #769 ), #3357, .T. ) ;
#17735=LINE ( 'NONE', #5064, #12350 ) ;
#17739=CARTESIAN_POINT ( 'NONE',  ( -0.03000000000000000236, 11.40000000000000036, -2.869354249208270301E-17 ) ) ;
#17747=ORIENTED_EDGE ( 'NONE', *, *, #11970, .T. ) ;
#17750=VERTEX_POINT ( 'NONE', #18062 ) ;
#17756=DIRECTION ( 'NONE',  ( -1.000000000000000000, 1.480297366166869931E-15, 0.000000000000000000 ) ) ;
#17763=DIRECTION ( 'NONE',  ( -0.2721173643531200059, 0.9622640697945191723, 0.000000000000000000 ) ) ;
#17764=VERTEX_POINT ( 'NONE', #3912 ) ;
#17770=EDGE_LOOP ( 'NONE', ( #13835, #4103, #2885, #527 ) ) ;
#17772=CARTESIAN_POINT ( 'NONE',  ( 2.500000000000000000, 3.500000000000000000, 0.6099999999999999867 ) ) ;
#17775=LINE ( 'NONE', #16501, #7017 ) ;
#17781=VERTEX_POINT ( 'NONE', #5211 ) ;
#17789=ORIENTED_EDGE ( 'NONE', *, *, #1276, .F. ) ;
#17791=CIRCLE ( 'NONE', #10136, 0.8000000000000000444 ) ;
#17794=CARTESIAN_POINT ( 'NONE',  ( 2.500000000000000000, 2.799999999999999822, 0.6099999999999999867 ) ) ;
#17808=VERTEX_POINT ( 'NONE', #4102 ) ;
#17810=DIRECTION ( 'NONE',  ( 0.000000000000000000, -1.000000000000000000, 0.000000000000000000 ) ) ;
#17813=ORIENTED_EDGE ( 'NONE', *, *, #11051, .F. ) ;
#17816=DIRECTION ( 'NONE',  ( 0.000000000000000000, 0.000000000000000000, -1.000000000000000000 ) ) ;
#17818=CARTESIAN_POINT ( 'NONE',  ( -2.200000000000000178, -2.672352773677590478E-16, 4.000000000000000000 ) ) ;
#17824=ORIENTED_EDGE ( 'NONE', *, *, #13839, .T. ) ;
#17825=ADVANCED_FACE ( 'NONE', ( #1055 ), #6693, .F. ) ;
#17826=EDGE_CURVE ( 'NONE', #8528, #1801, #11044, .T. ) ;
#17835=CARTESIAN_POINT ( 'NONE',  ( 1.890000000000029878, 4.100000000000000533, 3.000000000000000000 ) ) ;
#17837=EDGE_LOOP ( 'NONE', ( #15960, #16043, #9705 ) ) ;
#17842=CIRCLE ( 'NONE', #12251, 0.4000000000000001887 ) ;
#17845=PLANE ( 'NONE',  #15876 ) ;
#17851=ORIENTED_EDGE ( 'NONE', *, *, #5415, .T. ) ;
#17853=PLANE ( 'NONE',  #11928 ) ;
#17855=CIRCLE ( 'NONE', #12860, 0.5999999999999998668 ) ;
#17858=DIRECTION ( 'NONE',  ( -1.000000000000000000, 0.000000000000000000, 0.000000000000000000 ) ) ;
#17874=CARTESIAN_POINT ( 'NONE',  ( -2.500000000000000000, 2.000000000000000000, 1.600000000000000089 ) ) ;
#17875=PLANE ( 'NONE',  #4085 ) ;
#17877=( NAMED_UNIT ( * ) PLANE_ANGLE_UNIT ( ) SI_UNIT ( $, .RADIAN. ) );
#17885=CARTESIAN_POINT ( 'NONE',  ( -1.889999999999999902, 7.299999999999999822, 0.5999999999999999778 ) ) ;
#17889=DIRECTION ( 'NONE',  ( 8.997169018144999103E-17, -9.633757521571540356E-31, -1.000000000000000000 ) ) ;
#17892=CARTESIAN_POINT ( 'NONE',  ( 0.000000000000000000, 0.000000000000000000, 8.300000000000000711 ) ) ;
#17902=ORIENTED_EDGE ( 'NONE', *, *, #14944, .T. ) ;
#17903=ORIENTED_EDGE ( 'NONE', *, *, #9808, .F. ) ;
#17904=DIRECTION ( 'NONE',  ( 0.000000000000000000, 0.000000000000000000, 1.000000000000000000 ) ) ;
#17906=CARTESIAN_POINT ( 'NONE',  ( 1.983927814618709873E-15, 10.80000000000000071, 8.599999999999999645 ) ) ;
#17911=VECTOR ( 'NONE', #2053, 1000.000000000000000 ) ;
#17918=VECTOR ( 'NONE', #11650, 1000.000000000000000 ) ;
#17919=CYLINDRICAL_SURFACE ( 'NONE', #10019, 0.6500000000000003553 ) ;
#17926=ORIENTED_EDGE ( 'NONE', *, *, #1276, .T. ) ;
#17928=AXIS2_PLACEMENT_3D ( 'NONE', #110, #9743, #5757 ) ;
#17929=VERTEX_POINT ( 'NONE', #2450 ) ;
#17935=ADVANCED_FACE ( 'NONE', ( #3721 ), #8180, .T. ) ;
#17943=FACE_OUTER_BOUND ( 'NONE', #5748, .T. ) ;
#17945=AXIS2_PLACEMENT_3D ( 'NONE', #4641, #7441, #1953 ) ;
#17946=ORIENTED_EDGE ( 'NONE', *, *, #9405, .F. ) ;
#17948=DIRECTION ( 'NONE',  ( -7.401486830834380223E-16, -1.000000000000000000, 0.000000000000000000 ) ) ;
#17952=EDGE_CURVE ( 'NONE', #1650, #10646, #13923, .T. ) ;
#17954=ORIENTED_EDGE ( 'NONE', *, *, #12319, .T. ) ;
#17955=DIRECTION ( 'NONE',  ( 0.000000000000000000, 0.000000000000000000, 1.000000000000000000 ) ) ;
#17959=AXIS2_PLACEMENT_3D ( 'NONE', #2323, #7972, #3884 ) ;
#17963=CARTESIAN_POINT ( 'NONE',  ( 1.889999999999999902, 8.500000000000000000, 0.6099999999999999867 ) ) ;
#17966=VECTOR ( 'NONE', #17673, 1000.000000000000000 ) ;
#17969=ORIENTED_EDGE ( 'NONE', *, *, #9808, .T. ) ;
#17970=ADVANCED_FACE ( 'NONE', ( #1323 ), #11132, .T. ) ;
#17984=CARTESIAN_POINT ( 'NONE',  ( 2.500000000000000000, 11.15000000000000036, 1.600000000000000089 ) ) ;
#17988=DIRECTION ( 'NONE',  ( 0.000000000000000000, 0.000000000000000000, -1.000000000000000000 ) ) ;
#17992=CARTESIAN_POINT ( 'NONE',  ( -11.62823001646920140, -7.413791402719209319E-16, 0.5999999999999698908 ) ) ;
#18001=DIRECTION ( 'NONE',  ( 2.242874797222529735E-16, 0.000000000000000000, 1.000000000000000000 ) ) ;
#18002=CIRCLE ( 'NONE', #8850, 1.016666666666670160 ) ;
#18007=DIRECTION ( 'NONE',  ( 0.000000000000000000, 0.000000000000000000, -1.000000000000000000 ) ) ;
#18009=DIRECTION ( 'NONE',  ( 1.807003620809174583E-15, 1.000000000000000000, 1.807003620809174385E-16 ) ) ;
#18012=VECTOR ( 'NONE', #3497, 1000.000000000000000 ) ;
#18016=CARTESIAN_POINT ( 'NONE',  ( 2.500000000000000000, 9.199999999999999289, 1.600000000000000089 ) ) ;
#18023=DIRECTION ( 'NONE',  ( 0.000000000000000000, 0.000000000000000000, 1.000000000000000000 ) ) ;
#18024=CARTESIAN_POINT ( 'NONE',  ( 1.899999999999999911, 3.500000000000000000, 0.6099999999999999867 ) ) ;
#18025=EDGE_LOOP ( 'NONE', ( #7293, #1284, #8148, #18135 ) ) ;
#18029=ADVANCED_FACE ( 'NONE', ( #8821 ), #14473, .F. ) ;
#18032=CARTESIAN_POINT ( 'NONE',  ( -1.599999999999869971, 12.00000000000000000, -2.399999999999999911 ) ) ;
#18035=DIRECTION ( 'NONE',  ( -2.168404344971009262E-15, -1.000000000000000000, -2.220446049250220143E-16 ) ) ;
#18037=DIRECTION ( 'NONE',  ( -4.440892098500630895E-15, 1.000000000000000000, 0.000000000000000000 ) ) ;
#18046=CARTESIAN_POINT ( 'NONE',  ( 1.875000000000000000, -2.296212748401290437E-16, 7.700000000000000178 ) ) ;
#18048=DIRECTION ( 'NONE',  ( -2.529805069132844337E-15, 1.000000000000000000, 1.807003620809174385E-16 ) ) ;
#18053=EDGE_CURVE ( 'NONE', #14775, #12624, #9428, .T. ) ;
#18056=EDGE_CURVE ( 'NONE', #6568, #11460, #11486, .T. ) ;
#18060=DIRECTION ( 'NONE',  ( 6.672013369141562259E-16, 0.000000000000000000, 1.000000000000000000 ) ) ;
#18062=CARTESIAN_POINT ( 'NONE',  ( -2.500000000000000000, 7.299999999999999822, 0.6099999999999999867 ) ) ;
#18076=LINE ( 'NONE', #9671, #10415 ) ;
#18079=VECTOR ( 'NONE', #18112, 1000.000000000000000 ) ;
#18084=ORIENTED_EDGE ( 'NONE', *, *, #3475, .F. ) ;
#18093=EDGE_CURVE ( 'NONE', #1995, #12906, #6215, .T. ) ;
#18101=DIRECTION ( 'NONE',  ( 1.000000000000000000, 0.000000000000000000, -7.401486830834370362E-16 ) ) ;
#18102=DIRECTION ( 'NONE',  ( 2.220446049250309876E-16, 1.000000000000000000, -1.064962222048364037E-31 ) ) ;
#18104=ORIENTED_EDGE ( 'NONE', *, *, #7129, .F. ) ;
#18107=DIRECTION ( 'NONE',  ( 3.097720492815730124E-16, 1.000000000000000000, 0.000000000000000000 ) ) ;
#18108=CARTESIAN_POINT ( 'NONE',  ( -2.500000000000000000, 1.071484571201660082E-16, -8.514390157257050626E-16 ) ) ;
#18112=DIRECTION ( 'NONE',  ( 0.000000000000000000, 1.000000000000000000, 0.000000000000000000 ) ) ;
#18116=FACE_OUTER_BOUND ( 'NONE', #17, .T. ) ;
#18118=DIRECTION ( 'NONE',  ( 1.000000000000000000, 0.000000000000000000, 0.000000000000000000 ) ) ;
#18120=ORIENTED_EDGE ( 'NONE', *, *, #6072, .T. ) ;
#18123=ORIENTED_EDGE ( 'NONE', *, *, #10412, .F. ) ;
#18124=VERTEX_POINT ( 'NONE', #4633 ) ;
#18128=CARTESIAN_POINT ( 'NONE',  ( 1.800000000000000044, 12.00000000000000000, 1.600000000000000089 ) ) ;
#18130=DIRECTION ( 'NONE',  ( 1.216682766712499758E-16, 4.229421046191059358E-17, 1.000000000000000000 ) ) ;
#18131=DIRECTION ( 'NONE',  ( 7.401486830834370362E-16, 0.000000000000000000, 1.000000000000000000 ) ) ;
#18132=CARTESIAN_POINT ( 'NONE',  ( -2.500000000000000000, 2.000000000000000000, -2.537652627714639929E-16 ) ) ;
#18135=ORIENTED_EDGE ( 'NONE', *, *, #2275, .T. ) ;
#18147=EDGE_LOOP ( 'NONE', ( #10156, #4911, #11723 ) ) ;
#18149=EDGE_CURVE ( 'NONE', #12817, #4099, #10556, .T. ) ;
#18152=FACE_OUTER_BOUND ( 'NONE', #634, .T. ) ;
#18153=CARTESIAN_POINT ( 'NONE',  ( 2.500000000000000000, 11.29999999999999893, 7.649999999999999467 ) ) ;
#18154=CARTESIAN_POINT ( 'NONE',  ( 2.500000000000000000, 0.7500000000000000000, 7.649999999999999467 ) ) ;
#18158=DIRECTION ( 'NONE',  ( -1.853875224168160112E-15, -1.000000000000000000, -2.960594732333760372E-15 ) ) ;
#18159=DIRECTION ( 'NONE',  ( -0.000000000000000000, 1.000000000000000000, 0.000000000000000000 ) ) ;
#18164=VERTEX_POINT ( 'NONE', #14926 ) ;
#18165=EDGE_CURVE ( 'NONE', #6674, #12720, #3263, .T. ) ;
#18167=DIRECTION ( 'NONE',  ( 1.000000000000000000, -1.103950578158349959E-14, 0.000000000000000000 ) ) ;
#18170=ORIENTED_EDGE ( 'NONE', *, *, #4848, .F. ) ;
#18180=CARTESIAN_POINT ( 'NONE',  ( -1.899999999999999911, 2.799999999999999822, 1.600000000000000089 ) ) ;
#18186=EDGE_LOOP ( 'NONE', ( #9310, #6384, #7498, #5495 ) ) ;
#18187=CIRCLE ( 'NONE', #2251, 0.4166666666666671848 ) ;
#18189=DIRECTION ( 'NONE',  ( 1.000000000000000000, 0.000000000000000000, -6.049014748177260544E-16 ) ) ;
#18190=CARTESIAN_POINT ( 'NONE',  ( -1.800000000000000044, 11.29999999999999893, 1.600000000000000089 ) ) ;
#18192=EDGE_CURVE ( 'NONE', #14967, #9046, #12378, .T. ) ;
#18196=CARTESIAN_POINT ( 'NONE',  ( 1.875000000000000000, 11.25000000000000000, 7.700000000000000178 ) ) ;
#18199=DIRECTION ( 'NONE',  ( -7.109522442527898025E-16, 0.000000000000000000, -1.000000000000000000 ) ) ;
#18201=DIRECTION ( 'NONE',  ( 0.000000000000000000, 0.000000000000000000, -1.000000000000000000 ) ) ;
#18202=CARTESIAN_POINT ( 'NONE',  ( 1.800000000000000044, 12.00000000000000000, 7.649999999999999467 ) ) ;
#18204=AXIS2_PLACEMENT_3D ( 'NONE', #14759, #15061, #2370 ) ;
#18205=EDGE_CURVE ( 'NONE', #7679, #4501, #16217, .T. ) ;
#18207=CIRCLE ( 'NONE', #10240, 0.4000000000000000222 ) ;
#18208=EDGE_LOOP ( 'NONE', ( #16937, #14346 ) ) ;
#18210=ORIENTED_EDGE ( 'NONE', *, *, #3519, .F. ) ;
#18211=LINE ( 'NONE', #10009, #15787 ) ;
#18213=ORIENTED_EDGE ( 'NONE', *, *, #14564, .T. ) ;
#18214=ORIENTED_EDGE ( 'NONE', *, *, #10288, .F. ) ;
#18225=DIRECTION ( 'NONE',  ( 0.000000000000000000, -1.000000000000000000, 0.000000000000000000 ) ) ;
#18226=FACE_OUTER_BOUND ( 'NONE', #15927, .T. ) ;
#18233=AXIS2_PLACEMENT_3D ( 'NONE', #6483, #11946, #14916 ) ;
#18235=CARTESIAN_POINT ( 'NONE',  ( 1.800000000000000044, 11.40000000000000036, 1.600000000000000089 ) ) ;
#18240=VECTOR ( 'NONE', #16363, 1000.000000000000000 ) ;
#18243=DIRECTION ( 'NONE',  ( 0.000000000000000000, 0.000000000000000000, -1.000000000000000000 ) ) ;
#18244=VERTEX_POINT ( 'NONE', #9266 ) ;
#18253=VERTEX_POINT ( 'NONE', #16924 ) ;
#18258=DIRECTION ( 'NONE',  ( 1.216682766712499758E-16, 4.229421046191059358E-17, 1.000000000000000000 ) ) ;
#18262=CYLINDRICAL_SURFACE ( 'NONE', #9842, 1.016666666666670160 ) ;
#18263=AXIS2_PLACEMENT_3D ( 'NONE', #5264, #6458, #6267 ) ;
#18268=ADVANCED_FACE ( 'NONE', ( #1286 ), #5728, .T. ) ;
#18269=DIRECTION ( 'NONE',  ( -1.000000000000000000, 0.000000000000000000, 0.000000000000000000 ) ) ;
#18282=EDGE_CURVE ( 'NONE', #15780, #13146, #9108, .T. ) ;
#18288=ORIENTED_EDGE ( 'NONE', *, *, #11975, .T. ) ;
ENDSEC;
END-ISO-10303-21;
